ISO-10303-21;
HEADER;
FILE_DESCRIPTION (('STEP AP214'),
    '1' );
FILE_NAME ('Terminal Screw 2.step',
    '2026-10-05T22:38:29',
    ( '' ),
    ( '' ),
    'SwSTEP 2.0',
    'SolidWorks 2020',
    '' );
FILE_SCHEMA (( 'AUTOMOTIVE_DESIGN' ));
ENDSEC;

DATA;
#2=CARTESIAN_POINT ( 'NONE',  ( 10.88210843320517007, 2.862311695598936723, 6.901605483505062644 ) ) ;
#6=CARTESIAN_POINT ( 'NONE',  ( 11.11718313518939816, 3.377550038693600154, 6.712912394634500401 ) ) ;
#21=ADVANCED_FACE ( 'NONE', ( #67495 ), #4617, .T. ) ;
#37=CARTESIAN_POINT ( 'NONE',  ( 8.691343736187999269, 3.625767601089900261, 6.690658690097199823 ) ) ;
#38=CARTESIAN_POINT ( 'NONE',  ( 11.59999999999999964, 3.116215992411100366, 7.174999999999999822 ) ) ;
#54=CARTESIAN_POINT ( 'NONE',  ( 9.804975701332999449, 4.636077325177999420, 6.910836541441499392 ) ) ;
#86=CARTESIAN_POINT ( 'NONE',  ( 11.05435090131019926, 5.119447121461000449, 6.807613609764599616 ) ) ;
#98=CARTESIAN_POINT ( 'NONE',  ( 8.592138961223998450, 5.059894361919000438, 6.783753885003399375 ) ) ;
#108=CARTESIAN_POINT ( 'NONE',  ( 9.860128811416625894, 4.869607263996035940, 7.403483289911290122 ) ) ;
#135=CARTESIAN_POINT ( 'NONE',  ( 10.08963399569799790, 5.271405458160000279, 7.358888170452400068 ) ) ;
#162=EDGE_CURVE ( 'NONE', #21254, #36556, #58057, .T. ) ;
#230=CARTESIAN_POINT ( 'NONE',  ( 10.29399293566599916, 4.546741702992100009, 6.829299525004299376 ) ) ;
#319=CARTESIAN_POINT ( 'NONE',  ( 10.29262282008599882, 4.451581486939200083, 6.771613406921599854 ) ) ;
#334=CARTESIAN_POINT ( 'NONE',  ( 10.98579841651039857, 3.550031058388499972, 6.303820944768999901 ) ) ;
#346=CARTESIAN_POINT ( 'NONE',  ( 10.74795391537419853, 4.830118059977199785, 6.936213817702099327 ) ) ;
#361=DIRECTION ( 'NONE',  ( 0.000000000000000000, 1.000000000000000000, 0.000000000000000000 ) ) ;
#379=CARTESIAN_POINT ( 'NONE',  ( 8.717397846562217723, 3.754687009553119736, 6.659228100213050006 ) ) ;
#396=CARTESIAN_POINT ( 'NONE',  ( 11.00000000000000000, 3.031410575668799900, 7.825000000000000178 ) ) ;
#399=CARTESIAN_POINT ( 'NONE',  ( 10.99999975383417627, 2.937013229513552925, 7.633391978603163430 ) ) ;
#410=CARTESIAN_POINT ( 'NONE',  ( 11.04749144726329924, 3.499163784537000055, 8.206726025856399431 ) ) ;
#427=CARTESIAN_POINT ( 'NONE',  ( 10.43614141025499897, 4.549633050978300730, 6.521048559232099251 ) ) ;
#442=ORIENTED_EDGE ( 'NONE', *, *, #23207, .F. ) ;
#453=CARTESIAN_POINT ( 'NONE',  ( 9.150912690312626552, 3.194792839887663938, 7.157693560935859622 ) ) ;
#456=CARTESIAN_POINT ( 'NONE',  ( 11.41486084871699802, 2.792989229543000107, 7.174999999999999822 ) ) ;
#475=ADVANCED_FACE ( 'NONE', ( #66987 ), #44994, .T. ) ;
#479=CARTESIAN_POINT ( 'NONE',  ( 9.758342523874999230, 2.871335344632000020, 7.672773098917999413 ) ) ;
#534=EDGE_CURVE ( 'NONE', #39090, #52961, #7578, .T. ) ;
#574=CARTESIAN_POINT ( 'NONE',  ( 8.599999952505998024, 4.000000000000000000, 7.500000000000000000 ) ) ;
#579=CARTESIAN_POINT ( 'NONE',  ( 10.40480513895999870, 4.779740423663599636, 7.933462475324499330 ) ) ;
#613=B_SPLINE_SURFACE_WITH_KNOTS ( 'NONE', 3, 3, ( 
 ( #37486, #31912, #20724, #14796, #5326, #20038, #26668, #47984, #15137, #57429, #36115, #42052, #31566, #58467, #4984, #21069, #25628, #47300, #9888, #15820, #86, #25972, #51846, #42737, #36458, #9535, #25283, #4633, #64041, #41367, #47646, #16162, #46617, #58812, #4292 ),
 ( #30533, #3944, #30880, #26318, #52193, #36812, #46956, #68259, #41705, #63008, #57777, #31229, #52536, #68604, #63358, #15485, #58130, #10231, #54603, #43434, #6007, #17900, #33636, #38166, #48323, #49350, #65428, #49014, #11949, #59496, #54248, #27347, #32260, #53569, #427 ),
 ( #44483, #16844, #21743, #39217, #1121, #59843, #1812, #10916, #23132, #5664, #11594, #32593, #27005, #54952, #17551, #44130, #33288, #48669, #1465, #43075, #22780, #64382, #49703, #16503, #37830, #59153, #11255, #65774, #53907, #32938, #774, #22089, #22434, #64728, #6350 ),
 ( #27698, #43776, #6701, #65070, #38877, #17190, #60199, #38521, #28042, #12303, #7053, #28389, #50745, #23481, #14033, #50058, #56681, #35359, #45161, #18243, #44820, #2842, #61575, #19264, #13691, #51088, #55649, #8095, #39917, #24518, #8780, #55991, #12649, #3190, #66467 ) ),
 .UNSPECIFIED., .F., .F., .F.,
 ( 4, 4 ),
 ( 4, 1, 1, 1, 1, 1, 1, 1, 1, 1, 1, 1, 1, 1, 1, 1, 1, 1, 1, 1, 1, 1, 1, 1, 1, 1, 1, 1, 1, 1, 1, 1, 4 ),
 ( -0.02000000000000000042, 1.020000000000000018 ),
 ( 0.1633025096610999927, 0.1899619885200000136, 0.2166214673788000034, 0.2432809462376999965, 0.2699404250964999585, 0.2965999039553000038, 0.3232593828141999692, 0.3499188616730000145, 0.3765783405318000043, 0.4032378193906999697, 0.4298972982494999595, 0.4565567771083000048, 0.4832162559671999702, 0.5098757348260000155, 0.5365352136848999809, 0.5631946925437000262, 0.5898541714025000715, 0.6165136502614000369, 0.6431731291201999712, 0.6698326079790000165, 0.6964920868378999819, 0.7231515656967000272, 0.7498110445554999615, 0.7764705234143999268, 0.8031300022731999722, 0.8297894811320000175, 0.8564489599908999828, 0.8831084388497000282, 0.9097679177085999935, 0.9364273965674000388, 0.9630868754261999731, 0.9897463542851000495, 1.016405833144000015 ),
 .UNSPECIFIED. ) ;
#623=CARTESIAN_POINT ( 'NONE',  ( 10.40769129028899975, 3.110563525881361535, 6.586710612921465646 ) ) ;
#667=CARTESIAN_POINT ( 'NONE',  ( 10.45257053952200010, 3.605640676136899980, 8.422730500489899796 ) ) ;
#682=CARTESIAN_POINT ( 'NONE',  ( 11.61759063708296047, 5.217265640542000149, 7.157757529645699890 ) ) ;
#695=CARTESIAN_POINT ( 'NONE',  ( 11.31410538575739899, 4.975963290822400076, 7.733337754805098996 ) ) ;
#743=CARTESIAN_POINT ( 'NONE',  ( 8.791809814040998816, 4.530359890157599878, 6.814123855771700100 ) ) ;
#747=CARTESIAN_POINT ( 'NONE',  ( 11.00000000000000000, 2.941427501403999667, 7.174999999999999822 ) ) ;
#774=CARTESIAN_POINT ( 'NONE',  ( 10.48280513895999988, 4.903310631086600146, 8.002155910165599906 ) ) ;
#802=CARTESIAN_POINT ( 'NONE',  ( 10.26539516633362759, 4.233208782175254647, 6.656705459454948404 ) ) ;
#824=CARTESIAN_POINT ( 'NONE',  ( 11.39700581613019992, 4.869652672166700391, 6.941573685175900010 ) ) ;
#826=CARTESIAN_POINT ( 'NONE',  ( 10.06229229006299875, 4.987433183662999703, 8.073332500201798823 ) ) ;
#830=EDGE_CURVE ( 'NONE', #13026, #36556, #49687, .T. ) ;
#832=CARTESIAN_POINT ( 'NONE',  ( 10.56059687351646481, 4.629523725463624118, 6.407767014557177454 ) ) ;
#878=CARTESIAN_POINT ( 'NONE',  ( 10.18988779216199880, 5.056118594996999782, 7.119137915499500480 ) ) ;
#925=CARTESIAN_POINT ( 'NONE',  ( 11.44366954483529852, 4.485203148598100320, 8.248643701125299543 ) ) ;
#932=CARTESIAN_POINT ( 'NONE',  ( 10.19810941423799910, 4.946022705791000007, 8.359277272599898723 ) ) ;
#1016=CARTESIAN_POINT ( 'NONE',  ( 11.43718179236249988, 3.790319673775199849, 8.481317998227099864 ) ) ;
#1030=CARTESIAN_POINT ( 'NONE',  ( 11.10887482311539998, 5.184953745778000389, 7.021250586468399391 ) ) ;
#1047=CARTESIAN_POINT ( 'NONE',  ( 11.01872200990539952, 3.052519557825900343, 7.830502140005199507 ) ) ;
#1082=DIRECTION ( 'NONE',  ( 0.000000000000000000, 1.000000000000000000, 0.000000000000000000 ) ) ;
#1108=CARTESIAN_POINT ( 'NONE',  ( 10.60441638348510018, 3.158410350011299883, 7.705001100909899314 ) ) ;
#1121=CARTESIAN_POINT ( 'NONE',  ( 11.56322412107030928, 4.054600656575539475, 8.532060764998998792 ) ) ;
#1140=CARTESIAN_POINT ( 'NONE',  ( 10.55068303964747578, 3.428091289053144308, 8.161067340483363353 ) ) ;
#1142=B_SPLINE_CURVE_WITH_KNOTS ( 'NONE', 3,
 ( #7494, #49808, #55750, #28491, #28141, #34774, #17656, #49454, #65874, #33737, #55052, #40018, #67853, #28849, #2261, #50495, #8191, #50158 ),
 .UNSPECIFIED., .F., .F.,
 ( 4, 2, 2, 2, 2, 2, 2, 2, 4 ),
 ( 0.000000000000000000, 0.1250000000000000000, 0.2500000000000000000, 0.3750000000000000000, 0.5000000000000000000, 0.6250000000000000000, 0.7500000000000000000, 0.8750000000000000000, 1.000000000000000000 ),
 .UNSPECIFIED. ) ;
#1151=CARTESIAN_POINT ( 'NONE',  ( 10.01210369451062654, 3.801861024511436593, 8.352216648108843344 ) ) ;
#1169=CARTESIAN_POINT ( 'NONE',  ( 10.85679632507500081, 4.490665650747399873, 6.590394082213600235 ) ) ;
#1171=CARTESIAN_POINT ( 'NONE',  ( 9.429063610504998749, 4.468346739194200445, 6.458661544034999480 ) ) ;
#1178=EDGE_CURVE ( 'NONE', #50051, #21433, #30369, .T. ) ;
#1182=DIRECTION ( 'NONE',  ( 0.000000000000000000, -1.000000000000000000, 0.000000000000000000 ) ) ;
#1217=CARTESIAN_POINT ( 'NONE',  ( 11.04752711762115780, 5.162390711389719833, 7.175009463222314032 ) ) ;
#1219=VERTEX_POINT ( 'NONE', #59857 ) ;
#1220=CARTESIAN_POINT ( 'NONE',  ( 9.229392757687000071, 4.677963304775400566, 6.758914271013199304 ) ) ;
#1229=CARTESIAN_POINT ( 'NONE',  ( 9.535355082327999554, 3.611978631017199959, 8.275336934318801241 ) ) ;
#1231=VERTEX_POINT ( 'NONE', #55311 ) ;
#1266=CARTESIAN_POINT ( 'NONE',  ( 10.52946886766499901, 3.569835351907400423, 8.281567006984099422 ) ) ;
#1272=CARTESIAN_POINT ( 'NONE',  ( 10.14887885159599890, 5.269014563305000287, 7.651388779553199626 ) ) ;
#1352=CARTESIAN_POINT ( 'NONE',  ( 11.04333729122639873, 2.996877626170000308, 7.526388557597149642 ) ) ;
#1369=CARTESIAN_POINT ( 'NONE',  ( 11.20733594839949809, 4.840266102192999575, 8.462948211532999920 ) ) ;
#1384=CARTESIAN_POINT ( 'NONE',  ( 10.92026088462129962, 4.002135146349410810, 8.503467136482999678 ) ) ;
#1389=CARTESIAN_POINT ( 'NONE',  ( 8.736413463905998711, 4.084156314540369870, 6.617590440947399344 ) ) ;
#1406=CARTESIAN_POINT ( 'NONE',  ( 8.783078676347997771, 3.752732269140699906, 6.553315803938899897 ) ) ;
#1416=B_SPLINE_CURVE_WITH_KNOTS ( 'NONE', 3,
 ( #37175, #68632, #53599, #456 ),
 .UNSPECIFIED., .F., .F.,
 ( 4, 4 ),
 ( 0.000000000000000000, 1.000000000000000000 ),
 .UNSPECIFIED. ) ;
#1452=CARTESIAN_POINT ( 'NONE',  ( 10.72749279009019929, 3.774717370312400178, 6.663611138821799784 ) ) ;
#1461=VECTOR ( 'NONE', #1082, 1000.000000000000000 ) ;
#1465=CARTESIAN_POINT ( 'NONE',  ( 10.98146005378009882, 4.911671201000399556, 7.986817550794899745 ) ) ;
#1513=CARTESIAN_POINT ( 'NONE',  ( 11.67403632436368888, 3.023821283238099955, 7.727966254184200245 ) ) ;
#1515=CARTESIAN_POINT ( 'NONE',  ( 9.329759580229000093, 2.755835090116000696, 7.797385380423699885 ) ) ;
#1519=CARTESIAN_POINT ( 'NONE',  ( 10.59184687351642751, 4.999583552997727054, 6.731816600031356401 ) ) ;
#1561=CARTESIAN_POINT ( 'NONE',  ( 9.406696787962999906, 4.172481380750499902, 8.489491017455099708 ) ) ;
#1568=CARTESIAN_POINT ( 'NONE',  ( 10.03992546752099990, 2.997990738918999920, 7.569424354486659290 ) ) ;
#1599=B_SPLINE_SURFACE_WITH_KNOTS ( 'NONE', 3, 3, ( 
 ( #37380, #15714, #30765, #37042, #58357, #20269, #42628, #36701, #58021, #26555, #46504, #9088, #52075, #57321, #10123, #4521, #10459, #14686, #25857, #4179, #3831, #25169, #9422, #25518, #47537, #46846, #41595, #41252, #62567, #68150, #19931, #31801, #31455, #15025, #62904, #52773, #36349, #47882, #31121, #69186, #57664, #53117, #21298, #4868, #5219, #63938, #9770, #26209, #16049, #30427, #15372, #51737, #67807, #68842, #36005, #20960, #42298, #63596, #52424, #47190, #68491, #20615, #41939, #63247, #54491, #319, #17433 ),
 ( #22669, #48563, #64277, #6592, #6936, #17788, #53465, #28271, #27933, #11834, #49591, #5897, #38061, #11152, #23018, #1016, #21635, #22324, #32826, #60087, #64963, #42970, #43666, #58702, #54142, #5558, #16394, #17076, #38762, #49242, #44366, #1352, #65665, #38409, #44012, #1698, #65317, #12193, #37721, #10805, #48908, #33521, #59733, #27582, #33174, #59385, #6240, #32149, #26900, #54840, #48212, #59050, #32486, #27239, #53800, #667, #21979, #43320, #64624, #16732, #11486, #56217, #49940, #55182, #24745, #3069, #28979 ),
 ( #13239, #50286, #8667, #23711, #18473, #61802, #7632, #45046, #61462, #45389, #46071, #67377, #29317, #7287, #24402, #39799, #2051, #66700, #28626, #23370, #66354, #55534, #56560, #13919, #34565, #18822, #61123, #44710, #34901, #55878, #30012, #24056, #18130, #51315, #60430, #39106, #35246, #7984, #40147, #50630, #3410, #12538, #33867, #66007, #2731, #2387, #39452, #45732, #13581, #60771, #8327, #29670, #50973, #67040, #12886, #19151, #34215, #40473, #47447, #30679, #53034, #47105, #68402, #36959, #56902, #47800, #62480 ),
 ( #20870, #26467, #5130, #9683, #9001, #4779, #20180, #51650, #25774, #35590, #30344, #25428, #35921, #58273, #63511, #14938, #20525, #41507, #3747, #15286, #4091, #10376, #4435, #67717, #31714, #40818, #19501, #15628, #57579, #41851, #46761, #62143, #14262, #25083, #46416, #68064, #51986, #19844, #52683, #31033, #41173, #62819, #9334, #63157, #36262, #14601, #26119, #57234, #68753, #42209, #52341, #36610, #57936, #10032, #31371, #37295, #29148, #42887, #48132, #932, #64535, #1272, #5480, #16652, #21551, #63852, #15965 ) ),
 .UNSPECIFIED., .F., .F., .F.,
 ( 4, 4 ),
 ( 4, 1, 1, 1, 1, 1, 1, 1, 1, 1, 1, 1, 1, 1, 1, 1, 1, 1, 1, 1, 1, 1, 1, 1, 1, 1, 1, 1, 1, 1, 1, 1, 1, 1, 1, 1, 1, 1, 1, 1, 1, 1, 1, 1, 1, 1, 1, 1, 1, 1, 1, 1, 1, 1, 1, 1, 1, 1, 1, 1, 1, 1, 1, 1, 4 ),
 ( -0.02000000000000000042, 1.020000000000000018 ),
 ( 0.008747244164287000176, 0.02453926110774999961, 0.04033127805120999970, 0.05612329499467000327, 0.07191531193812999989, 0.08770732888158999652, 0.1034993458251000087, 0.1192913627684999978, 0.1350833797120000179, 0.1508753966553999792, 0.1666674135988999994, 0.1824594305423999918, 0.1982514474858000086, 0.2140434644293000011, 0.2298354813727000179, 0.2456274983162000103, 0.2614195152596999749, 0.2772115322030999640, 0.2930035491465999842, 0.3087955660900000288, 0.3245875830334999934, 0.3403795999769999581, 0.3561716169204000026, 0.3719636338639000228, 0.3877556508073999875, 0.4035476677507999765, 0.4193396846942999967, 0.4351317016376999858, 0.4509237185811999504, 0.4667157355247000261, 0.4825077524681000152, 0.4982997694115999798, 0.5140917863550000799, 0.5298838032985000446, 0.5456758202420000092, 0.5614678371854000538, 0.5772598541289000185, 0.5930518710723000630, 0.6088438880158000277, 0.6246359049592999924, 0.6404279219027000369, 0.6562199388462000016, 0.6720119557896999662, 0.6878039727331000108, 0.7035959896765999755, 0.7193880066200000201, 0.7351800235634999847, 0.7509720405069999494, 0.7667640574504001050, 0.7825560743939000696, 0.7983480913373000032, 0.8141401082808000789, 0.8299321252243000435, 0.8457241421676999771, 0.8615161591112000528, 0.8773081760545999863, 0.8931001929981000620, 0.9088922099416000266, 0.9246842268849999602, 0.9404762438285000359, 0.9562682607720000005, 0.9720602777153999341, 0.9878522946589000098, 1.003644311601999961, 1.019436328545999970 ),
 .UNSPECIFIED. ) ;
#1610=B_SPLINE_SURFACE_WITH_KNOTS ( 'NONE', 3, 3, ( 
 ( #57043, #37102, #43030, #58760 ),
 ( #10864, #36760, #21357, #9833 ),
 ( #21694, #5276, #58081, #42355 ),
 ( #32210, #31860, #68551, #37 ) ),
 .UNSPECIFIED., .F., .F., .F.,
 ( 4, 4 ),
 ( 4, 4 ),
 ( -0.01349945606786999951, 0.08053609420915000539 ),
 ( -0.0005287450254680999126, 0.02696599629895000266 ),
 .UNSPECIFIED. ) ;
#1653=CARTESIAN_POINT ( 'NONE',  ( 10.37581074856900187, 2.827416853083249748, 6.999756549658378901 ) ) ;
#1668=CARTESIAN_POINT ( 'NONE',  ( 11.36486084871759950, 2.792989229543000107, 7.174999999999999822 ) ) ;
#1693=CARTESIAN_POINT ( 'NONE',  ( 11.30367835872029936, 2.886444435522000251, 8.201822467543799178 ) ) ;
#1698=CARTESIAN_POINT ( 'NONE',  ( 10.94487616594229884, 3.696562859151900415, 8.456491899811199531 ) ) ;
#1729=CARTESIAN_POINT ( 'NONE',  ( 11.16225954179439839, 4.877394611789299894, 6.770980925167799036 ) ) ;
#1757=CARTESIAN_POINT ( 'NONE',  ( 9.323602683899247623, 2.780955253993290022, 7.819247029363189050 ) ) ;
#1768=ORIENTED_EDGE ( 'NONE', *, *, #64540, .F. ) ;
#1798=CARTESIAN_POINT ( 'NONE',  ( 11.07210672858429845, 3.307795442047700263, 8.020722037455799480 ) ) ;
#1812=CARTESIAN_POINT ( 'NONE',  ( 11.48011496860029901, 4.919769165942200040, 7.971338736265699332 ) ) ;
#1824=ORIENTED_EDGE ( 'NONE', *, *, #13802, .T. ) ;
#1862=CARTESIAN_POINT ( 'NONE',  ( 11.47500581613029880, 4.988618570924500339, 6.865182626353099948 ) ) ;
#1865=CARTESIAN_POINT ( 'NONE',  ( 9.733013376692998264, 2.982096917914000223, 8.017308190024898806 ) ) ;
#1901=CARTESIAN_POINT ( 'NONE',  ( 9.114639751325487538, 5.184985712744429875, 7.040280035170889406 ) ) ;
#1916=CARTESIAN_POINT ( 'NONE',  ( 9.102747021775998704, 3.245052836381700168, 6.837506920432799618 ) ) ;
#1918=CARTESIAN_POINT ( 'NONE',  ( 9.099999931440999390, 5.246365646610000155, 7.595250590283559866 ) ) ;
#1922=CARTESIAN_POINT ( 'NONE',  ( 9.206076168957999073, 3.560025096655699883, 6.752918994396699404 ) ) ;
#1995=DIRECTION ( 'NONE',  ( -0.5000000000000150990, 0.08222066253632250021, -0.8621135439442261239 ) ) ;
#2018=ORIENTED_EDGE ( 'NONE', *, *, #830, .T. ) ;
#2045=CARTESIAN_POINT ( 'NONE',  ( 11.17901463001529905, 4.697110652903200290, 8.616511311517999872 ) ) ;
#2051=CARTESIAN_POINT ( 'NONE',  ( 11.33456651104149948, 4.112542507956200133, 8.635175889530000148 ) ) ;
#2056=ADVANCED_FACE ( 'NONE', ( #29033 ), #38009, .F. ) ;
#2079=VECTOR ( 'NONE', #48036, 1000.000000000000114 ) ;
#2085=CARTESIAN_POINT ( 'NONE',  ( 10.76841504065829902, 4.914510326623699576, 8.181880472491098288 ) ) ;
#2150=CARTESIAN_POINT ( 'NONE',  ( 10.82179975933729921, 4.948878321068100661, 7.826467126457498757 ) ) ;
#2192=CARTESIAN_POINT ( 'NONE',  ( 8.751496707488000126, 4.081676005979390176, 6.643597378104299622 ) ) ;
#2212=CARTESIAN_POINT ( 'NONE',  ( 11.56322412107030928, 4.054600656575539475, 8.532060764998998792 ) ) ;
#2214=CARTESIAN_POINT ( 'NONE',  ( 9.175772138681999479, 3.575113238066399912, 8.559813987224998755 ) ) ;
#2218=UNCERTAINTY_MEASURE_WITH_UNIT (LENGTH_MEASURE( 1.000000000000000082E-05 ), #30891, 'distance_accuracy_value', 'NONE');
#2259=CARTESIAN_POINT ( 'NONE',  ( 9.001430433046998303, 3.145249924879699677, 8.027488966151301142 ) ) ;
#2261=CARTESIAN_POINT ( 'NONE',  ( 9.435596873515667227, 2.907767014557176566, 6.870476274536375882 ) ) ;
#2264=CARTESIAN_POINT ( 'NONE',  ( 8.978113844317999082, 4.218953675027299788, 8.338908357746399602 ) ) ;
#2266=EDGE_LOOP ( 'NONE', ( #53785, #31479 ) ) ;
#2296=CARTESIAN_POINT ( 'NONE',  ( 10.89393020684959978, 2.750000000000000000, 7.500000000000000000 ) ) ;
#2300=CARTESIAN_POINT ( 'NONE',  ( 10.59195391537400077, 5.057233422790000432, 6.781965272201699868 ) ) ;
#2329=CARTESIAN_POINT ( 'NONE',  ( 10.10478570706233370, 5.131706358131709500, 6.886599490775120458 ) ) ;
#2387=CARTESIAN_POINT ( 'NONE',  ( 10.62072335273219892, 4.397090433355999473, 6.430603299050000388 ) ) ;
#2419=CARTESIAN_POINT ( 'NONE',  ( 11.38379707368349969, 3.433355370490100533, 8.490052513816499058 ) ) ;
#2441=CARTESIAN_POINT ( 'NONE',  ( 8.734997988989999129, 3.937347817007940343, 6.633566614602599998 ) ) ;
#2486=CARTESIAN_POINT ( 'NONE',  ( 10.60026222744819790, 3.225465054973100099, 6.861998062869400172 ) ) ;
#2513=VECTOR ( 'NONE', #53549, 1000.000000000000227 ) ;
#2547=CARTESIAN_POINT ( 'NONE',  ( 9.806988259785999418, 3.868581654116200141, 6.504223158184999853 ) ) ;
#2593=CARTESIAN_POINT ( 'NONE',  ( 9.126063610504999701, 4.468346739194200445, 6.458661544034999480 ) ) ;
#2598=CARTESIAN_POINT ( 'NONE',  ( 10.26788779216199821, 4.929030047862200448, 7.164969140522200242 ) ) ;
#2604=CARTESIAN_POINT ( 'NONE',  ( 11.44571737393083133, 2.988799872700407700, 6.726238946114240669 ) ) ;
#2640=CARTESIAN_POINT ( 'NONE',  ( 10.54272335273199879, 4.444874504667400750, 6.301916924546999255 ) ) ;
#2658=AXIS2_PLACEMENT_3D ( 'NONE', #67437, #41568, #62877 ) ;
#2728=ORIENTED_EDGE ( 'NONE', *, *, #23207, .T. ) ;
#2731=CARTESIAN_POINT ( 'NONE',  ( 10.64533863405319991, 4.703785194191100416, 6.602238051205399749 ) ) ;
#2765=CARTESIAN_POINT ( 'NONE',  ( 11.30995122972050027, 4.452766304612699955, 8.547040013405998948 ) ) ;
#2826=CARTESIAN_POINT ( 'NONE',  ( 10.47718582084299932, 3.343463760027599818, 8.258888014436699621 ) ) ;
#2840=ORIENTED_EDGE ( 'NONE', *, *, #46005, .T. ) ;
#2842=CARTESIAN_POINT ( 'NONE',  ( 10.77879632507499785, 4.423544049216699747, 6.714825466131699727 ) ) ;
#2891=CARTESIAN_POINT ( 'NONE',  ( 9.477709346417000802, 4.907312911337299965, 7.930842873041400232 ) ) ;
#2937=CARTESIAN_POINT ( 'NONE',  ( 9.708633995697999453, 5.134843509922999871, 7.374045024026299799 ) ) ;
#3014=CARTESIAN_POINT ( 'NONE',  ( 11.59999999999999964, 4.935123867447915202, 8.208828950335220753 ) ) ;
#3017=CARTESIAN_POINT ( 'NONE',  ( 9.873096873515667227, 2.782534154164606921, 7.827184855449101697 ) ) ;
#3059=CARTESIAN_POINT ( 'NONE',  ( 10.01660887879199890, 3.803658216258800184, 8.344486736701099971 ) ) ;
#3069=CARTESIAN_POINT ( 'NONE',  ( 10.21462282008599942, 4.523146351753199568, 6.656181553372300108 ) ) ;
#3089=B_SPLINE_CURVE_WITH_KNOTS ( 'NONE', 3,
 ( #30741, #29472, #50781, #62541 ),
 .UNSPECIFIED., .F., .F.,
 ( 4, 4 ),
 ( 0.000000000000000000, 1.000000000000000000 ),
 .UNSPECIFIED. ) ;
#3103=EDGE_CURVE ( 'NONE', #64627, #19590, #12079, .T. ) ;
#3104=CARTESIAN_POINT ( 'NONE',  ( 10.39918582084299992, 3.253651555277099927, 8.362701637490498996 ) ) ;
#3177=CARTESIAN_POINT ( 'NONE',  ( 11.09256785386839894, 3.167490253789400523, 6.939751505745099358 ) ) ;
#3188=ORIENTED_EDGE ( 'NONE', *, *, #15214, .T. ) ;
#3190=CARTESIAN_POINT ( 'NONE',  ( 10.29399293566599916, 4.546741702992100009, 6.829299525004299376 ) ) ;
#3207=CARTESIAN_POINT ( 'NONE',  ( 9.099999931440999390, 5.246365646610000155, 7.595250590283559866 ) ) ;
#3238=CARTESIAN_POINT ( 'NONE',  ( 10.98656920625009903, 4.032067152264009913, 8.391549386185598536 ) ) ;
#3240=CARTESIAN_POINT ( 'NONE',  ( 9.251759580228998914, 2.889471124893000287, 7.765443149353999708 ) ) ;
#3284=CARTESIAN_POINT ( 'NONE',  ( 9.759292290062999697, 4.987433183662999703, 8.073332500201798823 ) ) ;
#3290=CARTESIAN_POINT ( 'NONE',  ( 11.59999999999999964, 3.801977891258315534, 6.428664210949555979 ) ) ;
#3322=CARTESIAN_POINT ( 'NONE',  ( 10.51810807141099779, 4.059045408506610109, 6.223352037434000117 ) ) ;
#3338=CARTESIAN_POINT ( 'NONE',  ( 10.32118582084299874, 3.163839350524900063, 8.466515260542900378 ) ) ;
#3405=CARTESIAN_POINT ( 'NONE',  ( 11.14767835872009982, 3.125658946326500320, 8.051056647135798272 ) ) ;
#3410=CARTESIAN_POINT ( 'NONE',  ( 10.74379975933729980, 5.078682052940000524, 7.871126858273000515 ) ) ;
#3427=FACE_OUTER_BOUND ( 'NONE', #47908, .T. ) ;
#3436=CARTESIAN_POINT ( 'NONE',  ( 10.07309687351575178, 5.217465845835396188, 7.172815144550900968 ) ) ;
#3439=CARTESIAN_POINT ( 'NONE',  ( 11.18272066707849888, 5.093522884867000222, 8.161456030935699602 ) ) ;
#3462=CARTESIAN_POINT ( 'NONE',  ( 11.33810207955129812, 4.796537143354000499, 7.174999999999999822 ) ) ;
#3509=CARTESIAN_POINT ( 'NONE',  ( 11.58487348028854846, 3.117292544139400157, 7.022738645480499642 ) ) ;
#3523=FACE_OUTER_BOUND ( 'NONE', #68930, .T. ) ;
#3547=ORIENTED_EDGE ( 'NONE', *, *, #57600, .T. ) ;
#3557=CARTESIAN_POINT ( 'NONE',  ( 11.11486084871780022, 5.207010770456999893, 7.825000000000000178 ) ) ;
#3572=CARTESIAN_POINT ( 'NONE',  ( 9.150442991499998513, 3.928121959910110483, 8.639547276484998761 ) ) ;
#3618=CARTESIAN_POINT ( 'NONE',  ( 8.577265421554999492, 3.785712956512099936, 6.391527115138999626 ) ) ;
#3646=CARTESIAN_POINT ( 'NONE',  ( 10.64393020684969926, 5.250000000000000000, 7.500000000000000000 ) ) ;
#3690=CARTESIAN_POINT ( 'NONE',  ( 11.59999999999999964, 4.420828903570659385, 8.516100029838437280 ) ) ;
#3693=CIRCLE ( 'NONE', #51712, 1.249999999999999778 ) ;
#3737=CARTESIAN_POINT ( 'NONE',  ( 9.082867883171827472, 4.782673203840020371, 6.525013452213887177 ) ) ;
#3742=CARTESIAN_POINT ( 'NONE',  ( 10.72702344389999851, 2.995605560827999891, 8.109550315577399360 ) ) ;
#3747=CARTESIAN_POINT ( 'NONE',  ( 11.20733594839949809, 4.840266102192999575, 8.462948211532999920 ) ) ;
#3764=DIRECTION ( 'NONE',  ( -1.000000000000000000, 0.000000000000000000, 0.000000000000000000 ) ) ;
#3779=CARTESIAN_POINT ( 'NONE',  ( 10.47303166480599934, 2.862083839376000416, 7.419769534118209720 ) ) ;
#3831=CARTESIAN_POINT ( 'NONE',  ( 11.39210538575740017, 4.842454415653899780, 7.701417844014099678 ) ) ;
#3847=CARTESIAN_POINT ( 'NONE',  ( 11.30995122972050027, 4.452766304612699955, 8.547040013405998948 ) ) ;
#3866=CARTESIAN_POINT ( 'NONE',  ( 11.29364426047339975, 4.466097552695299733, 6.769896129503799820 ) ) ;
#3895=PRODUCT_DEFINITION_FORMATION_WITH_SPECIFIED_SOURCE ( 'ANY', '', #50578, .NOT_KNOWN. ) ;
#3911=CARTESIAN_POINT ( 'NONE',  ( 9.501025935145998247, 3.874109063559000088, 8.357822485499299958 ) ) ;
#3944=CARTESIAN_POINT ( 'NONE',  ( 11.75203632436369894, 2.890282938442000127, 7.759151359668400083 ) ) ;
#3957=CARTESIAN_POINT ( 'NONE',  ( 9.607317406968999052, 4.212364169857599983, 6.378110563671000044 ) ) ;
#4034=CARTESIAN_POINT ( 'NONE',  ( 11.00000000000000000, 5.079754677601000523, 7.174999999999999822 ) ) ;
#4074=CARTESIAN_POINT ( 'NONE',  ( 11.76077869730539938, 3.404661623424200201, 8.673950353177000139 ) ) ;
#4086=CARTESIAN_POINT ( 'NONE',  ( 10.76346886766499900, 3.365322927604099679, 8.653146038559000885 ) ) ;
#4091=CARTESIAN_POINT ( 'NONE',  ( 11.15810538575740019, 5.242981041160000188, 7.797177576385699638 ) ) ;
#4120=CARTESIAN_POINT ( 'NONE',  ( 10.27610941423800028, 4.844410192686099847, 8.266982106121901097 ) ) ;
#4179=CARTESIAN_POINT ( 'NONE',  ( 11.41672066707849886, 4.741156262620799922, 7.948314604624900248 ) ) ;
#4194=CARTESIAN_POINT ( 'NONE',  ( 11.50962052873067520, 3.830320465062102109, 8.360247930805771333 ) ) ;
#4197=CARTESIAN_POINT ( 'NONE',  ( 10.37872469555899890, 4.502158848185001006, 8.368784980615899372 ) ) ;
#4211=CARTESIAN_POINT ( 'NONE',  ( 10.70287750876920008, 3.530799696887600092, 6.771886227364699806 ) ) ;
#4259=CARTESIAN_POINT ( 'NONE',  ( 9.224417874593999755, 3.075647715286899953, 7.107043063332000088 ) ) ;
#4292=CARTESIAN_POINT ( 'NONE',  ( 10.51414141025500015, 4.615773412711500434, 6.403245959303999868 ) ) ;
#4295=CARTESIAN_POINT ( 'NONE',  ( 11.01053724730969918, 3.051574408741400291, 7.825000000000000178 ) ) ;
#4307=CARTESIAN_POINT ( 'NONE',  ( 8.541480666858999982, 4.426512626096299918, 6.293984733123999753 ) ) ;
#4313=CARTESIAN_POINT ( 'NONE',  ( 11.59999999999999964, 5.064318446328999634, 6.844464917182299324 ) ) ;
#4338=CARTESIAN_POINT ( 'NONE',  ( 9.760355082327999199, 3.427502311996299955, 8.643954013369999245 ) ) ;
#4354=DIRECTION ( 'NONE',  ( 0.000000000000000000, 1.000000000000000000, 0.000000000000000000 ) ) ;
#4430=CARTESIAN_POINT ( 'NONE',  ( 11.05946005378019947, 5.036385109519999403, 8.053412743695298914 ) ) ;
#4435=CARTESIAN_POINT ( 'NONE',  ( 11.10887482311539998, 5.184953745778000389, 7.021250586468399391 ) ) ;
#4461=CARTESIAN_POINT ( 'NONE',  ( 10.02101354018262569, 4.768183399968643599, 6.500416447002272946 ) ) ;
#4510=DIRECTION ( 'NONE',  ( 0.000000000000000000, 0.8514543052404082157, -0.5244287998266055073 ) ) ;
#4521=CARTESIAN_POINT ( 'NONE',  ( 11.51518179236248862, 3.819003318705799899, 8.347076615013298451 ) ) ;
#4534=CARTESIAN_POINT ( 'NONE',  ( 11.43114108301961629, 4.620688244309836712, 8.119401481368297979 ) ) ;
#4536=CARTESIAN_POINT ( 'NONE',  ( 10.57149279008999798, 3.703313553258400059, 6.398515879103999993 ) ) ;
#4551=CARTESIAN_POINT ( 'NONE',  ( 11.85159063708299954, 4.825025306051200502, 7.268038553423699533 ) ) ;
#4602=CARTESIAN_POINT ( 'NONE',  ( 10.26090035061499961, 4.231093494672100164, 6.664354444139199529 ) ) ;
#4617=CONICAL_SURFACE ( 'NONE', #49237, 0.9346783463124002100, 0.7853981908209605178 ) ;
#4633=CARTESIAN_POINT ( 'NONE',  ( 10.76346886766499900, 3.365322927604099679, 8.653146038559000885 ) ) ;
#4647=CARTESIAN_POINT ( 'NONE',  ( 9.428000818238999159, 2.868129552070000088, 6.903968392969799694 ) ) ;
#4676=CARTESIAN_POINT ( 'NONE',  ( 9.836342523874998633, 2.735516931877000513, 7.693563834190999984 ) ) ;
#4690=ORIENTED_EDGE ( 'NONE', *, *, #830, .F. ) ;
#4772=CARTESIAN_POINT ( 'NONE',  ( 10.43614141025499897, 4.549633050978300730, 6.521048559232099251 ) ) ;
#4779=CARTESIAN_POINT ( 'NONE',  ( 11.52733460557258915, 4.206337284815599986, 6.238754009183999472 ) ) ;
#4788=AXIS2_PLACEMENT_3D ( 'NONE', #574, #11394, #26807 ) ;
#4796=DIRECTION ( 'NONE',  ( 0.000000000000000000, 1.000000000000000000, 0.000000000000000000 ) ) ;
#4810=LINE ( 'NONE', #19869, #56975 ) ;
#4813=VECTOR ( 'NONE', #59778, 1000.000000000000000 ) ;
#4851=FACE_OUTER_BOUND ( 'NONE', #51598, .T. ) ;
#4868=CARTESIAN_POINT ( 'NONE',  ( 10.82595391537419971, 4.716560378569699452, 7.013338090450799811 ) ) ;
#4883=CARTESIAN_POINT ( 'NONE',  ( 10.59610807141099897, 4.052703327804870526, 6.360477084256999980 ) ) ;
#4896=CARTESIAN_POINT ( 'NONE',  ( 10.93937577273821482, 3.538822733277925181, 6.300114087089554893 ) ) ;
#4900=CARTESIAN_POINT ( 'NONE',  ( 11.26902897915239876, 4.221721321201099997, 6.662660017635100296 ) ) ;
#4909=ORIENTED_EDGE ( 'NONE', *, *, #18148, .F. ) ;
#4928=B_SPLINE_CURVE_WITH_KNOTS ( 'NONE', 3,
 ( #45444, #66757, #39504, #3462 ),
 .UNSPECIFIED., .F., .F.,
 ( 4, 4 ),
 ( 0.000000000000000000, 1.000000000000000000 ),
 .UNSPECIFIED. ) ;
#4946=AXIS2_PLACEMENT_3D ( 'NONE', #5710, #64086, #53270 ) ;
#4950=CARTESIAN_POINT ( 'NONE',  ( 8.996455549952997899, 4.781695603001899997, 8.130709350565298976 ) ) ;
#4970=CARTESIAN_POINT ( 'NONE',  ( 11.00000000000000000, 4.991767524623399233, 7.825000000000000178 ) ) ;
#4984=CARTESIAN_POINT ( 'NONE',  ( 11.30367835872029936, 2.886444435522000251, 8.201822467543799178 ) ) ;
#4997=CARTESIAN_POINT ( 'NONE',  ( 9.579975701332999805, 4.938486452461599896, 6.630731591496600075 ) ) ;
#5054=EDGE_CURVE ( 'NONE', #13504, #25295, #56395, .T. ) ;
#5074=CARTESIAN_POINT ( 'NONE',  ( 11.60000000000000142, 3.327218134278213224, 8.148846660984084167 ) ) ;
#5125=CARTESIAN_POINT ( 'NONE',  ( 11.19434208742519843, 3.521141233577200325, 6.747282993577999655 ) ) ;
#5130=CARTESIAN_POINT ( 'NONE',  ( 11.60118044953561878, 5.133201153721000054, 6.909094663619399945 ) ) ;
#5168=CARTESIAN_POINT ( 'NONE',  ( 10.89393020684959978, 2.750000000000000000, 7.500000000000000000 ) ) ;
#5219=CARTESIAN_POINT ( 'NONE',  ( 10.80133863405319872, 4.534404523786000674, 6.818303296693398963 ) ) ;
#5234=CARTESIAN_POINT ( 'NONE',  ( 11.06379841651039797, 3.598362324325699912, 6.432302808027999141 ) ) ;
#5246=VERTEX_POINT ( 'NONE', #13065 ) ;
#5247=CARTESIAN_POINT ( 'NONE',  ( 9.458513540183334456, 3.836375382625530239, 6.250000000000000000 ) ) ;
#5249=CARTESIAN_POINT ( 'NONE',  ( 10.99410672858429905, 3.198097575668700010, 8.103244025831999764 ) ) ;
#5261=CARTESIAN_POINT ( 'NONE',  ( 11.33810207955129812, 4.796537143354000499, 7.174999999999999822 ) ) ;
#5276=CARTESIAN_POINT ( 'NONE',  ( 8.726967411678998587, 3.935557623441470643, 6.608809560686199625 ) ) ;
#5289=CARTESIAN_POINT ( 'NONE',  ( 8.807788144226000426, 4.090932644426789722, 6.546538158064899804 ) ) ;
#5294=CARTESIAN_POINT ( 'NONE',  ( 10.27934687351620724, 3.836375382625536012, 8.750000000000001776 ) ) ;
#5296=CARTESIAN_POINT ( 'NONE',  ( 8.844480666858999030, 4.334888990546500231, 6.553061479084200336 ) ) ;
#5326=CARTESIAN_POINT ( 'NONE',  ( 11.71922412107039868, 4.069539071394910223, 8.814426450544999625 ) ) ;
#5339=CARTESIAN_POINT ( 'NONE',  ( 9.225367640781000134, 4.603017491986999943, 8.628164124510998789 ) ) ;
#5345=ADVANCED_FACE ( 'NONE', ( #43060 ), #31282, .F. ) ;
#5354=CARTESIAN_POINT ( 'NONE',  ( 9.961445400145626294, 4.347277725169313989, 8.303075619429563403 ) ) ;
#5378=CARTESIAN_POINT ( 'NONE',  ( 9.887000818240000655, 2.868129552070000088, 6.903968392969799694 ) ) ;
#5451=ORIENTED_EDGE ( 'NONE', *, *, #27624, .F. ) ;
#5464=B_SPLINE_SURFACE_WITH_KNOTS ( 'NONE', 3, 3, ( 
 ( #47089, #14923, #68051, #4074, #51972, #31354, #20165, #25411, #35572, #37881, #36246, #36593, #46746, #9320, #31016, #27054, #41835, #11303, #32642, #68389, #19828, #21793, #15269, #41493, #53952, #24729, #46055, #67359, #19482, #40803, #62125, #14244, #56888, #46400, #8985 ),
 ( #30327, #51635, #41159, #62465, #14585, #17246, #44867, #66172, #1862, #34033, #27750, #39611, #17601, #38221, #38926, #49401, #7442, #12350, #59549, #60248, #39267, #11645, #33682, #54299, #55000, #55346, #23180, #60937, #44529, #13052, #7101, #17949, #18292, #65823, #60590 ),
 ( #34380, #1513, #23526, #28439, #2212, #6056, #49753, #48722, #824, #12696, #27394, #28793, #50104, #22141, #43481, #64779, #32984, #16892, #22831, #6402, #49062, #1169, #22483, #43825, #44178, #65125, #38567, #59892, #12000, #33338, #65475, #54653, #6748, #28087, #8485 ),
 ( #29135, #30498, #23872, #9161, #56730, #24565, #29830, #35067, #13734, #40985, #51136, #56382, #66513, #46581, #45888, #67540, #3238, #66862, #67198, #19664, #51473, #41331, #25243, #19309, #29490, #35742, #30168, #61618, #57061, #55698, #20006, #40634, #61968, #18975, #62308 ) ),
 .UNSPECIFIED., .F., .F., .F.,
 ( 4, 4 ),
 ( 4, 1, 1, 1, 1, 1, 1, 1, 1, 1, 1, 1, 1, 1, 1, 1, 1, 1, 1, 1, 1, 1, 1, 1, 1, 1, 1, 1, 1, 1, 1, 1, 4 ),
 ( -0.02000000000000000042, 1.020000000000000018 ),
 ( 0.1633025096610999927, 0.1899619885200000136, 0.2166214673788000034, 0.2432809462376999965, 0.2699404250964999585, 0.2965999039553000038, 0.3232593828141999692, 0.3499188616730000145, 0.3765783405318000043, 0.4032378193906999697, 0.4298972982494999595, 0.4565567771083000048, 0.4832162559671999702, 0.5098757348260000155, 0.5365352136848999809, 0.5631946925437000262, 0.5898541714025000715, 0.6165136502614000369, 0.6431731291201999712, 0.6698326079790000165, 0.6964920868378999819, 0.7231515656967000272, 0.7498110445554999615, 0.7764705234143999268, 0.8031300022731999722, 0.8297894811320000175, 0.8564489599908999828, 0.8831084388497000282, 0.9097679177085999935, 0.9364273965674000388, 0.9630868754261999731, 0.9897463542851000495, 1.016405833144000015 ),
 .UNSPECIFIED. ) ;
#5480=CARTESIAN_POINT ( 'NONE',  ( 10.12426357027499790, 5.254871132332000094, 7.257895958275299542 ) ) ;
#5542=ORIENTED_EDGE ( 'NONE', *, *, #62589, .F. ) ;
#5558=CARTESIAN_POINT ( 'NONE',  ( 11.19102897915239936, 4.256858847510399890, 6.529961657816500065 ) ) ;
#5572=CARTESIAN_POINT ( 'NONE',  ( 11.52733460557258915, 4.206337284815599986, 6.238754009183999472 ) ) ;
#5584=CARTESIAN_POINT ( 'NONE',  ( 11.65871932425156920, 3.852858594438699935, 6.507377093516500288 ) ) ;
#5596=CARTESIAN_POINT ( 'NONE',  ( 11.04664311227086415, 4.444039568019538144, 6.293666904468256718 ) ) ;
#5626=CARTESIAN_POINT ( 'NONE',  ( 11.22823073745748168, 3.830325957789608715, 6.639671036489041001 ) ) ;
#5630=ORIENTED_EDGE ( 'NONE', *, *, #16251, .F. ) ;
#5646=CARTESIAN_POINT ( 'NONE',  ( 11.63825819896753977, 3.148796120250299868, 7.339530235223699073 ) ) ;
#5664=CARTESIAN_POINT ( 'NONE',  ( 11.35545123989519922, 4.475221369382300196, 6.582230774881299595 ) ) ;
#5692=CARTESIAN_POINT ( 'NONE',  ( 9.176241837494625742, 3.342362352854908458, 6.922899494040819945 ) ) ;
#5710=CARTESIAN_POINT ( 'NONE',  ( 11.59999999999999964, 4.000000000000000000, 7.500000000000000000 ) ) ;
#5715=CARTESIAN_POINT ( 'NONE',  ( 9.279101285863998072, 3.176316400316700150, 8.478738839062499366 ) ) ;
#5757=CARTESIAN_POINT ( 'NONE',  ( 11.59999999999999787, 3.244119941477264124, 8.017883087166149281 ) ) ;
#5770=CARTESIAN_POINT ( 'NONE',  ( 11.18220574173929904, 5.136173005413447790, 8.088082908809449023 ) ) ;
#5888=CONICAL_SURFACE ( 'NONE', #68413, 0.9999998338055000602, 0.7853981908209605178 ) ;
#5897=CARTESIAN_POINT ( 'NONE',  ( 11.53564291764652872, 3.004110626587600308, 7.623106493640399606 ) ) ;
#5913=CARTESIAN_POINT ( 'NONE',  ( 11.47810404293059960, 3.436653965247300047, 6.352848032645000309 ) ) ;
#5928=CARTESIAN_POINT ( 'NONE',  ( 11.70794988689359961, 4.455786710255300598, 6.606015074393400077 ) ) ;
#5991=CARTESIAN_POINT ( 'NONE',  ( 11.19518313518939934, 3.462699341914400097, 6.820583637845799352 ) ) ;
#6007=CARTESIAN_POINT ( 'NONE',  ( 10.97635090131019986, 4.999207052587699707, 6.881982988766500497 ) ) ;
#6036=CARTESIAN_POINT ( 'NONE',  ( 9.100254395947628083, 3.149024541069663563, 7.703403631282998099 ) ) ;
#6044=FACE_OUTER_BOUND ( 'NONE', #14930, .T. ) ;
#6056=CARTESIAN_POINT ( 'NONE',  ( 11.52166954483529793, 4.562096242626500597, 8.367285821793199574 ) ) ;
#6059=CARTESIAN_POINT ( 'NONE',  ( 9.203113844318000503, 4.323050436788100193, 8.737749087159000894 ) ) ;
#6107=CARTESIAN_POINT ( 'NONE',  ( 8.697480666858998788, 4.334888990546500231, 6.553061479084200336 ) ) ;
#6125=EDGE_CURVE ( 'NONE', #66054, #37252, #8058, .T. ) ;
#6151=CARTESIAN_POINT ( 'NONE',  ( 10.44125056272499918, 5.033400911533000510, 7.484684486284700178 ) ) ;
#6240=CARTESIAN_POINT ( 'NONE',  ( 10.67410807141119911, 4.046361247106100123, 6.497602131078999754 ) ) ;
#6257=CARTESIAN_POINT ( 'NONE',  ( 11.08425954179440076, 4.982976321082899673, 6.683254058608399717 ) ) ;
#6264=DIRECTION ( 'NONE',  ( -1.000000000000000000, 0.000000000000000000, 0.000000000000000000 ) ) ;
#6270=CARTESIAN_POINT ( 'NONE',  ( 10.35826357027499789, 4.850513154668600002, 7.335909308151700614 ) ) ;
#6318=CARTESIAN_POINT ( 'NONE',  ( 8.867797255587998251, 4.866234952405400271, 7.536673658251589636 ) ) ;
#6333=CARTESIAN_POINT ( 'NONE',  ( 11.12133729122639991, 3.134101783108900197, 7.522778681411049995 ) ) ;
#6350=CARTESIAN_POINT ( 'NONE',  ( 10.35814141025499957, 4.483492689244800822, 6.638851159159999682 ) ) ;
#6367=SURFACE_SIDE_STYLE ('',( #32953 ) ) ;
#6387=CARTESIAN_POINT ( 'NONE',  ( 11.59999999999999964, 4.000000000000000000, 7.500000000000000000 ) ) ;
#6402=CARTESIAN_POINT ( 'NONE',  ( 10.93990547754509812, 5.032986398992000510, 7.467215766047949899 ) ) ;
#6404=CARTESIAN_POINT ( 'NONE',  ( 9.152455549953000258, 4.995562869655000071, 8.303267676773000261 ) ) ;
#6453=CARTESIAN_POINT ( 'NONE',  ( 9.961925467520998723, 2.860918852493000486, 7.578921399676699089 ) ) ;
#6461=CARTESIAN_POINT ( 'NONE',  ( 9.282063610504998508, 4.355629271815800507, 6.709281487801199262 ) ) ;
#6464=EDGE_CURVE ( 'NONE', #6746, #61459, #17208, .T. ) ;
#6498=DIRECTION ( 'NONE',  ( 0.000000000000000000, 0.000000000000000000, -1.000000000000000000 ) ) ;
#6502=CARTESIAN_POINT ( 'NONE',  ( 10.56591429142999949, 4.019686495353769651, 8.533318907609000803 ) ) ;
#6541=DIRECTION ( 'NONE',  ( 0.000000000000000000, 0.000000000000000000, 1.000000000000000000 ) ) ;
#6586=CARTESIAN_POINT ( 'NONE',  ( 11.39975833414730033, 4.796537143354000499, 7.825000000000000178 ) ) ;
#6592=CARTESIAN_POINT ( 'NONE',  ( 11.73256516821459883, 4.706297556651700020, 6.787191910456499500 ) ) ;
#6606=CARTESIAN_POINT ( 'NONE',  ( 11.37964291764649971, 2.731641218595000087, 7.656787697937099679 ) ) ;
#6613=EDGE_CURVE ( 'NONE', #21433, #24707, #55131, .T. ) ;
#6619=DIRECTION ( 'NONE',  ( -1.000000000000000000, 0.000000000000000000, 0.000000000000000000 ) ) ;
#6626=CARTESIAN_POINT ( 'NONE',  ( 11.73256516821459883, 4.706297556651700020, 6.787191910456499500 ) ) ;
#6628=CARTESIAN_POINT ( 'NONE',  ( 10.66684687351590277, 4.768183399968648040, 8.499583552997725278 ) ) ;
#6671=CARTESIAN_POINT ( 'NONE',  ( 8.842468108405999061, 4.834201109053600121, 7.263744984161399465 ) ) ;
#6685=CARTESIAN_POINT ( 'NONE',  ( 10.94903032197929882, 4.503839166471300004, 8.204588308639600314 ) ) ;
#6701=CARTESIAN_POINT ( 'NONE',  ( 11.56833327354034857, 3.253412192327699959, 7.988332985010599963 ) ) ;
#6720=CARTESIAN_POINT ( 'NONE',  ( 9.352250488097009651, 2.907725329094806188, 8.129544561320940943 ) ) ;
#6728=CARTESIAN_POINT ( 'NONE',  ( 9.733483075504627990, 3.885520926571138567, 6.632574608010647133 ) ) ;
#6729=CARTESIAN_POINT ( 'NONE',  ( 9.393930206848999376, 2.750000000000000000, 7.500000000000000000 ) ) ;
#6746=VERTEX_POINT ( 'NONE', #62268 ) ;
#6748=CARTESIAN_POINT ( 'NONE',  ( 10.39969598649000027, 4.888000489779200208, 6.971269690999399415 ) ) ;
#6750=CARTESIAN_POINT ( 'NONE',  ( 10.21426717315699939, 3.130949526459800403, 8.240598219300300897 ) ) ;
#6801=CARTESIAN_POINT ( 'NONE',  ( 10.11390035061499937, 4.304339077956200299, 6.399494776650000105 ) ) ;
#6808=CARTESIAN_POINT ( 'NONE',  ( 9.180747021775998107, 3.348327362764200288, 6.928134003122899287 ) ) ;
#6931=CARTESIAN_POINT ( 'NONE',  ( 11.34523293495530005, 2.684794526488000432, 7.552870914315270134 ) ) ;
#6936=CARTESIAN_POINT ( 'NONE',  ( 11.70794988689359961, 4.455786710255300598, 6.606015074393400077 ) ) ;
#6972=CARTESIAN_POINT ( 'NONE',  ( 11.26072066707849828, 4.976067344118500380, 8.090408888831799317 ) ) ;
#6977=CARTESIAN_POINT ( 'NONE',  ( 8.733215486276282746, 4.027942412209718270, 6.616784466747247073 ) ) ;
#7011=CARTESIAN_POINT ( 'NONE',  ( 11.30671024775549505, 4.620655945117460028, 6.880623181275071332 ) ) ;
#7022=CARTESIAN_POINT ( 'NONE',  ( 8.724265421554999733, 3.837285628664199866, 6.658304367510099908 ) ) ;
#7040=CARTESIAN_POINT ( 'NONE',  ( 10.70287750876920008, 3.530799696887600092, 6.771886227364699806 ) ) ;
#7053=CARTESIAN_POINT ( 'NONE',  ( 11.23589666366019912, 3.960399224793059947, 6.608753462694600067 ) ) ;
#7085=ADVANCED_FACE ( 'NONE', ( #51353 ), #66395, .T. ) ;
#7101=CARTESIAN_POINT ( 'NONE',  ( 10.56080513895999928, 5.026880838510000338, 8.070849345005600028 ) ) ;
#7103=CARTESIAN_POINT ( 'NONE',  ( 9.076468108405999047, 5.230803879475000251, 7.151422676278199830 ) ) ;
#7109=CARTESIAN_POINT ( 'NONE',  ( 10.63351354018304740, 5.250000000000001776, 7.336375382625529795 ) ) ;
#7116=AXIS2_PLACEMENT_3D ( 'NONE', #29639, #35888, #34534 ) ;
#7153=CARTESIAN_POINT ( 'NONE',  ( 9.508013376692998619, 3.104586782631499897, 7.955057656228099461 ) ) ;
#7158=CARTESIAN_POINT ( 'NONE',  ( 8.800809814040999157, 4.530359890157599878, 6.814123855771700100 ) ) ;
#7177=EDGE_CURVE ( 'NONE', #5246, #10441, #52859, .T. ) ;
#7196=CARTESIAN_POINT ( 'NONE',  ( 10.82145113417867677, 4.723115832319042084, 7.008885863206549161 ) ) ;
#7234=CARTESIAN_POINT ( 'NONE',  ( 9.841846873515665450, 3.000416447002276943, 8.268183399968647151 ) ) ;
#7287=CARTESIAN_POINT ( 'NONE',  ( 11.40841235500449891, 3.158861363519000154, 8.270568563129298667 ) ) ;
#7306=DIRECTION ( 'NONE',  ( -1.000000000000000000, 0.000000000000000000, 1.554312234491000161E-14 ) ) ;
#7316=CARTESIAN_POINT ( 'NONE',  ( 11.60533460557258323, 4.184174550317700358, 6.374224726731999802 ) ) ;
#7366=B_SPLINE_CURVE_WITH_KNOTS ( 'NONE', 3,
 ( #5261, #26253, #43369, #64669 ),
 .UNSPECIFIED., .F., .F.,
 ( 4, 4 ),
 ( 0.000000000000000000, 1.000000000000000000 ),
 .UNSPECIFIED. ) ;
#7383=CARTESIAN_POINT ( 'NONE',  ( 10.89564560330029863, 4.307504762655200103, 8.455191956516999952 ) ) ;
#7442=CARTESIAN_POINT ( 'NONE',  ( 11.14256920625030034, 4.042230905578960254, 8.674127893687000324 ) ) ;
#7445=CARTESIAN_POINT ( 'NONE',  ( 9.049126402770998112, 5.068373778467000434, 7.902879529556599891 ) ) ;
#7482=EDGE_CURVE ( 'NONE', #51100, #5246, #60112, .T. ) ;
#7484=ORIENTED_EDGE ( 'NONE', *, *, #53664, .F. ) ;
#7492=CARTESIAN_POINT ( 'NONE',  ( 8.672151519676999598, 4.021721698617580110, 6.495824366094999469 ) ) ;
#7494=CARTESIAN_POINT ( 'NONE',  ( 9.643930206848999376, 5.250000000000000000, 7.500000000000000000 ) ) ;
#7498=CARTESIAN_POINT ( 'NONE',  ( 9.484696787962999309, 4.148886440911999429, 8.354131589521699652 ) ) ;
#7530=ORIENTED_EDGE ( 'NONE', *, *, #66129, .F. ) ;
#7532=CARTESIAN_POINT ( 'NONE',  ( 10.91991225946278199, 4.700767082376348327, 8.022508467459166681 ) ) ;
#7536=CARTESIAN_POINT ( 'NONE',  ( 10.73964560330029983, 4.391636236366600166, 8.716526793355999558 ) ) ;
#7551=B_SPLINE_CURVE_WITH_KNOTS ( 'NONE', 3,
 ( #12668, #29108, #66143, #56006, #18261, #8113, #55315, #60905, #18607, #39581, #39236, #60217, #39933, #38540, #6720, #22452, #60561, #50075 ),
 .UNSPECIFIED., .F., .F.,
 ( 4, 2, 2, 2, 2, 2, 2, 2, 4 ),
 ( 0.1494581667962507632, 0.2557758959467194004, 0.3620936250971880654, 0.4684113542476566749, 0.5747290833981253400, 0.6810468125485940050, 0.7873645416990626700, 0.8936822708495313350, 1.000000000000000000 ),
 .UNSPECIFIED. ) ;
#7571=EDGE_CURVE ( 'NONE', #33283, #23956, #38436, .T. ) ;
#7578=LINE ( 'NONE', #7929, #49338 ) ;
#7585=DIRECTION ( 'NONE',  ( 1.000000000000000000, 0.000000000000000000, 0.000000000000000000 ) ) ;
#7624=ORIENTED_EDGE ( 'NONE', *, *, #35410, .T. ) ;
#7632=CARTESIAN_POINT ( 'NONE',  ( 11.58071932425156980, 3.832730087831799803, 6.371589232479998977 ) ) ;
#7667=CARTESIAN_POINT ( 'NONE',  ( 11.06379841651039797, 3.598362324325699912, 6.432302808027999141 ) ) ;
#7669=CARTESIAN_POINT ( 'NONE',  ( 10.79184687351629535, 3.000416447002276943, 8.268183399968645375 ) ) ;
#7680=B_SPLINE_CURVE_WITH_KNOTS ( 'NONE', 3,
 ( #66574, #34780, #8198, #19028, #13792, #24624, #56438, #8539, #29889, #51197, #3290, #58834, #53246, #63727, #63030, #4313 ),
 .UNSPECIFIED., .F., .F.,
 ( 4, 2, 2, 2, 2, 2, 2, 4 ),
 ( 0.000000000000000000, 0.06250000000000055511, 0.1250000000000011102, 0.2500000000000009437, 0.3750000000000007772, 0.5000000000000005551, 0.7500000000000003331, 1.000000000000000000 ),
 .UNSPECIFIED. ) ;
#7691=CARTESIAN_POINT ( 'NONE',  ( 8.706426979769998908, 3.641148095589300304, 6.723921629386799381 ) ) ;
#7733=CARTESIAN_POINT ( 'NONE',  ( 10.67410807141119911, 4.046361247106100123, 6.497602131078999754 ) ) ;
#7765=CARTESIAN_POINT ( 'NONE',  ( 9.051300837857860770, 5.190117543293265356, 7.276433888703319752 ) ) ;
#7771=B_SPLINE_CURVE_WITH_KNOTS ( 'NONE', 3,
 ( #63095, #20121, #41451, #62759 ),
 .UNSPECIFIED., .F., .F.,
 ( 4, 4 ),
 ( 0.000000000000000000, 1.000000000000000000 ),
 .UNSPECIFIED. ) ;
#7798=CARTESIAN_POINT ( 'NONE',  ( 9.655013376692998861, 3.104586782631499897, 7.955057656228099461 ) ) ;
#7818=EDGE_CURVE ( 'NONE', #1231, #32603, #10779, .T. ) ;
#7848=CARTESIAN_POINT ( 'NONE',  ( 9.379355082327998971, 3.488994418336600400, 8.521081653687000212 ) ) ;
#7855=CARTESIAN_POINT ( 'NONE',  ( 8.775480666858998191, 4.289077172771600388, 6.682599852064000423 ) ) ;
#7908=CARTESIAN_POINT ( 'NONE',  ( 10.54272335273199879, 4.444874504667400750, 6.301916924546999255 ) ) ;
#7925=CARTESIAN_POINT ( 'NONE',  ( 8.849999778957998942, 4.000000000000000000, 7.500000000000000000 ) ) ;
#7928=CARTESIAN_POINT ( 'NONE',  ( 9.779346873515665450, 3.836375382625536012, 8.750000000000001776 ) ) ;
#7929=CARTESIAN_POINT ( 'NONE',  ( 8.751496707488000126, 4.081676005979390176, 6.643597378104299622 ) ) ;
#7981=B_SPLINE_CURVE_WITH_KNOTS ( 'NONE', 3,
 ( #24128, #66777, #61876, #51386, #19916, #41241, #45800, #14675, #30084, #61194, #45463, #57306, #19222, #24819, #18893, #9409, #52060, #30753 ),
 .UNSPECIFIED., .F., .F.,
 ( 4, 2, 2, 2, 2, 2, 2, 2, 4 ),
 ( 0.000000000000000000, 0.1249999999999996669, 0.2499999999999993339, 0.3749999999999990008, 0.4999999999999986677, 0.6249999999999990008, 0.7499999999999993339, 0.8749999999999996669, 1.000000000000000000 ),
 .UNSPECIFIED. ) ;
#7984=CARTESIAN_POINT ( 'NONE',  ( 10.81764560330029923, 4.349570499512200428, 8.585859374935999710 ) ) ;
#8015=CARTESIAN_POINT ( 'NONE',  ( 11.40841235500449891, 3.158861363519000154, 8.270568563129298667 ) ) ;
#8040=CARTESIAN_POINT ( 'NONE',  ( 9.232128830620874638, 3.792804146276640864, 8.743003876391233220 ) ) ;
#8058=B_SPLINE_CURVE_WITH_KNOTS ( 'NONE', 3,
 ( #30038, #51340, #18502, #60799, #66033, #24082, #34929, #61827, #8351, #45757, #50314, #50657, #55906, #33892, #45418, #49963, #44735, #19179 ),
 .UNSPECIFIED., .F., .F.,
 ( 4, 2, 2, 2, 2, 2, 2, 2, 4 ),
 ( 0.000000000000000000, 0.1249999999999996669, 0.2499999999999993339, 0.3749999999999990008, 0.4999999999999986677, 0.6249999999999990008, 0.7499999999999993339, 0.8749999999999996669, 1.000000000000000000 ),
 .UNSPECIFIED. ) ;
#8082=CARTESIAN_POINT ( 'NONE',  ( 10.30903300763299946, 4.597717337857299746, 6.873077781830399857 ) ) ;
#8095=CARTESIAN_POINT ( 'NONE',  ( 10.52946886766499901, 3.569835351907400423, 8.281567006984099422 ) ) ;
#8113=CARTESIAN_POINT ( 'NONE',  ( 9.216839207166817260, 4.768179003839036589, 8.499566091636108212 ) ) ;
#8143=CARTESIAN_POINT ( 'NONE',  ( 9.528367640780999182, 4.473477001189199775, 8.385811396220899994 ) ) ;
#8189=CARTESIAN_POINT ( 'NONE',  ( 9.176721904869998170, 4.995641764568400589, 6.941043897400199114 ) ) ;
#8191=CARTESIAN_POINT ( 'NONE',  ( 9.404346873515669003, 2.750000000000000000, 7.336375382625536901 ) ) ;
#8198=CARTESIAN_POINT ( 'NONE',  ( 11.59999999999999964, 3.137911629819545745, 7.087473780876516471 ) ) ;
#8220=( GEOMETRIC_REPRESENTATION_CONTEXT ( 3 ) GLOBAL_UNCERTAINTY_ASSIGNED_CONTEXT ( ( #15020 ) ) GLOBAL_UNIT_ASSIGNED_CONTEXT ( ( #39578, #33651, #54967 ) ) REPRESENTATION_CONTEXT ( 'NONE', 'WORKASPACE' ) );
#8231=CARTESIAN_POINT ( 'NONE',  ( 11.08810207955139937, 3.203462856645999945, 7.825000000000000178 ) ) ;
#8233=CARTESIAN_POINT ( 'NONE',  ( 10.83810672858429847, 2.978701842912999886, 8.268288002587098617 ) ) ;
#8248=CARTESIAN_POINT ( 'NONE',  ( 10.19810941423799910, 4.946022705791000007, 8.359277272599898723 ) ) ;
#8321=CARTESIAN_POINT ( 'NONE',  ( 11.67766954483535891, 4.715882430684499305, 8.604570063127999546 ) ) ;
#8327=CARTESIAN_POINT ( 'NONE',  ( 10.49764694612699856, 2.940513484064000149, 7.077178005756699974 ) ) ;
#8351=CARTESIAN_POINT ( 'NONE',  ( 9.708513540183332680, 4.163624617374472869, 8.749999999999996447 ) ) ;
#8358=CARTESIAN_POINT ( 'NONE',  ( 10.50180110216399854, 3.143606124884799957, 8.023010882787499298 ) ) ;
#8393=ORIENTED_EDGE ( 'NONE', *, *, #8990, .T. ) ;
#8426=CARTESIAN_POINT ( 'NONE',  ( 11.60948876160955479, 3.304472173606900043, 6.776679950459500112 ) ) ;
#8468=CARTESIAN_POINT ( 'NONE',  ( 8.772923981633081070, 4.310454296184184741, 6.685328252913995684 ) ) ;
#8485=CARTESIAN_POINT ( 'NONE',  ( 10.35814141025499957, 4.483492689244800822, 6.638851159159999682 ) ) ;
#8487=CARTESIAN_POINT ( 'NONE',  ( 10.40644474310099810, 4.893483781708200198, 7.066400461213500073 ) ) ;
#8533=CARTESIAN_POINT ( 'NONE',  ( 8.619480666858999385, 4.380700808321400075, 6.423523106103999680 ) ) ;
#8539=CARTESIAN_POINT ( 'NONE',  ( 11.60000000000000142, 3.450002592736672646, 6.620235306175750623 ) ) ;
#8572=CARTESIAN_POINT ( 'NONE',  ( 10.22272469555899832, 4.639546521693399761, 8.606479382885998675 ) ) ;
#8581=CARTESIAN_POINT ( 'NONE',  ( 11.00000000000000000, 2.941427501403999667, 7.174999999999999822 ) ) ;
#8594=ORIENTED_EDGE ( 'NONE', *, *, #68408, .F. ) ;
#8609=CARTESIAN_POINT ( 'NONE',  ( 11.60000000000000320, 4.590480015894799593, 8.459313701734300750 ) ) ;
#8611=CARTESIAN_POINT ( 'NONE',  ( 9.758513540182331525, 4.163624617374472869, 8.749999999999996447 ) ) ;
#8654=CARTESIAN_POINT ( 'NONE',  ( 10.24457120343299898, 3.957971921952620598, 6.634008278083699750 ) ) ;
#8659=CARTESIAN_POINT ( 'NONE',  ( 11.43856039236529831, 5.032284719763000069, 7.449760924956519759 ) ) ;
#8667=CARTESIAN_POINT ( 'NONE',  ( 11.67918044953561996, 5.011483761127000669, 6.972563939641199582 ) ) ;
#8700=CARTESIAN_POINT ( 'NONE',  ( 11.30579707368350029, 3.365167912142600137, 8.609190966793999422 ) ) ;
#8769=CARTESIAN_POINT ( 'NONE',  ( 10.72333863405319931, 4.619094858989799768, 6.710270673950399889 ) ) ;
#8780=CARTESIAN_POINT ( 'NONE',  ( 10.40480513895999870, 4.779740423663599636, 7.933462475324499330 ) ) ;
#8782=CARTESIAN_POINT ( 'NONE',  ( 11.14595257254739913, 3.168263696564200149, 7.258104750172799768 ) ) ;
#8827=CARTESIAN_POINT ( 'NONE',  ( 10.03495058442699950, 4.398663815465100768, 8.421905343605699201 ) ) ;
#8863=CARTESIAN_POINT ( 'NONE',  ( 11.06049777433069892, 3.148547701490199913, 7.825000000000000178 ) ) ;
#8878=CARTESIAN_POINT ( 'NONE',  ( 9.430013376692999216, 2.982096917914000223, 8.017308190024898806 ) ) ;
#8949=CARTESIAN_POINT ( 'NONE',  ( 11.59999999999999609, 5.139199170149530538, 7.925587283338801470 ) ) ;
#8985=CARTESIAN_POINT ( 'NONE',  ( 10.51414141025500015, 4.615773412711500434, 6.403245959303999868 ) ) ;
#8990=EDGE_CURVE ( 'NONE', #45676, #1231, #22414, .T. ) ;
#8994=VERTEX_POINT ( 'NONE', #17756 ) ;
#8996=CARTESIAN_POINT ( 'NONE',  ( 11.22567835872029995, 3.006051690924700370, 8.126439557340900066 ) ) ;
#9001=CARTESIAN_POINT ( 'NONE',  ( 11.55194988689359903, 4.580487242693600081, 6.361426117087999543 ) ) ;
#9017=CARTESIAN_POINT ( 'NONE',  ( 8.748821772879614045, 4.302364887094737966, 6.625936606111492821 ) ) ;
#9032=CARTESIAN_POINT ( 'NONE',  ( 11.60118044953561878, 5.133201153721000054, 6.909094663619399945 ) ) ;
#9075=DIRECTION ( 'NONE',  ( -1.000000000000000000, 0.000000000000000000, 0.000000000000000000 ) ) ;
#9088=CARTESIAN_POINT ( 'NONE',  ( 11.61364291764652812, 3.140345330584100036, 7.606265891492399511 ) ) ;
#9104=CARTESIAN_POINT ( 'NONE',  ( 10.20641772631199906, 4.431553727090300043, 6.611684804099500212 ) ) ;
#9113=EDGE_LOOP ( 'NONE', ( #10583, #7484, #36259, #68221, #52697, #44349, #5451, #442, #67044, #39540, #56298 ) ) ;
#9117=CARTESIAN_POINT ( 'NONE',  ( 11.31825954179440075, 4.666231193203100425, 6.946434658287599540 ) ) ;
#9156=DIRECTION ( 'NONE',  ( 0.7071067486699967874, -0.7071068137030968037, 9.022793105466955192E-11 ) ) ;
#9161=CARTESIAN_POINT ( 'NONE',  ( 11.52677869730533011, 3.596497913043499750, 8.295667533166499297 ) ) ;
#9163=CARTESIAN_POINT ( 'NONE',  ( 9.072442991499999110, 3.936771438983030169, 8.502419298200999620 ) ) ;
#9205=CARTESIAN_POINT ( 'NONE',  ( 9.985242056249999720, 3.541248877825399877, 6.305876158747000026 ) ) ;
#9218=CARTESIAN_POINT ( 'NONE',  ( 8.916525748329494405, 3.463676007238744692, 8.432246543101921787 ) ) ;
#9261=CARTESIAN_POINT ( 'NONE',  ( 10.34580110216399973, 2.909301855364999856, 8.166103548914600552 ) ) ;
#9269=ORIENTED_EDGE ( 'NONE', *, *, #9550, .T. ) ;
#9273=CARTESIAN_POINT ( 'NONE',  ( 10.08521345716899908, 4.924890298941200228, 6.659120737011199331 ) ) ;
#9300=MECHANICAL_DESIGN_GEOMETRIC_PRESENTATION_REPRESENTATION('',(#68480),#8220);
#9320=CARTESIAN_POINT ( 'NONE',  ( 11.34523293495530005, 2.684794526488000432, 7.552870914315270134 ) ) ;
#9329=CARTESIAN_POINT ( 'NONE',  ( 11.59966954483535773, 4.638989336656000440, 8.485927942460499196 ) ) ;
#9334=CARTESIAN_POINT ( 'NONE',  ( 10.61656919669529842, 5.225637333137999718, 7.137881914002699446 ) ) ;
#9364=CARTESIAN_POINT ( 'NONE',  ( 11.40425819896749893, 2.744109752373000255, 7.263238376356399684 ) ) ;
#9409=CARTESIAN_POINT ( 'NONE',  ( 10.32309687351566652, 2.782534154164606921, 7.827184855449101697 ) ) ;
#9422=CARTESIAN_POINT ( 'NONE',  ( 11.34287482311539996, 4.803125295093300551, 7.175518335304800210 ) ) ;
#9436=CARTESIAN_POINT ( 'NONE',  ( 11.52531641787287597, 3.660964319297691283, 8.308706962315561384 ) ) ;
#9438=CARTESIAN_POINT ( 'NONE',  ( 10.81764560330029923, 4.349570499512200428, 8.585859374935999710 ) ) ;
#9453=CARTESIAN_POINT ( 'NONE',  ( 10.67826222744820086, 3.331419131587999960, 6.949274830123499669 ) ) ;
#9503=CARTESIAN_POINT ( 'NONE',  ( 10.18491290906799840, 3.451408805716100314, 6.828616613600999585 ) ) ;
#9535=CARTESIAN_POINT ( 'NONE',  ( 10.84657802013509986, 2.684088780794000151, 7.530633716161349689 ) ) ;
#9550=EDGE_CURVE ( 'NONE', #21890, #21254, #68222, .T. ) ;
#9552=CARTESIAN_POINT ( 'NONE',  ( 8.617468108405999416, 5.230803879475000251, 7.151422676278199830 ) ) ;
#9583=CARTESIAN_POINT ( 'NONE',  ( 9.912329965421998068, 3.111510091554099855, 6.579690231462300254 ) ) ;
#9591=CARTESIAN_POINT ( 'NONE',  ( 11.10328610135029948, 3.121939224269600022, 7.174999999999999822 ) ) ;
#9627=ORIENTED_EDGE ( 'NONE', *, *, #3103, .T. ) ;
#9672=CARTESIAN_POINT ( 'NONE',  ( 9.065735834902588053, 4.411345979885467727, 6.337235623390005124 ) ) ;
#9673=ORIENTED_EDGE ( 'NONE', *, *, #162, .T. ) ;
#9676=AXIS2_PLACEMENT_3D ( 'NONE', #40345, #19020, #18341 ) ;
#9677=CARTESIAN_POINT ( 'NONE',  ( 11.26723293495529887, 2.826061044294000180, 7.547192037433419820 ) ) ;
#9683=CARTESIAN_POINT ( 'NONE',  ( 11.57656516821460890, 4.899536366368299589, 6.592171857671999646 ) ) ;
#9688=CARTESIAN_POINT ( 'NONE',  ( 8.751496707488000126, 4.081676005979390176, 6.643597378104299622 ) ) ;
#9713=CARTESIAN_POINT ( 'NONE',  ( 9.958513540182876156, 3.836375382625530239, 6.250000000000000000 ) ) ;
#9756=CYLINDRICAL_SURFACE ( 'NONE', #50575, 1.250000000000000222 ) ;
#9770=CARTESIAN_POINT ( 'NONE',  ( 10.75210807141120029, 4.040019166404060336, 6.634727177901499573 ) ) ;
#9789=CARTESIAN_POINT ( 'NONE',  ( 10.28026357027499849, 4.985299147223100746, 7.309904858193100097 ) ) ;
#9791=VECTOR ( 'NONE', #62313, 1000.000000000000114 ) ;
#9800=CARTESIAN_POINT ( 'NONE',  ( 10.99664311227126312, 4.444039568019539033, 6.293666904468254941 ) ) ;
#9805=CARTESIAN_POINT ( 'NONE',  ( 11.19518313518939934, 3.462699341914400097, 6.820583637845799352 ) ) ;
#9833=CARTESIAN_POINT ( 'NONE',  ( 8.705449068729999240, 3.636021264089499994, 6.712833982956899703 ) ) ;
#9851=CARTESIAN_POINT ( 'NONE',  ( 10.25851354018279160, 4.163624617374472869, 8.749999999999996447 ) ) ;
#9853=CARTESIAN_POINT ( 'NONE',  ( 9.249747021775998945, 3.245052836381700168, 6.837506920432799618 ) ) ;
#9888=CARTESIAN_POINT ( 'NONE',  ( 11.13746005378019888, 5.161099018038999731, 8.120007936598501175 ) ) ;
#9891=CARTESIAN_POINT ( 'NONE',  ( 11.08810207955139937, 3.203462856645999945, 7.825000000000000178 ) ) ;
#9904=CARTESIAN_POINT ( 'NONE',  ( 8.566809814040999171, 4.782507962695600412, 6.488038963273999649 ) ) ;
#9918=ADVANCED_FACE ( 'NONE', ( #11101 ), #38011, .T. ) ;
#9963=ORIENTED_EDGE ( 'NONE', *, *, #24084, .F. ) ;
#9977=CARTESIAN_POINT ( 'NONE',  ( 11.59999999999999609, 4.988477031107064086, 8.147838400233640144 ) ) ;
#10027=CARTESIAN_POINT ( 'NONE',  ( 11.14256920625030034, 4.042230905578960254, 8.674127893687000324 ) ) ;
#10032=CARTESIAN_POINT ( 'NONE',  ( 10.34580110216399973, 2.909301855364999856, 8.166103548914600552 ) ) ;
#10123=CARTESIAN_POINT ( 'NONE',  ( 11.53979707368350027, 3.569730287184500472, 8.251775607861899786 ) ) ;
#10139=CARTESIAN_POINT ( 'NONE',  ( 11.62994988689359843, 4.518136976474400157, 6.483720595741000459 ) ) ;
#10154=CARTESIAN_POINT ( 'NONE',  ( 9.364763540183330903, 2.782534154164605589, 7.172815144550902744 ) ) ;
#10155=CARTESIAN_POINT ( 'NONE',  ( 11.49056651104150006, 4.085456792591960706, 8.361971998931499783 ) ) ;
#10168=DIRECTION ( 'NONE',  ( -1.000000000000000000, 0.000000000000000000, 0.000000000000000000 ) ) ;
#10201=CARTESIAN_POINT ( 'NONE',  ( 9.931621437244999129, 4.575883738927100097, 8.148124882831599081 ) ) ;
#10206=EDGE_LOOP ( 'NONE', ( #45351, #40761, #58544, #9269 ) ) ;
#10231=CARTESIAN_POINT ( 'NONE',  ( 11.10101463001529964, 4.622233839778099984, 8.496586578655598743 ) ) ;
#10244=CARTESIAN_POINT ( 'NONE',  ( 8.744113844317999096, 4.323050436788100193, 8.737749087159000894 ) ) ;
#10262=ORIENTED_EDGE ( 'NONE', *, *, #63952, .F. ) ;
#10278=CARTESIAN_POINT ( 'NONE',  ( 10.03897570133299944, 4.938486452461599896, 6.630731591496600075 ) ) ;
#10357=EDGE_CURVE ( 'NONE', #24707, #64627, #1142, .T. ) ;
#10370=CARTESIAN_POINT ( 'NONE',  ( 10.36325056272499978, 4.892034740700499817, 7.486779603004729111 ) ) ;
#10376=CARTESIAN_POINT ( 'NONE',  ( 11.13349010443639919, 5.274453806861999716, 7.404690636538299842 ) ) ;
#10393=CYLINDRICAL_SURFACE ( 'NONE', #26420, 1.250000000000000222 ) ;
#10426=EDGE_LOOP ( 'NONE', ( #2018, #47983, #45995, #34328, #21470, #24970, #39620, #55480, #36089, #66880 ) ) ;
#10441=VERTEX_POINT ( 'NONE', #1918 ) ;
#10459=CARTESIAN_POINT ( 'NONE',  ( 11.49056651104150006, 4.085456792591960706, 8.361971998931499783 ) ) ;
#10464=DIRECTION ( 'NONE',  ( 0.000000000000000000, 1.000000000000000000, 0.000000000000000000 ) ) ;
#10474=CARTESIAN_POINT ( 'NONE',  ( 11.33456651104149948, 4.112542507956200133, 8.635175889530000148 ) ) ;
#10488=CARTESIAN_POINT ( 'NONE',  ( 11.03482133862663517, 4.942979055179590908, 6.626386139742056258 ) ) ;
#10492=CARTESIAN_POINT ( 'NONE',  ( 10.72333863405319931, 4.619094858989799768, 6.710270673950399889 ) ) ;
#10495=LINE ( 'NONE', #64308, #49865 ) ;
#10539=CARTESIAN_POINT ( 'NONE',  ( 10.28622949779699880, 4.480999174483200065, 6.778648208007999720 ) ) ;
#10555=ADVANCED_FACE ( 'NONE', ( #36744 ), #31843, .T. ) ;
#10561=EDGE_CURVE ( 'NONE', #44978, #52369, #48691, .T. ) ;
#10583=ORIENTED_EDGE ( 'NONE', *, *, #13802, .F. ) ;
#10588=CARTESIAN_POINT ( 'NONE',  ( 8.642797255587998606, 5.278067516796999925, 7.554109351283189611 ) ) ;
#10596=CARTESIAN_POINT ( 'NONE',  ( 9.834799664234624927, 4.795722374051563541, 7.136189372949617749 ) ) ;
#10597=CARTESIAN_POINT ( 'NONE',  ( 8.956149159797568871, 2.922971693198220144, 7.790330864865198990 ) ) ;
#10618=CARTESIAN_POINT ( 'NONE',  ( 9.937659112603999034, 3.444147913214900214, 6.347865960448999090 ) ) ;
#10654=ORIENTED_EDGE ( 'NONE', *, *, #67293, .F. ) ;
#10711=CARTESIAN_POINT ( 'NONE',  ( 10.37199293566600034, 4.633387186021100668, 6.723009541442299231 ) ) ;
#10742=VERTEX_POINT ( 'NONE', #28315 ) ;
#10752=CARTESIAN_POINT ( 'NONE',  ( 11.00000000000000000, 4.000000000000000000, 7.500000000000000000 ) ) ;
#10754=CARTESIAN_POINT ( 'NONE',  ( 10.77934687351631382, 3.836375382625536012, 8.750000000000001776 ) ) ;
#10779=B_SPLINE_CURVE_WITH_KNOTS ( 'NONE', 3,
 ( #48763, #38267, #63798, #37924 ),
 .UNSPECIFIED., .F., .F.,
 ( 4, 4 ),
 ( 0.000000000000000000, 1.000000000000000000 ),
 .UNSPECIFIED. ) ;
#10805=CARTESIAN_POINT ( 'NONE',  ( 10.84641504065830020, 4.804462279649600376, 8.099826052678000821 ) ) ;
#10821=CARTESIAN_POINT ( 'NONE',  ( 10.20226357027499908, 5.120085139777000194, 7.283900408233900059 ) ) ;
#10836=CARTESIAN_POINT ( 'NONE',  ( 10.62487750876920067, 3.456442671114800191, 6.656497609330299881 ) ) ;
#10848=CARTESIAN_POINT ( 'NONE',  ( 11.59999999999999964, 4.000000000000000000, 7.500000000000000000 ) ) ;
#10864=CARTESIAN_POINT ( 'NONE',  ( 8.748305582559998683, 4.091272957481129957, 6.637573130164000190 ) ) ;
#10886=CARTESIAN_POINT ( 'NONE',  ( 9.070430433046999141, 3.262177192690499883, 7.955330044604899342 ) ) ;
#10900=CARTESIAN_POINT ( 'NONE',  ( 11.73671932425159881, 3.872987101045399783, 6.643164954553199664 ) ) ;
#10916=CARTESIAN_POINT ( 'NONE',  ( 11.43856039236529831, 5.032284719763000069, 7.449760924956519759 ) ) ;
#10934=CARTESIAN_POINT ( 'NONE',  ( 9.503988259786000370, 3.832626376493700082, 6.231784538167999266 ) ) ;
#10944=CARTESIAN_POINT ( 'NONE',  ( 9.252229279041625176, 4.091138914130668880, 6.629812682664218748 ) ) ;
#11065=CARTESIAN_POINT ( 'NONE',  ( 10.77368717260499942, 3.460071470104900015, 6.618743573831199711 ) ) ;
#11101=FACE_OUTER_BOUND ( 'NONE', #20379, .T. ) ;
#11152=CARTESIAN_POINT ( 'NONE',  ( 11.48641235500450009, 3.260080192309100067, 8.177841818594698609 ) ) ;
#11165=CARTESIAN_POINT ( 'NONE',  ( 10.66579975933730040, 5.208485784810999775, 7.915786590091300035 ) ) ;
#11178=CARTESIAN_POINT ( 'NONE',  ( 10.38287885159599888, 4.860099138268600072, 7.602606670248799325 ) ) ;
#11240=CARTESIAN_POINT ( 'NONE',  ( 10.77672335273219950, 4.301522290735800169, 6.687976048055599421 ) ) ;
#11255=CARTESIAN_POINT ( 'NONE',  ( 10.64902344389989963, 3.116469856398800253, 8.036199780531900316 ) ) ;
#11283=CARTESIAN_POINT ( 'NONE',  ( 9.302887573405627109, 4.590576684156811638, 6.854437106819677439 ) ) ;
#11301=ORIENTED_EDGE ( 'NONE', *, *, #27930, .T. ) ;
#11303=CARTESIAN_POINT ( 'NONE',  ( 11.17901463001529905, 4.697110652903200290, 8.616511311517999872 ) ) ;
#11306=CARTESIAN_POINT ( 'NONE',  ( 9.304430433046999127, 2.911395389258000233, 8.171806809244198888 ) ) ;
#11354=CARTESIAN_POINT ( 'NONE',  ( 9.254721904869999349, 4.875830726371099821, 7.008306153105300140 ) ) ;
#11394=DIRECTION ( 'NONE',  ( -1.000000000000000000, 0.000000000000000000, 0.000000000000000000 ) ) ;
#11398=CARTESIAN_POINT ( 'NONE',  ( 10.48791429142999831, 4.016993441347180394, 8.391963954669400039 ) ) ;
#11418=CARTESIAN_POINT ( 'NONE',  ( 11.08810207955139937, 3.203462856645999945, 7.825000000000000178 ) ) ;
#11447=ORIENTED_EDGE ( 'NONE', *, *, #66781, .T. ) ;
#11486=CARTESIAN_POINT ( 'NONE',  ( 10.32949413291699869, 4.912929163218899831, 7.916546720849799712 ) ) ;
#11501=CARTESIAN_POINT ( 'NONE',  ( 11.57656516821460890, 4.899536366368299589, 6.592171857671999646 ) ) ;
#11515=CARTESIAN_POINT ( 'NONE',  ( 11.24025954179439957, 4.771812902496799680, 6.858707791728399172 ) ) ;
#11526=VECTOR ( 'NONE', #6619, 1000.000000000000000 ) ;
#11562=CARTESIAN_POINT ( 'NONE',  ( 8.918455549952998496, 4.674761969675400586, 8.044430187461498960 ) ) ;
#11563=B_SPLINE_CURVE_WITH_KNOTS ( 'NONE', 3,
 ( #3207, #40274, #7765, #61591, #13708, #35037, #56005, #30138, #67169, #55667 ),
 .UNSPECIFIED., .F., .F.,
 ( 4, 2, 2, 2, 4 ),
 ( 0.000000000000000000, 0.2500000000000000000, 0.5000000000000000000, 0.7500000000000000000, 1.000000000000000000 ),
 .UNSPECIFIED. ) ;
#11577=CARTESIAN_POINT ( 'NONE',  ( 11.36749010443639918, 4.863785690678500195, 7.435402237490909449 ) ) ;
#11594=CARTESIAN_POINT ( 'NONE',  ( 11.31389666366019853, 3.954123449088899900, 6.467512203247999913 ) ) ;
#11614=CARTESIAN_POINT ( 'NONE',  ( 10.62452888361057113, 3.128042445605609512, 7.438521339935803667 ) ) ;
#11624=CARTESIAN_POINT ( 'NONE',  ( 10.21473687196862734, 3.686226525417862998, 6.683251291081091949 ) ) ;
#11640=CYLINDRICAL_SURFACE ( 'NONE', #4946, 1.250000000000000222 ) ;
#11645=CARTESIAN_POINT ( 'NONE',  ( 10.93479632507519916, 4.557787252275099732, 6.465962698293999722 ) ) ;
#11651=CARTESIAN_POINT ( 'NONE',  ( 9.682355082327998019, 3.488994418336600400, 8.521081653687000212 ) ) ;
#11655=CARTESIAN_POINT ( 'NONE',  ( 10.57101354018312023, 4.768183399968643599, 6.500416447002274722 ) ) ;
#11679=ORIENTED_EDGE ( 'NONE', *, *, #57600, .F. ) ;
#11697=CARTESIAN_POINT ( 'NONE',  ( 9.482684229509999341, 3.291972602441000095, 8.212418068717900255 ) ) ;
#11703=CARTESIAN_POINT ( 'NONE',  ( 11.35565467195930189, 2.863826994586553987, 8.088082908809450799 ) ) ;
#11704=CARTESIAN_POINT ( 'NONE',  ( 9.383380199233998908, 4.860242402105300563, 7.608124715612800237 ) ) ;
#11744=CARTESIAN_POINT ( 'NONE',  ( 11.36056039236529891, 4.891071240644300211, 7.456633480985620288 ) ) ;
#11831=ORIENTED_EDGE ( 'NONE', *, *, #41784, .F. ) ;
#11834=CARTESIAN_POINT ( 'NONE',  ( 11.58487348028854846, 3.117292544139400157, 7.022738645480499642 ) ) ;
#11846=ORIENTED_EDGE ( 'NONE', *, *, #51992, .F. ) ;
#11851=CARTESIAN_POINT ( 'NONE',  ( 11.50271932425157040, 3.812601581225100400, 6.235801371442999397 ) ) ;
#11865=CARTESIAN_POINT ( 'NONE',  ( 10.29262282008599882, 4.451581486939200083, 6.771613406921599854 ) ) ;
#11888=CARTESIAN_POINT ( 'NONE',  ( 8.776575450301999481, 3.932070968445029902, 6.560591699025100532 ) ) ;
#11916=CARTESIAN_POINT ( 'NONE',  ( 9.121088727410999297, 3.136022381937999981, 7.427538838030949719 ) ) ;
#11923=ORIENTED_EDGE ( 'NONE', *, *, #43404, .F. ) ;
#11924=EDGE_CURVE ( 'NONE', #24276, #21416, #25148, .T. ) ;
#11934=CARTESIAN_POINT ( 'NONE',  ( 11.56441235500451015, 3.361299021099800388, 8.085115074060599483 ) ) ;
#11949=CARTESIAN_POINT ( 'NONE',  ( 10.64391429142989765, 4.022379549362480766, 8.674673860548999471 ) ) ;
#11956=CONICAL_SURFACE ( 'NONE', #67789, 0.9999998338055000602, 0.7853981908209605178 ) ;
#11963=CARTESIAN_POINT ( 'NONE',  ( 9.957691290288998687, 3.110563525881361535, 6.586710612921466534 ) ) ;
#11968=CARTESIAN_POINT ( 'NONE',  ( 10.31652245563454073, 4.682420780414364714, 6.971781362826274808 ) ) ;
#11977=CARTESIAN_POINT ( 'NONE',  ( 9.328216720588626387, 4.762939826712631941, 7.071683423462644669 ) ) ;
#12000=CARTESIAN_POINT ( 'NONE',  ( 10.56591429142999949, 4.019686495353769651, 8.533318907609000803 ) ) ;
#12002=CARTESIAN_POINT ( 'NONE',  ( 9.403734463322997783, 4.118936914955599882, 6.364399516445999438 ) ) ;
#12007=CARTESIAN_POINT ( 'NONE',  ( 10.49809687351654297, 3.672815144550898303, 6.282534154164607365 ) ) ;
#12030=EDGE_LOOP ( 'NONE', ( #47639, #12720, #62870, #20643, #48432, #11923, #19345, #51339, #68354, #57801, #68429, #35402 ) ) ;
#12054=CARTESIAN_POINT ( 'NONE',  ( 8.646822372493998543, 3.711294259598199918, 6.555546982591299532 ) ) ;
#12062=CARTESIAN_POINT ( 'NONE',  ( 8.876797255587998592, 4.866234952405400271, 7.536673658251589636 ) ) ;
#12079=LINE ( 'NONE', #50179, #61842 ) ;
#12149=CARTESIAN_POINT ( 'NONE',  ( 10.34393020684899867, 2.750000000000000000, 7.500000000000000000 ) ) ;
#12187=CARTESIAN_POINT ( 'NONE',  ( 11.46989666366029859, 3.941571897678119996, 6.185029684353999357 ) ) ;
#12193=CARTESIAN_POINT ( 'NONE',  ( 10.89564560330029863, 4.307504762655200103, 8.455191956516999952 ) ) ;
#12224=CARTESIAN_POINT ( 'NONE',  ( 10.30487885159599770, 4.996404279947399552, 7.618867373350600047 ) ) ;
#12275=CARTESIAN_POINT ( 'NONE',  ( 9.171747021775997766, 3.348327362764200288, 6.928134003122899287 ) ) ;
#12291=CARTESIAN_POINT ( 'NONE',  ( 11.85159063708299954, 4.825025306051200502, 7.268038553423699533 ) ) ;
#12303=CARTESIAN_POINT ( 'NONE',  ( 11.27745123989519982, 4.410212499603100689, 6.707778874960499849 ) ) ;
#12313=EDGE_CURVE ( 'NONE', #56577, #39090, #61071, .T. ) ;
#12332=CARTESIAN_POINT ( 'NONE',  ( 9.049596101582626062, 3.436622489763541122, 8.169431139013614285 ) ) ;
#12350=CARTESIAN_POINT ( 'NONE',  ( 11.10101463001529964, 4.622233839778099984, 8.496586578655598743 ) ) ;
#12352=CARTESIAN_POINT ( 'NONE',  ( 9.884988259786998910, 3.850604015305000072, 6.368003848175999515 ) ) ;
#12357=CARTESIAN_POINT ( 'NONE',  ( 10.53976354018315753, 4.327184855449099921, 6.282534154164603812 ) ) ;
#12403=CARTESIAN_POINT ( 'NONE',  ( 8.824126402770998467, 4.939810497841199854, 7.854398824525599565 ) ) ;
#12409=CARTESIAN_POINT ( 'NONE',  ( 9.459367640780998343, 4.408706755790200660, 8.264635032075899446 ) ) ;
#12442=CARTESIAN_POINT ( 'NONE',  ( 10.87068169682078178, 4.873909797778569697, 7.519268307021759412 ) ) ;
#12446=CARTESIAN_POINT ( 'NONE',  ( 10.86272200990529946, 2.793294545435000220, 7.920925559347199219 ) ) ;
#12456=EDGE_LOOP ( 'NONE', ( #62442, #10262, #41957, #57369, #4690, #22882, #46440, #23227, #4909, #52255, #45650 ) ) ;
#12531=CARTESIAN_POINT ( 'NONE',  ( 11.05435090131019926, 5.119447121461000449, 6.807613609764599616 ) ) ;
#12538=CARTESIAN_POINT ( 'NONE',  ( 10.71918447801630059, 5.140463864104999558, 7.525145395936648995 ) ) ;
#12552=ORIENTED_EDGE ( 'NONE', *, *, #16472, .T. ) ;
#12560=EDGE_CURVE ( 'NONE', #44978, #36556, #18497, .T. ) ;
#12569=CARTESIAN_POINT ( 'NONE',  ( 11.21149010443640037, 5.137564434800999891, 7.414927836855409460 ) ) ;
#12598=CARTESIAN_POINT ( 'NONE',  ( 9.262620115046999558, 3.343122245339613663, 8.575407073603340535 ) ) ;
#12635=CARTESIAN_POINT ( 'NONE',  ( 10.92026088462129962, 4.002135146349410810, 8.503467136482999678 ) ) ;
#12649=CARTESIAN_POINT ( 'NONE',  ( 10.32169598648999909, 4.766524664146899681, 7.043598424555200133 ) ) ;
#12668=CARTESIAN_POINT ( 'NONE',  ( 9.143927823787139531, 5.249988444743198812, 7.500000155056751439 ) ) ;
#12696=CARTESIAN_POINT ( 'NONE',  ( 11.35545123989519922, 4.475221369382300196, 6.582230774881299595 ) ) ;
#12698=CARTESIAN_POINT ( 'NONE',  ( 9.631696787963999640, 4.196076320588900010, 8.624850445389000697 ) ) ;
#12703=CARTESIAN_POINT ( 'NONE',  ( 10.52934687351650389, 4.163624617374466652, 6.250000000000000000 ) ) ;
#12720=ORIENTED_EDGE ( 'NONE', *, *, #38370, .T. ) ;
#12722=B_SPLINE_CURVE_WITH_KNOTS ( 'NONE', 3,
 ( #29259, #35862, #2329, #9273 ),
 .UNSPECIFIED., .F., .F.,
 ( 4, 4 ),
 ( 0.000000000000000000, 1.000000000000000000 ),
 .UNSPECIFIED. ) ;
#12739=B_SPLINE_CURVE_WITH_KNOTS ( 'NONE', 3,
 ( #23561, #1901, #61657, #61316 ),
 .UNSPECIFIED., .F., .F.,
 ( 4, 4 ),
 ( 0.000000000000000000, 0.1494581667962507632 ),
 .UNSPECIFIED. ) ;
#12750=CARTESIAN_POINT ( 'NONE',  ( 8.655265421554998895, 3.811499292588199861, 6.524915741324599949 ) ) ;
#12757=CARTESIAN_POINT ( 'NONE',  ( 10.25944474310099785, 4.893483781708200198, 7.066400461213500073 ) ) ;
#12796=CARTESIAN_POINT ( 'NONE',  ( 10.24733997687999931, 4.272363749081500295, 8.748653021963999521 ) ) ;
#12853=CARTESIAN_POINT ( 'NONE',  ( 11.42394752546313441, 3.297753801639562443, 6.396140797112706444 ) ) ;
#12886=CARTESIAN_POINT ( 'NONE',  ( 10.39918582084299992, 3.253651555277099927, 8.362701637490498996 ) ) ;
#12913=VERTEX_POINT ( 'NONE', #40239 ) ;
#12919=CARTESIAN_POINT ( 'NONE',  ( 10.47718582084299932, 3.343463760027599818, 8.258888014436699621 ) ) ;
#12942=CARTESIAN_POINT ( 'NONE',  ( 8.749283493600000128, 4.089987329977850194, 6.649720865199900466 ) ) ;
#12990=CARTESIAN_POINT ( 'NONE',  ( 11.31410538575739899, 4.975963290822400076, 7.733337754805098996 ) ) ;
#13026=VERTEX_POINT ( 'NONE', #56316 ) ;
#13052=CARTESIAN_POINT ( 'NONE',  ( 10.60235971519489873, 4.605301262871499546, 8.506961598696999971 ) ) ;
#13055=CARTESIAN_POINT ( 'NONE',  ( 8.947809814040999399, 4.698458605182900705, 6.596733927440100231 ) ) ;
#13065=CARTESIAN_POINT ( 'NONE',  ( 9.099999931440999390, 5.250000000000000000, 7.500000000000000000 ) ) ;
#13100=CARTESIAN_POINT ( 'NONE',  ( 9.809950584426999853, 4.453199839589800035, 8.548019252390998801 ) ) ;
#13108=CARTESIAN_POINT ( 'NONE',  ( 8.826138961223998436, 4.718363881473300658, 7.014550357332099750 ) ) ;
#13166=CARTESIAN_POINT ( 'NONE',  ( 10.73964560330029983, 4.391636236366600166, 8.716526793355999558 ) ) ;
#13182=FACE_OUTER_BOUND ( 'NONE', #21226, .T. ) ;
#13239=CARTESIAN_POINT ( 'NONE',  ( 11.70379573085659786, 5.106255642043000087, 7.308581953418300081 ) ) ;
#13272=CARTESIAN_POINT ( 'NONE',  ( 10.98995257254739855, 2.904643075091000171, 7.181435527216799564 ) ) ;
#13274=CARTESIAN_POINT ( 'NONE',  ( 10.73976354018279977, 3.672815144550903632, 8.717465845835395299 ) ) ;
#13338=CARTESIAN_POINT ( 'NONE',  ( 11.06795257254739973, 3.036453385827900142, 7.219770138693499817 ) ) ;
#13380=CARTESIAN_POINT ( 'NONE',  ( 8.922950365671626471, 4.680938325111460685, 8.049413566043876145 ) ) ;
#13401=CARTESIAN_POINT ( 'NONE',  ( 10.11093802597399893, 3.477805217445600228, 8.357994702431799539 ) ) ;
#13420=EDGE_LOOP ( 'NONE', ( #58138, #44129, #26416, #50068 ) ) ;
#13450=CARTESIAN_POINT ( 'NONE',  ( 9.404684229509999938, 3.195116560491999991, 8.309874741421300115 ) ) ;
#13491=CARTESIAN_POINT ( 'NONE',  ( 10.39503166480599994, 2.725152142215999884, 7.410114961806599787 ) ) ;
#13504=VERTEX_POINT ( 'NONE', #65245 ) ;
#13570=FACE_OUTER_BOUND ( 'NONE', #32910, .T. ) ;
#13574=CARTESIAN_POINT ( 'NONE',  ( 11.71922412107039868, 4.069539071394910223, 8.814426450544999625 ) ) ;
#13581=CARTESIAN_POINT ( 'NONE',  ( 10.54687750876899877, 3.382085645339300228, 6.541108991297599928 ) ) ;
#13613=CARTESIAN_POINT ( 'NONE',  ( 11.65456516821461008, 4.802916961510000249, 6.689681884064299311 ) ) ;
#13676=CARTESIAN_POINT ( 'NONE',  ( 11.75718044953559804, 4.889766368533900120, 7.036033215662999218 ) ) ;
#13681=CARTESIAN_POINT ( 'NONE',  ( 11.08810207955139937, 3.203462856645999945, 7.825000000000000178 ) ) ;
#13691=CARTESIAN_POINT ( 'NONE',  ( 10.65413259636999932, 3.216622244594500302, 7.073141822156699732 ) ) ;
#13708=CARTESIAN_POINT ( 'NONE',  ( 8.978248830702483474, 4.955089878105851220, 6.882626671536596241 ) ) ;
#13734=CARTESIAN_POINT ( 'NONE',  ( 11.31900581613029821, 4.750686773407899466, 7.017964743997199939 ) ) ;
#13736=CARTESIAN_POINT ( 'NONE',  ( 9.401721904869997815, 4.875830726371099821, 7.008306153105300140 ) ) ;
#13784=CARTESIAN_POINT ( 'NONE',  ( 9.227380199234000102, 5.132898093246000215, 7.642395078236999595 ) ) ;
#13792=CARTESIAN_POINT ( 'NONE',  ( 11.59999999999999964, 3.186931496511417272, 6.962391415777370973 ) ) ;
#13802=EDGE_CURVE ( 'NONE', #1219, #43427, #60066, .T. ) ;
#13826=CARTESIAN_POINT ( 'NONE',  ( 10.93656785386839836, 2.939720539848000413, 6.786470850652599474 ) ) ;
#13831=CARTESIAN_POINT ( 'NONE',  ( 9.343930206849998754, 2.750000000000000000, 7.500000000000000000 ) ) ;
#13861=CARTESIAN_POINT ( 'NONE',  ( 11.60000000000000142, 4.813860086966100127, 8.315594847681079926 ) ) ;
#13863=CARTESIAN_POINT ( 'NONE',  ( 9.821013540182335078, 3.231816600031359510, 8.499583552997727054 ) ) ;
#13907=CARTESIAN_POINT ( 'NONE',  ( 9.057169810767971896, 4.203513387681364399, 6.292830123317686208 ) ) ;
#13914=CARTESIAN_POINT ( 'NONE',  ( 11.27234208742519783, 3.445253572379500362, 6.627995351445298944 ) ) ;
#13919=CARTESIAN_POINT ( 'NONE',  ( 11.16225954179439839, 4.877394611789299894, 6.770980925167799036 ) ) ;
#13952=CARTESIAN_POINT ( 'NONE',  ( 11.45348876160960039, 3.114179898019400206, 6.578783887955899523 ) ) ;
#14000=CARTESIAN_POINT ( 'NONE',  ( 10.60226354018307937, 5.092232985442822546, 6.870476274536374106 ) ) ;
#14020=CARTESIAN_POINT ( 'NONE',  ( 10.96949144726329806, 3.419793223320000131, 8.318725197575499664 ) ) ;
#14032=DIRECTION ( 'NONE',  ( 0.000000000000000000, 0.000000000000000000, -1.000000000000000000 ) ) ;
#14033=CARTESIAN_POINT ( 'NONE',  ( 11.06967835872019812, 3.245266201729799960, 7.975673736933100777 ) ) ;
#14035=CARTESIAN_POINT ( 'NONE',  ( 11.53979707368350027, 3.569730287184500472, 8.251775607861899786 ) ) ;
#14082=CARTESIAN_POINT ( 'NONE',  ( 10.18692546752099837, 2.997990738918999920, 7.569424354486659290 ) ) ;
#14126=FILL_AREA_STYLE_COLOUR ( '', #26515 ) ;
#14128=CARTESIAN_POINT ( 'NONE',  ( 9.480671671056999372, 2.873958896683999953, 7.310881302803900361 ) ) ;
#14146=ORIENTED_EDGE ( 'NONE', *, *, #7818, .T. ) ;
#14170=CARTESIAN_POINT ( 'NONE',  ( 11.13459739833729856, 3.176841881612200158, 7.174999999999999822 ) ) ;
#14184=CARTESIAN_POINT ( 'NONE',  ( 10.39503166480599994, 2.725152142215999884, 7.410114961806599787 ) ) ;
#14244=CARTESIAN_POINT ( 'NONE',  ( 10.59725056272499977, 5.316133253199000208, 7.480494252843770120 ) ) ;
#14251=CARTESIAN_POINT ( 'NONE',  ( 10.14325461470300027, 3.159754091322399816, 7.286236678332599581 ) ) ;
#14256=CARTESIAN_POINT ( 'NONE',  ( 10.52799293566599914, 4.806678152079100208, 6.510429574318199464 ) ) ;
#14262=CARTESIAN_POINT ( 'NONE',  ( 10.86272200990529946, 2.793294545435000220, 7.920925559347199219 ) ) ;
#14265=ORIENTED_EDGE ( 'NONE', *, *, #35615, .T. ) ;
#14294=CARTESIAN_POINT ( 'NONE',  ( 11.01041369783139956, 3.935522326596939902, 6.223614866029000048 ) ) ;
#14297=CARTESIAN_POINT ( 'NONE',  ( 10.80226354018299872, 2.907767014557178786, 8.129523725463625894 ) ) ;
#14332=VERTEX_POINT ( 'NONE', #55127 ) ;
#14364=CARTESIAN_POINT ( 'NONE',  ( 11.11302897915239818, 4.291996373817799970, 6.397263297997000109 ) ) ;
#14381=CARTESIAN_POINT ( 'NONE',  ( 11.36749010443639918, 4.863785690678500195, 7.435402237490909449 ) ) ;
#14413=CARTESIAN_POINT ( 'NONE',  ( 11.13220574173981170, 5.136173005413450454, 8.088082908809449023 ) ) ;
#14427=CARTESIAN_POINT ( 'NONE',  ( 9.021784697134998865, 4.545051930576500254, 8.343659109631099469 ) ) ;
#14447=ADVANCED_FACE ( 'NONE', ( #13182 ), #11956, .T. ) ;
#14474=CARTESIAN_POINT ( 'NONE',  ( 10.03590035061499997, 4.340961869598300105, 6.267064942904999825 ) ) ;
#14539=EDGE_LOOP ( 'NONE', ( #22256, #25053, #41176 ) ) ;
#14585=CARTESIAN_POINT ( 'NONE',  ( 11.64122412107036908, 4.062069863985690255, 8.673243607771999208 ) ) ;
#14595=CARTESIAN_POINT ( 'NONE',  ( 11.64633327354034797, 3.135095881599500256, 8.065722083251399610 ) ) ;
#14601=CARTESIAN_POINT ( 'NONE',  ( 10.54272335273199879, 4.444874504667400750, 6.301916924546999255 ) ) ;
#14632=CARTESIAN_POINT ( 'NONE',  ( 10.25149413291699929, 5.037815157227999663, 7.973529073237199505 ) ) ;
#14675=CARTESIAN_POINT ( 'NONE',  ( 10.19809687351566474, 4.327184855449106138, 8.717465845835393523 ) ) ;
#14684=CARTESIAN_POINT ( 'NONE',  ( 8.849999778957998942, 4.000000000000000000, 7.500000000000000000 ) ) ;
#14686=CARTESIAN_POINT ( 'NONE',  ( 11.46595122972049907, 4.343798595649099425, 8.295047870239098842 ) ) ;
#14703=CARTESIAN_POINT ( 'NONE',  ( 11.08841369783139896, 3.942447888101379583, 6.360711682373000109 ) ) ;
#14717=CARTESIAN_POINT ( 'NONE',  ( 10.82595391537419971, 4.716560378569699452, 7.013338090450799811 ) ) ;
#14766=CARTESIAN_POINT ( 'NONE',  ( 9.653000818238998804, 3.232852935619000334, 7.096028062709999418 ) ) ;
#14796=CARTESIAN_POINT ( 'NONE',  ( 11.76077869730539938, 3.404661623424200201, 8.673950353177000139 ) ) ;
#14811=CARTESIAN_POINT ( 'NONE',  ( 9.352013376692999813, 2.859607053196999704, 8.079558723821699928 ) ) ;
#14827=ORIENTED_EDGE ( 'NONE', *, *, #12560, .F. ) ;
#14865=CARTESIAN_POINT ( 'NONE',  ( 10.27195525820100031, 3.879327850572200198, 8.772302877803999976 ) ) ;
#14923=CARTESIAN_POINT ( 'NONE',  ( 11.83003632436370012, 2.756744593645999775, 7.790336465152099876 ) ) ;
#14930=EDGE_LOOP ( 'NONE', ( #46721, #49864, #9627, #33810 ) ) ;
#14933=CARTESIAN_POINT ( 'NONE',  ( 10.44999293566599974, 4.720032669050099550, 6.616719557880299085 ) ) ;
#14938=CARTESIAN_POINT ( 'NONE',  ( 11.28118179236249929, 3.732952383914999839, 8.749800764654999341 ) ) ;
#14968=CARTESIAN_POINT ( 'NONE',  ( 10.22687885159599830, 5.132709421626000079, 7.635128076451499268 ) ) ;
#15009=CARTESIAN_POINT ( 'NONE',  ( 11.59999999999999964, 4.000000000000000000, 7.500000000000000000 ) ) ;
#15020=UNCERTAINTY_MEASURE_WITH_UNIT (LENGTH_MEASURE( 1.000000000000000082E-05 ), #39578, 'distance_accuracy_value', 'NONE');
#15025=CARTESIAN_POINT ( 'NONE',  ( 11.07210672858429845, 3.307795442047700263, 8.020722037455799480 ) ) ;
#15040=CARTESIAN_POINT ( 'NONE',  ( 10.21462282008599942, 4.523146351753199568, 6.656181553372300108 ) ) ;
#15049=CARTESIAN_POINT ( 'NONE',  ( 10.84393020684979980, 2.750000000000000000, 7.500000000000000000 ) ) ;
#15054=CARTESIAN_POINT ( 'NONE',  ( 11.68748876160954886, 3.399618311400500303, 6.875627981711399883 ) ) ;
#15105=CARTESIAN_POINT ( 'NONE',  ( 9.425038493598998812, 4.627468580434300094, 8.098323595618600379 ) ) ;
#15137=CARTESIAN_POINT ( 'NONE',  ( 11.55300581613033906, 5.107584469683000172, 6.788791567531699656 ) ) ;
#15151=CARTESIAN_POINT ( 'NONE',  ( 8.997405316140000053, 3.728406863338599830, 6.249951378708000327 ) ) ;
#15182=CARTESIAN_POINT ( 'NONE',  ( 9.709696787963999043, 4.219671260427300119, 8.760209873321999297 ) ) ;
#15214=EDGE_CURVE ( 'NONE', #68576, #19063, #27636, .T. ) ;
#15269=CARTESIAN_POINT ( 'NONE',  ( 10.97124174884019965, 3.963805917081910213, 6.184229974648999928 ) ) ;
#15272=ORIENTED_EDGE ( 'NONE', *, *, #35410, .F. ) ;
#15281=CARTESIAN_POINT ( 'NONE',  ( 10.84657802013509986, 2.684088780794000151, 7.530633716161349689 ) ) ;
#15286=CARTESIAN_POINT ( 'NONE',  ( 11.18272066707849888, 5.093522884867000222, 8.161456030935699602 ) ) ;
#15334=MECHANICAL_DESIGN_GEOMETRIC_PRESENTATION_REPRESENTATION('',(#30960),#34312);
#15372=CARTESIAN_POINT ( 'NONE',  ( 10.65364694612719809, 3.195501139158400061, 7.178938988280099132 ) ) ;
#15391=CARTESIAN_POINT ( 'NONE',  ( 10.49764694612699856, 2.940513484064000149, 7.077178005756699974 ) ) ;
#15419=LINE ( 'NONE', #33565, #4813 ) ;
#15450=CARTESIAN_POINT ( 'NONE',  ( 10.18559687351583243, 5.092232985442825210, 8.129523725463618788 ) ) ;
#15453=CARTESIAN_POINT ( 'NONE',  ( 9.577013376692997682, 3.227076647348800176, 7.892807122431200639 ) ) ;
#15468=B_SPLINE_CURVE_WITH_KNOTS ( 'NONE', 3,
 ( #47261, #47608, #42017, #5289 ),
 .UNSPECIFIED., .F., .F.,
 ( 4, 4 ),
 ( 0.8163836489557156906, 1.000000000000000000 ),
 .UNSPECIFIED. ) ;
#15485=CARTESIAN_POINT ( 'NONE',  ( 11.18412378248529926, 3.450971646934100079, 8.538714411016998795 ) ) ;
#15499=CARTESIAN_POINT ( 'NONE',  ( 9.200038493598999167, 4.925784867300699865, 8.382783533462799141 ) ) ;
#15503=B_SPLINE_SURFACE_WITH_KNOTS ( 'NONE', 3, 3, ( 
 ( #60766, #34896, #49934, #66001, #13574, #8321, #19145, #40466, #24397, #45727, #12187, #33516, #54832, #6931, #1693, #44360, #18125, #2045, #65660, #39101, #12531, #33862, #55177, #39445, #57574, #15281, #25077, #4086, #30006, #52336, #63152, #40813, #56555, #14256, #46411 ),
 ( #56897, #62473, #67712, #26114, #20174, #9329, #19838, #35583, #41501, #68397, #62137, #36604, #62814, #9677, #8996, #68059, #10027, #31027, #4430, #25768, #25422, #47442, #57930, #41168, #35914, #30674, #3742, #31366, #52677, #47097, #20520, #30338, #57229, #14933, #4772 ),
 ( #41846, #68748, #14595, #51645, #36257, #20865, #67371, #8659, #51980, #46756, #61797, #13914, #35241, #51308, #3405, #24739, #46066, #19496, #64875, #32399, #43575, #64528, #54054, #11065, #43223, #21546, #16302, #63504, #6502, #16987, #22237, #6151, #31708, #10711, #63847 ),
 ( #64189, #15623, #42203, #37973, #53029, #925, #59645, #11744, #59295, #58268, #27492, #5125, #21205, #37627, #53374, #33086, #26811, #42882, #38317, #32058, #48125, #16647, #48472, #49154, #27847, #53714, #48817, #1266, #11398, #54402, #579, #10370, #26462, #230, #58610 ) ),
 .UNSPECIFIED., .F., .F., .F.,
 ( 4, 4 ),
 ( 4, 1, 1, 1, 1, 1, 1, 1, 1, 1, 1, 1, 1, 1, 1, 1, 1, 1, 1, 1, 1, 1, 1, 1, 1, 1, 1, 1, 1, 1, 1, 1, 4 ),
 ( -0.02000000000000000042, 1.020000000000000018 ),
 ( 0.1633025096610999927, 0.1899619885200000136, 0.2166214673788000034, 0.2432809462376999965, 0.2699404250964999585, 0.2965999039553000038, 0.3232593828141999692, 0.3499188616730000145, 0.3765783405318000043, 0.4032378193906999697, 0.4298972982494999595, 0.4565567771083000048, 0.4832162559671999702, 0.5098757348260000155, 0.5365352136848999809, 0.5631946925437000262, 0.5898541714025000715, 0.6165136502614000369, 0.6431731291201999712, 0.6698326079790000165, 0.6964920868378999819, 0.7231515656967000272, 0.7498110445554999615, 0.7764705234143999268, 0.8031300022731999722, 0.8297894811320000175, 0.8564489599908999828, 0.8831084388497000282, 0.9097679177085999935, 0.9364273965674000388, 0.9630868754261999731, 0.9897463542851000495, 1.016405833144000015 ),
 .UNSPECIFIED. ) ;
#15511=CARTESIAN_POINT ( 'NONE',  ( 8.883506238772763908, 4.136150106583479591, 8.533506295447224943 ) ) ;
#15531=CARTESIAN_POINT ( 'NONE',  ( 10.46957120343300041, 3.937990586507050139, 6.222291352336999815 ) ) ;
#15618=EDGE_CURVE ( 'NONE', #33463, #56577, #24496, .T. ) ;
#15623=CARTESIAN_POINT ( 'NONE',  ( 11.59603632436369125, 3.157359628034400068, 7.696781148700499564 ) ) ;
#15628=CARTESIAN_POINT ( 'NONE',  ( 10.98579841651039857, 3.550031058388499972, 6.303820944768999901 ) ) ;
#15655=CARTESIAN_POINT ( 'NONE',  ( 9.885596873516499627, 2.907767014557175678, 6.870476274536375882 ) ) ;
#15662=CARTESIAN_POINT ( 'NONE',  ( 10.75851354018298522, 4.163624617374472869, 8.749999999999996447 ) ) ;
#15686=LINE ( 'NONE', #48539, #37488 ) ;
#15714=CARTESIAN_POINT ( 'NONE',  ( 11.85159063708299954, 4.825025306051200502, 7.268038553423699533 ) ) ;
#15730=CARTESIAN_POINT ( 'NONE',  ( 11.43302763632549990, 2.964209339073000216, 7.977941233841399971 ) ) ;
#15746=CARTESIAN_POINT ( 'NONE',  ( 11.04333729122639873, 2.996877626170000308, 7.526388557597149642 ) ) ;
#15789=CARTESIAN_POINT ( 'NONE',  ( 9.376392757686998536, 4.677963304775400566, 6.758914271013199304 ) ) ;
#15820=CARTESIAN_POINT ( 'NONE',  ( 11.09590547754519996, 5.315605332491999846, 7.458246194669389872 ) ) ;
#15833=CARTESIAN_POINT ( 'NONE',  ( 9.174709346416998201, 5.155548326249999924, 8.048718920009699573 ) ) ;
#15841=CARTESIAN_POINT ( 'NONE',  ( 9.429533309317625012, 4.633212041316643770, 8.103800281262431682 ) ) ;
#15864=CARTESIAN_POINT ( 'NONE',  ( 9.431076168958000494, 3.350848599899200142, 6.397735581984999698 ) ) ;
#15870=LINE ( 'NONE', #65752, #2079 ) ;
#15900=CARTESIAN_POINT ( 'NONE',  ( 11.41486084871699802, 2.792989229543000107, 7.174999999999999822 ) ) ;
#15906=CARTESIAN_POINT ( 'NONE',  ( 11.59999999999999964, 3.182579051151299687, 7.825000000000000178 ) ) ;
#15952=VERTEX_POINT ( 'NONE', #47449 ) ;
#15965=CARTESIAN_POINT ( 'NONE',  ( 10.05041772631199848, 4.549624259497900169, 6.368647051112000135 ) ) ;
#16009=ORIENTED_EDGE ( 'NONE', *, *, #12313, .F. ) ;
#16039=AXIS2_PLACEMENT_3D ( 'NONE', #14684, #62565, #62902 ) ;
#16049=CARTESIAN_POINT ( 'NONE',  ( 10.70287750876920008, 3.530799696887600092, 6.771886227364699806 ) ) ;
#16060=VERTEX_POINT ( 'NONE', #35166 ) ;
#16063=CARTESIAN_POINT ( 'NONE',  ( 11.42887348028849992, 2.875789035466000065, 6.892162778124999889 ) ) ;
#16078=CARTESIAN_POINT ( 'NONE',  ( 10.79718447801629999, 5.003225587801999552, 7.522119512433738997 ) ) ;
#16114=CARTESIAN_POINT ( 'NONE',  ( 8.724507172011824352, 3.875764422069721604, 6.625492773506611144 ) ) ;
#16132=CARTESIAN_POINT ( 'NONE',  ( 9.323721904869998411, 4.756019688173900306, 7.075568408810499754 ) ) ;
#16162=CARTESIAN_POINT ( 'NONE',  ( 10.59725056272499977, 5.316133253199000208, 7.480494252843770120 ) ) ;
#16176=CARTESIAN_POINT ( 'NONE',  ( 8.946747021775999897, 3.038503783616799847, 6.656252755052399550 ) ) ;
#16188=CARTESIAN_POINT ( 'NONE',  ( 10.03743284169262573, 3.545113930219122800, 8.247402791297171021 ) ) ;
#16208=CARTESIAN_POINT ( 'NONE',  ( 10.54555864497999984, 5.007105485494000696, 6.711254117843599154 ) ) ;
#16251=EDGE_CURVE ( 'NONE', #13504, #14332, #50199, .T. ) ;
#16258=CARTESIAN_POINT ( 'NONE',  ( 11.59999999999999964, 5.207010770456999893, 7.174999999999999822 ) ) ;
#16263=CARTESIAN_POINT ( 'NONE',  ( 11.23424042080529972, 4.544092497359197402, 8.657883396625686956 ) ) ;
#16302=CARTESIAN_POINT ( 'NONE',  ( 10.64902344389989963, 3.116469856398800253, 8.036199780531900316 ) ) ;
#16394=CARTESIAN_POINT ( 'NONE',  ( 11.16641369783139837, 3.949373449607799902, 6.497808498716000081 ) ) ;
#16407=CARTESIAN_POINT ( 'NONE',  ( 11.40425819896749893, 2.744109752373000255, 7.263238376356399684 ) ) ;
#16423=CARTESIAN_POINT ( 'NONE',  ( 11.09256785386839894, 3.167490253789400523, 6.939751505745099358 ) ) ;
#16470=CARTESIAN_POINT ( 'NONE',  ( 8.817138961223998095, 4.718363881473300658, 7.014550357332099750 ) ) ;
#16472=EDGE_CURVE ( 'NONE', #10742, #19003, #41004, .T. ) ;
#16487=CARTESIAN_POINT ( 'NONE',  ( 10.85056919669530018, 4.830699382454300306, 7.254567470917099747 ) ) ;
#16503=CARTESIAN_POINT ( 'NONE',  ( 10.77368717260499942, 3.460071470104900015, 6.618743573831199711 ) ) ;
#16522=CARTESIAN_POINT ( 'NONE',  ( 10.64914416493166449, 3.188141180065802160, 7.176001761109866095 ) ) ;
#16551=B_SPLINE_CURVE_WITH_KNOTS ( 'NONE', 3,
 ( #56547, #30669, #3737, #9672, #13907, #25071 ),
 .UNSPECIFIED., .F., .F.,
 ( 4, 2, 4 ),
 ( 0.000000000000000000, 0.1967045975185045814, 0.3934091950370091628 ),
 .UNSPECIFIED. ) ;
#16554=CARTESIAN_POINT ( 'NONE',  ( 10.01163399569799850, 5.134843509922999871, 7.374045024026299799 ) ) ;
#16604=CARTESIAN_POINT ( 'NONE',  ( 9.178734463322998138, 4.104624583183299258, 6.501052555474699624 ) ) ;
#16636=B_SPLINE_SURFACE_WITH_KNOTS ( 'NONE', 3, 3, ( 
 ( #68182, #4551, #25200, #57018, #68872, #36733, #52107, #58052, #15054, #25890, #30795, #62932, #62594, #36033, #14035, #26241, #10155, #41970, #47221, #51429, #51768, #14381, #35701, #9117, #3866, #4900, #40938, #24861, #9805, #46189, #8782, #47569, #68524, #19962, #67499, #31154, #20991, #61920, #56683, #35361, #52456, #57694, #30126, #14717, #57348, #19617, #62260, #20646, #4211, #9453, #25549, #20299, #46874, #41626, #42997, #53148, #33205, #32515, #54171, #64305, #53492, #11178, #6270, #38089, #27964, #11865, #43355 ),
 ( #48241, #43697, #42327, #6626, #5928, #53830, #5584, #27611, #48593, #26928, #63965, #22359, #64656, #26587, #47909, #32179, #48939, #21328, #17108, #16760, #695, #27269, #37752, #11515, #59416, #32859, #49274, #54524, #6, #16423, #63629, #15746, #1047, #5249, #64991, #59765, #1384, #38442, #58385, #37073, #42656, #16078, #59078, #346, #10492, #21663, #22007, #31832, #10836, #37410, #58731, #29014, #29704, #8358, #12919, #34599, #56251, #39833, #55912, #50320, #38792, #12224, #28658, #39135, #40179, #66733, #18163 ),
 ( #51005, #61495, #23743, #13613, #34935, #7316, #49970, #24091, #22700, #44045, #55566, #60808, #33900, #8015, #2419, #55217, #44398, #2765, #45081, #6972, #28301, #12569, #29353, #1729, #18852, #66388, #18511, #7667, #39485, #61154, #13272, #50664, #45424, #65350, #33551, #34246, #17469, #60118, #54871, #2085, #49623, #23048, #65697, #17821, #60462, #23403, #44741, #66039, #19872, #46789, #52020, #3779, #61832, #25116, #3104, #56936, #19184, #35278, #46448, #4120, #14632, #14968, #35950, #24437, #67748, #57264, #19531 ),
 ( #45763, #40507, #9032, #51681, #41203, #20212, #41538, #62513, #13952, #56594, #9364, #62850, #30710, #25457, #8700, #68095, #67071, #30044, #51347, #3439, #24776, #46103, #30373, #67409, #62172, #40852, #14294, #35623, #24310, #13826, #35154, #61373, #12446, #8233, #28536, #44624, #39710, #7536, #56469, #50200, #44960, #19059, #34125, #2300, #18727, #2640, #3322, #51226, #55787, #29580, #29918, #13491, #50882, #23967, #33778, #55096, #23620, #12796, #8572, #40385, #61030, #45302, #18385, #49849, #34813, #66264, #24654 ) ),
 .UNSPECIFIED., .F., .F., .F.,
 ( 4, 4 ),
 ( 4, 1, 1, 1, 1, 1, 1, 1, 1, 1, 1, 1, 1, 1, 1, 1, 1, 1, 1, 1, 1, 1, 1, 1, 1, 1, 1, 1, 1, 1, 1, 1, 1, 1, 1, 1, 1, 1, 1, 1, 1, 1, 1, 1, 1, 1, 1, 1, 1, 1, 1, 1, 1, 1, 1, 1, 1, 1, 1, 1, 1, 1, 1, 1, 4 ),
 ( -0.02000000000000000042, 1.020000000000000018 ),
 ( 0.008747244164287000176, 0.02453926110774999961, 0.04033127805120999970, 0.05612329499467000327, 0.07191531193812999989, 0.08770732888158999652, 0.1034993458251000087, 0.1192913627684999978, 0.1350833797120000179, 0.1508753966553999792, 0.1666674135988999994, 0.1824594305423999918, 0.1982514474858000086, 0.2140434644293000011, 0.2298354813727000179, 0.2456274983162000103, 0.2614195152596999749, 0.2772115322030999640, 0.2930035491465999842, 0.3087955660900000288, 0.3245875830334999934, 0.3403795999769999581, 0.3561716169204000026, 0.3719636338639000228, 0.3877556508073999875, 0.4035476677507999765, 0.4193396846942999967, 0.4351317016376999858, 0.4509237185811999504, 0.4667157355247000261, 0.4825077524681000152, 0.4982997694115999798, 0.5140917863550000799, 0.5298838032985000446, 0.5456758202420000092, 0.5614678371854000538, 0.5772598541289000185, 0.5930518710723000630, 0.6088438880158000277, 0.6246359049592999924, 0.6404279219027000369, 0.6562199388462000016, 0.6720119557896999662, 0.6878039727331000108, 0.7035959896765999755, 0.7193880066200000201, 0.7351800235634999847, 0.7509720405069999494, 0.7667640574504001050, 0.7825560743939000696, 0.7983480913373000032, 0.8141401082808000789, 0.8299321252243000435, 0.8457241421676999771, 0.8615161591112000528, 0.8773081760545999863, 0.8931001929981000620, 0.9088922099416000266, 0.9246842268849999602, 0.9404762438285000359, 0.9562682607720000005, 0.9720602777153999341, 0.9878522946589000098, 1.003644311601999961, 1.019436328545999970 ),
 .UNSPECIFIED. ) ;
#16647=CARTESIAN_POINT ( 'NONE',  ( 10.77879632507499785, 4.423544049216699747, 6.714825466131699727 ) ) ;
#16652=CARTESIAN_POINT ( 'NONE',  ( 10.09964828895399869, 5.121614868497999851, 6.887384543790600056 ) ) ;
#16732=CARTESIAN_POINT ( 'NONE',  ( 10.35410941423799791, 4.742797679580299963, 8.174686939644999484 ) ) ;
#16748=CARTESIAN_POINT ( 'NONE',  ( 11.13349010443639919, 5.274453806861999716, 7.404690636538299842 ) ) ;
#16760=CARTESIAN_POINT ( 'NONE',  ( 11.33872066707849768, 4.858611803369300652, 8.019361746728900897 ) ) ;
#16805=CARTESIAN_POINT ( 'NONE',  ( 11.00000000000000000, 4.991767524623399233, 7.825000000000000178 ) ) ;
#16827=CARTESIAN_POINT ( 'NONE',  ( 10.75210807141120029, 4.040019166404060336, 6.634727177901499573 ) ) ;
#16844=CARTESIAN_POINT ( 'NONE',  ( 11.67403632436368888, 3.023821283238099955, 7.727966254184200245 ) ) ;
#16874=CARTESIAN_POINT ( 'NONE',  ( 9.986774547327625484, 4.078513067950353843, 8.371417217572535208 ) ) ;
#16880=CARTESIAN_POINT ( 'NONE',  ( 9.643930206848999376, 5.250000000000000000, 7.500000000000000000 ) ) ;
#16889=FACE_OUTER_BOUND ( 'NONE', #10206, .T. ) ;
#16892=CARTESIAN_POINT ( 'NONE',  ( 11.02301463001509774, 4.547357026650399980, 8.376661845795100092 ) ) ;
#16894=CARTESIAN_POINT ( 'NONE',  ( 9.051138961223999857, 5.059894361919000438, 6.783753885003399375 ) ) ;
#16939=CARTESIAN_POINT ( 'NONE',  ( 10.08857120343299840, 3.944651031655580287, 6.359530327585999565 ) ) ;
#16946=CARTESIAN_POINT ( 'NONE',  ( 9.028772138681999238, 3.677371150249499898, 8.304747519296199698 ) ) ;
#16987=CARTESIAN_POINT ( 'NONE',  ( 10.52435971519499880, 4.532462039660099862, 8.385788382729799650 ) ) ;
#17032=CARTESIAN_POINT ( 'NONE',  ( 10.47145237372899906, 4.043732047787757189, 6.225919055146349912 ) ) ;
#17076=CARTESIAN_POINT ( 'NONE',  ( 11.14179841651039915, 3.646693590264900031, 6.560784671286499226 ) ) ;
#17092=CARTESIAN_POINT ( 'NONE',  ( 10.37457053952199892, 3.551693493661699730, 8.548957288282998945 ) ) ;
#17107=CARTESIAN_POINT ( 'NONE',  ( 9.510596873516666605, 4.629523725463622341, 6.407767014557176566 ) ) ;
#17108=CARTESIAN_POINT ( 'NONE',  ( 11.36333594839950045, 4.659759757475400832, 8.256087240512899328 ) ) ;
#17173=CARTESIAN_POINT ( 'NONE',  ( 10.50595525820100029, 3.918212119278319694, 8.362327856951900173 ) ) ;
#17175=EDGE_CURVE ( 'NONE', #26690, #8994, #50114, .T. ) ;
#17190=CARTESIAN_POINT ( 'NONE',  ( 11.44366954483529852, 4.485203148598100320, 8.248643701125299543 ) ) ;
#17208=B_SPLINE_CURVE_WITH_KNOTS ( 'NONE', 3,
 ( #48159, #58644, #21576, #48504 ),
 .UNSPECIFIED., .F., .F.,
 ( 4, 4 ),
 ( 0.000000000000000000, 1.000000000000000000 ),
 .UNSPECIFIED. ) ;
#17224=CARTESIAN_POINT ( 'NONE',  ( 10.16407857760462718, 3.262163830883630489, 7.029755324101339298 ) ) ;
#17246=CARTESIAN_POINT ( 'NONE',  ( 11.59966954483535773, 4.638989336656000440, 8.485927942460499196 ) ) ;
#17248=CARTESIAN_POINT ( 'NONE',  ( 10.26492546752099955, 2.860918852493000486, 7.578921399676699089 ) ) ;
#17275=VECTOR ( 'NONE', #66605, 1000.000000000000000 ) ;
#17297=CARTESIAN_POINT ( 'NONE',  ( 9.305380199233999505, 4.996570247675600207, 7.625259896924899472 ) ) ;
#17304=CARTESIAN_POINT ( 'NONE',  ( 10.09058376188599837, 3.152987476450699766, 6.960174024681499816 ) ) ;
#17401=CARTESIAN_POINT ( 'NONE',  ( 11.39043504475232993, 2.929202812228125286, 6.797261353019674601 ) ) ;
#17433=CARTESIAN_POINT ( 'NONE',  ( 10.28441772631199846, 4.372518460886800185, 6.733203680593099705 ) ) ;
#17453=CARTESIAN_POINT ( 'NONE',  ( 10.17764828895399809, 5.001141961424000471, 6.953185708700699408 ) ) ;
#17469=CARTESIAN_POINT ( 'NONE',  ( 10.84226088462129844, 4.002427228022017225, 8.640738455926999961 ) ) ;
#17517=CARTESIAN_POINT ( 'NONE',  ( 9.045101285863999863, 3.441732526340400167, 8.163359157892799089 ) ) ;
#17535=CARTESIAN_POINT ( 'NONE',  ( 11.24441369783139777, 3.956299011112040187, 6.634905315059499209 ) ) ;
#17542=ADVANCED_FACE ( 'NONE', ( #68956 ), #613, .F. ) ;
#17543=ORIENTED_EDGE ( 'NONE', *, *, #5054, .T. ) ;
#17551=CARTESIAN_POINT ( 'NONE',  ( 11.14767835872009982, 3.125658946326500320, 8.051056647135798272 ) ) ;
#17568=CARTESIAN_POINT ( 'NONE',  ( 10.47683719568447636, 4.186288604638629174, 8.354041075310609799 ) ) ;
#17599=AXIS2_PLACEMENT_3D ( 'NONE', #49072, #23195, #22844 ) ;
#17601=CARTESIAN_POINT ( 'NONE',  ( 11.30878751119029957, 2.958974835389999836, 6.955365841266999638 ) ) ;
#17603=CARTESIAN_POINT ( 'NONE',  ( 9.177784697135001224, 4.694174896253500151, 8.574479223074998657 ) ) ;
#17613=CARTESIAN_POINT ( 'NONE',  ( 8.599999999999999645, 4.000000000000000000, 7.500000000000000000 ) ) ;
#17654=CARTESIAN_POINT ( 'NONE',  ( 9.457355082327998375, 3.550486524676900402, 8.398209294002699110 ) ) ;
#17656=CARTESIAN_POINT ( 'NONE',  ( 9.560596873515667227, 4.629523725463624118, 6.407767014557177454 ) ) ;
#17660=CARTESIAN_POINT ( 'NONE',  ( 9.054101285863998427, 3.441732526340400167, 8.163359157892799089 ) ) ;
#17693=CARTESIAN_POINT ( 'NONE',  ( 10.96914282210478042, 4.267867395145749754, 8.332067702129235087 ) ) ;
#17756=CARTESIAN_POINT ( 'NONE',  ( 11.32299956498189886, 2.792989229543000107, 7.825000000000000178 ) ) ;
#17788=CARTESIAN_POINT ( 'NONE',  ( 11.68333460557258796, 4.162011815820000571, 6.509695444280099608 ) ) ;
#17810=CARTESIAN_POINT ( 'NONE',  ( 11.12299956498149811, 5.207010770456999893, 7.174999999999999822 ) ) ;
#17821=CARTESIAN_POINT ( 'NONE',  ( 10.66995391537419913, 4.943675741382899780, 6.859089544950699668 ) ) ;
#17842=CARTESIAN_POINT ( 'NONE',  ( 8.768793171737998549, 3.595811914175000013, 6.625874414451000227 ) ) ;
#17877=LINE ( 'NONE', #60517, #2513 ) ;
#17885=CARTESIAN_POINT ( 'NONE',  ( 10.65364694612719809, 3.195501139158400061, 7.178938988280099132 ) ) ;
#17900=CARTESIAN_POINT ( 'NONE',  ( 10.93479632507519916, 4.557787252275099732, 6.465962698293999722 ) ) ;
#17912=CARTESIAN_POINT ( 'NONE',  ( 9.893930206848997599, 2.750000000000000000, 7.500000000000000000 ) ) ;
#17929=CARTESIAN_POINT ( 'NONE',  ( 8.846962924124625260, 4.841836872161519700, 7.261582451272839300 ) ) ;
#17949=CARTESIAN_POINT ( 'NONE',  ( 10.51925056272499859, 5.174767082365999471, 7.482589369563879877 ) ) ;
#17951=CARTESIAN_POINT ( 'NONE',  ( 9.986304848515999311, 5.038423216181000086, 7.025224608805800131 ) ) ;
#17997=CARTESIAN_POINT ( 'NONE',  ( 8.976101285863999024, 3.353260484332500013, 8.268485718282699182 ) ) ;
#18005=CARTESIAN_POINT ( 'NONE',  ( 9.712659112603999390, 3.623260508844300176, 6.719118894894999805 ) ) ;
#18058=CARTESIAN_POINT ( 'NONE',  ( 11.12299956498149811, 5.207010770456999893, 7.174999999999999822 ) ) ;
#18061=ORIENTED_EDGE ( 'NONE', *, *, #60222, .T. ) ;
#18062=CARTESIAN_POINT ( 'NONE',  ( 11.15221028326116048, 3.091096528151293210, 7.824988602100019008 ) ) ;
#18076=CARTESIAN_POINT ( 'NONE',  ( 9.810596873515665450, 3.370476274536378103, 8.592232985442823434 ) ) ;
#18125=CARTESIAN_POINT ( 'NONE',  ( 11.22056920625029974, 4.047312782235129802, 8.815417147437999645 ) ) ;
#18130=CARTESIAN_POINT ( 'NONE',  ( 10.94072200990529886, 2.922907051630999842, 7.875713849677398848 ) ) ;
#18145=CARTESIAN_POINT ( 'NONE',  ( 9.015584277044482064, 3.283082709547154643, 6.568532107505763662 ) ) ;
#18148=EDGE_CURVE ( 'NONE', #68176, #1231, #4810, .T. ) ;
#18163=CARTESIAN_POINT ( 'NONE',  ( 10.20641772631199906, 4.431553727090300043, 6.611684804099500212 ) ) ;
#18167=CARTESIAN_POINT ( 'NONE',  ( 8.734814475091132735, 4.056037006134289413, 6.616514917701350029 ) ) ;
#18183=CARTESIAN_POINT ( 'NONE',  ( 8.755786719645998417, 3.934709392726489785, 6.597079156813799194 ) ) ;
#18226=CARTESIAN_POINT ( 'NONE',  ( 11.38795122972049967, 4.398282450130399646, 8.421043941822800249 ) ) ;
#18243=CARTESIAN_POINT ( 'NONE',  ( 10.86190547754509872, 4.891676932241900033, 7.471700551735359852 ) ) ;
#18261=CARTESIAN_POINT ( 'NONE',  ( 9.196006702408606515, 4.999605512837394627, 8.268211173249300217 ) ) ;
#18292=CARTESIAN_POINT ( 'NONE',  ( 10.47769598648999967, 5.009476315410999803, 6.898940957443399746 ) ) ;
#18294=CARTESIAN_POINT ( 'NONE',  ( 8.880265421554998539, 3.785712956512099936, 6.391527115138999626 ) ) ;
#18300=CONICAL_SURFACE ( 'NONE', #16039, 0.9999998338055000602, 0.7853981908209605178 ) ;
#18338=EDGE_CURVE ( 'NONE', #37252, #23962, #67207, .T. ) ;
#18341=DIRECTION ( 'NONE',  ( 1.000000000000000000, 0.000000000000000000, 0.000000000000000000 ) ) ;
#18343=CARTESIAN_POINT ( 'NONE',  ( 9.959912909067998754, 3.190593056227700064, 6.509421987543800192 ) ) ;
#18348=CARTESIAN_POINT ( 'NONE',  ( 9.231405316140000039, 3.815922504313999930, 6.652755395362000002 ) ) ;
#18385=CARTESIAN_POINT ( 'NONE',  ( 10.12426357027499790, 5.254871132332000094, 7.257895958275299542 ) ) ;
#18423=CARTESIAN_POINT ( 'NONE',  ( 9.685596873515667227, 5.092232985442825210, 8.129523725463618788 ) ) ;
#18473=CARTESIAN_POINT ( 'NONE',  ( 11.62994988689359843, 4.518136976474400157, 6.483720595741000459 ) ) ;
#18478=ADVANCED_FACE ( 'NONE', ( #52246 ), #41418, .F. ) ;
#18497=LINE ( 'NONE', #17810, #27683 ) ;
#18502=CARTESIAN_POINT ( 'NONE',  ( 9.614763540183330903, 5.217465845835394411, 7.827184855449092815 ) ) ;
#18511=CARTESIAN_POINT ( 'NONE',  ( 11.08841369783139896, 3.942447888101379583, 6.360711682373000109 ) ) ;
#18576=CARTESIAN_POINT ( 'NONE',  ( 10.43210941423799909, 4.641185166475500168, 8.082391773166900606 ) ) ;
#18607=CARTESIAN_POINT ( 'NONE',  ( 9.258504216683467902, 4.163629870566138536, 8.749972943975897977 ) ) ;
#18616=CARTESIAN_POINT ( 'NONE',  ( 9.024266954400625096, 3.674418004489155010, 8.312113682386053526 ) ) ;
#18638=CARTESIAN_POINT ( 'NONE',  ( 10.00962143724499853, 4.667147537636399335, 8.250837174995698575 ) ) ;
#18683=CARTESIAN_POINT ( 'NONE',  ( 9.835279731608999043, 4.102460098134500299, 8.637205511891998810 ) ) ;
#18727=CARTESIAN_POINT ( 'NONE',  ( 10.56733863405299800, 4.788475529394700558, 6.494205428462000107 ) ) ;
#18822=CARTESIAN_POINT ( 'NONE',  ( 11.11302897915239818, 4.291996373817799970, 6.397263297997000109 ) ) ;
#18852=CARTESIAN_POINT ( 'NONE',  ( 11.13764426047339917, 4.613828180779599997, 6.538488127609999978 ) ) ;
#18879=CARTESIAN_POINT ( 'NONE',  ( 9.242292592096250203, 3.634505416671740097, 8.705986097797767442 ) ) ;
#18893=CARTESIAN_POINT ( 'NONE',  ( 10.30226354018233437, 2.907767014557178786, 8.129523725463625894 ) ) ;
#18899=CARTESIAN_POINT ( 'NONE',  ( 11.53192018828833731, 3.091029700564639437, 7.824998071251875409 ) ) ;
#18917=CARTESIAN_POINT ( 'NONE',  ( 11.63410404293056999, 3.557672215630899970, 6.599279737936000423 ) ) ;
#18954=ADVANCED_FACE ( 'NONE', ( #53276 ), #22964, .F. ) ;
#18975=CARTESIAN_POINT ( 'NONE',  ( 10.29399293566599916, 4.546741702992100009, 6.829299525004299376 ) ) ;
#18977=CARTESIAN_POINT ( 'NONE',  ( 9.933633995697999097, 4.998281561686200192, 7.389201877599999690 ) ) ;
#19003=VERTEX_POINT ( 'NONE', #396 ) ;
#19020=DIRECTION ( 'NONE',  ( 0.000000000000000000, 0.000000000000000000, 1.000000000000000000 ) ) ;
#19022=CARTESIAN_POINT ( 'NONE',  ( 8.644809814040998575, 4.698458605182900705, 6.596733927440100231 ) ) ;
#19028=CARTESIAN_POINT ( 'NONE',  ( 11.59999999999999964, 3.168976350368595263, 7.002620348270788497 ) ) ;
#19059=CARTESIAN_POINT ( 'NONE',  ( 10.64118447801629941, 5.277702140407999565, 7.528171279442569919 ) ) ;
#19063=VERTEX_POINT ( 'NONE', #66786 ) ;
#19096=CARTESIAN_POINT ( 'NONE',  ( 11.59999999999999964, 5.179498027601999510, 7.825000000000000178 ) ) ;
#19145=CARTESIAN_POINT ( 'NONE',  ( 11.63611496860034933, 5.171412538012999605, 8.100294210499798808 ) ) ;
#19151=CARTESIAN_POINT ( 'NONE',  ( 10.37457053952199892, 3.551693493661699730, 8.548957288282998945 ) ) ;
#19163=B_SPLINE_CURVE_WITH_KNOTS ( 'NONE', 3,
 ( #59555, #7109, #60255, #14000, #1519, #11655, #832, #12357, #12703, #22838, #12007, #33689, #34040, #65830, #43488, #64785, #55007, #43832 ),
 .UNSPECIFIED., .F., .F.,
 ( 4, 2, 2, 2, 2, 2, 2, 2, 4 ),
 ( 0.000000000000000000, 0.1250000000000000000, 0.2500000000000000000, 0.3750000000000000000, 0.5000000000000000000, 0.6250000000000000000, 0.7500000000000000000, 0.8750000000000000000, 1.000000000000000000 ),
 .UNSPECIFIED. ) ;
#19179=CARTESIAN_POINT ( 'NONE',  ( 9.843930206850000530, 2.750000000000000000, 7.500000000000000000 ) ) ;
#19184=CARTESIAN_POINT ( 'NONE',  ( 10.34995525820099971, 3.892289273474800471, 8.635644537520001052 ) ) ;
#19222=CARTESIAN_POINT ( 'NONE',  ( 10.27101354018233437, 3.231816600031359066, 8.499583552997725278 ) ) ;
#19234=FACE_OUTER_BOUND ( 'NONE', #13420, .T. ) ;
#19249=CARTESIAN_POINT ( 'NONE',  ( 10.40749413291699987, 4.788043169210699723, 7.859564368461399830 ) ) ;
#19264=CARTESIAN_POINT ( 'NONE',  ( 10.69568717260499824, 3.533932086969799879, 6.739296831621899742 ) ) ;
#19298=CARTESIAN_POINT ( 'NONE',  ( 11.23627509987185746, 3.727547057523675988, 8.749999999999998224 ) ) ;
#19309=CARTESIAN_POINT ( 'NONE',  ( 10.69568717260499824, 3.533932086969799879, 6.739296831621899742 ) ) ;
#19312=CARTESIAN_POINT ( 'NONE',  ( 9.353076168957999315, 3.420574098817999786, 6.516130052788599691 ) ) ;
#19345=ORIENTED_EDGE ( 'NONE', *, *, #62774, .F. ) ;
#19363=CARTESIAN_POINT ( 'NONE',  ( 9.100734463322998735, 4.118936914955599882, 6.364399516445999438 ) ) ;
#19482=CARTESIAN_POINT ( 'NONE',  ( 10.72191429142990060, 4.025072603369280522, 8.816028813488999916 ) ) ;
#19496=CARTESIAN_POINT ( 'NONE',  ( 11.02301463001509774, 4.547357026650399980, 8.376661845795100092 ) ) ;
#19501=CARTESIAN_POINT ( 'NONE',  ( 11.01041369783139956, 3.935522326596939902, 6.223614866029000048 ) ) ;
#19527=DIRECTION ( 'NONE',  ( -1.000000000000000000, 0.000000000000000000, 1.665334536957000056E-14 ) ) ;
#19531=CARTESIAN_POINT ( 'NONE',  ( 10.12841772631199966, 4.490588993294299947, 6.490165927606000196 ) ) ;
#19587=DIRECTION ( 'NONE',  ( -1.000000000000000000, 0.000000000000000000, 0.000000000000000000 ) ) ;
#19590=VERTEX_POINT ( 'NONE', #13831 ) ;
#19605=CARTESIAN_POINT ( 'NONE',  ( 11.46179707368349909, 3.501542828836900156, 8.370914060838998694 ) ) ;
#19617=CARTESIAN_POINT ( 'NONE',  ( 10.77672335273219950, 4.301522290735800169, 6.687976048055599421 ) ) ;
#19664=CARTESIAN_POINT ( 'NONE',  ( 10.86190547754509872, 4.891676932241900033, 7.471700551735359852 ) ) ;
#19666=CARTESIAN_POINT ( 'NONE',  ( 9.731000818238999983, 3.111278474435999808, 7.032008172796599510 ) ) ;
#19701=CARTESIAN_POINT ( 'NONE',  ( 11.00000000000000000, 3.031410575668799900, 7.825000000000000178 ) ) ;
#19713=CARTESIAN_POINT ( 'NONE',  ( 8.720797255587999786, 5.140789995332999851, 7.548297453605989027 ) ) ;
#19763=ORIENTED_EDGE ( 'NONE', *, *, #40642, .F. ) ;
#19828=CARTESIAN_POINT ( 'NONE',  ( 11.05435090131019926, 5.119447121461000449, 6.807613609764599616 ) ) ;
#19838=CARTESIAN_POINT ( 'NONE',  ( 11.55811496860034815, 5.045590851977999947, 8.035816473382100256 ) ) ;
#19844=CARTESIAN_POINT ( 'NONE',  ( 10.73964560330029983, 4.391636236366600166, 8.716526793355999558 ) ) ;
#19869=CARTESIAN_POINT ( 'NONE',  ( 11.41486084871699802, 2.792989229543000107, 7.174999999999999822 ) ) ;
#19872=CARTESIAN_POINT ( 'NONE',  ( 10.54687750876899877, 3.382085645339300228, 6.541108991297599928 ) ) ;
#19903=FACE_OUTER_BOUND ( 'NONE', #12456, .T. ) ;
#19916=CARTESIAN_POINT ( 'NONE',  ( 10.14601354018233259, 4.999583552997728830, 8.268183399968640046 ) ) ;
#19931=CARTESIAN_POINT ( 'NONE',  ( 11.14595257254739913, 3.168263696564200149, 7.258104750172799768 ) ) ;
#19947=CARTESIAN_POINT ( 'NONE',  ( 11.21149010443640037, 5.137564434800999891, 7.414927836855409460 ) ) ;
#19961=CARTESIAN_POINT ( 'NONE',  ( 9.354346873516664829, 2.749999999999999112, 7.336375382625534236 ) ) ;
#19962=CARTESIAN_POINT ( 'NONE',  ( 11.07210672858429845, 3.307795442047700263, 8.020722037455799480 ) ) ;
#19989=CARTESIAN_POINT ( 'NONE',  ( 10.53521345716899837, 4.924890298941200228, 6.659120737011199331 ) ) ;
#20006=CARTESIAN_POINT ( 'NONE',  ( 10.40480513895999870, 4.779740423663599636, 7.933462475324499330 ) ) ;
#20008=CARTESIAN_POINT ( 'NONE',  ( 10.10892546752099896, 3.135062625344399834, 7.559927309296559983 ) ) ;
#20038=CARTESIAN_POINT ( 'NONE',  ( 11.67766954483535891, 4.715882430684499305, 8.604570063127999546 ) ) ;
#20053=CARTESIAN_POINT ( 'NONE',  ( 9.782608878791998919, 3.710311786319799854, 8.745979585038000437 ) ) ;
#20084=CARTESIAN_POINT ( 'NONE',  ( 10.21627973160999936, 4.114789684104299461, 8.774051692788999546 ) ) ;
#20121=CARTESIAN_POINT ( 'NONE',  ( 11.07273594314529142, 5.128905988536224037, 7.824979517142727659 ) ) ;
#20165=CARTESIAN_POINT ( 'NONE',  ( 11.63611496860034933, 5.171412538012999605, 8.100294210499798808 ) ) ;
#20174=CARTESIAN_POINT ( 'NONE',  ( 11.64122412107036908, 4.062069863985690255, 8.673243607771999208 ) ) ;
#20180=CARTESIAN_POINT ( 'NONE',  ( 11.50271932425157040, 3.812601581225100400, 6.235801371442999397 ) ) ;
#20212=CARTESIAN_POINT ( 'NONE',  ( 11.52733460557258915, 4.206337284815599986, 6.238754009183999472 ) ) ;
#20243=PLANE ( 'NONE',  #2658 ) ;
#20269=CARTESIAN_POINT ( 'NONE',  ( 11.76133460557259980, 4.139849081322200419, 6.645166161828299778 ) ) ;
#20283=CARTESIAN_POINT ( 'NONE',  ( 11.41544519387737289, 4.732426395176744016, 7.982107551664254785 ) ) ;
#20285=CARTESIAN_POINT ( 'NONE',  ( 10.23103300763299828, 4.692441239783899931, 6.773725604892799623 ) ) ;
#20299=CARTESIAN_POINT ( 'NONE',  ( 10.62903166480609940, 3.135947233695900227, 7.439078678739090122 ) ) ;
#20310=CARTESIAN_POINT ( 'NONE',  ( 11.02755399909320566, 4.133346405062087392, 6.221473734489903151 ) ) ;
#20328=CARTESIAN_POINT ( 'NONE',  ( 8.731616107288068918, 4.000002263255225898, 6.618420992905501343 ) ) ;
#20345=CARTESIAN_POINT ( 'NONE',  ( 9.678329965421998082, 3.397808798486600335, 6.876242273533999416 ) ) ;
#20379=EDGE_LOOP ( 'NONE', ( #12552, #25301, #61068, #27549 ) ) ;
#20392=PRESENTATION_STYLE_ASSIGNMENT (( #46629 ) ) ;
#20394=CARTESIAN_POINT ( 'NONE',  ( 9.250696787962999323, 4.219671260427300119, 8.760209873321999297 ) ) ;
#20405=CARTESIAN_POINT ( 'NONE',  ( 8.896714042595458949, 3.863849893574821781, 8.546714100015048388 ) ) ;
#20520=CARTESIAN_POINT ( 'NONE',  ( 10.56080513895999928, 5.026880838510000338, 8.070849345005600028 ) ) ;
#20525=CARTESIAN_POINT ( 'NONE',  ( 11.25656651104150008, 4.126085365637900182, 8.771777834828998976 ) ) ;
#20560=CARTESIAN_POINT ( 'NONE',  ( 10.71684687351633869, 4.768183399968648040, 8.499583552997721725 ) ) ;
#20599=DIRECTION ( 'NONE',  ( 0.000000000000000000, 1.000000000000000000, 0.000000000000000000 ) ) ;
#20615=CARTESIAN_POINT ( 'NONE',  ( 10.38287885159599888, 4.860099138268600072, 7.602606670248799325 ) ) ;
#20631=CARTESIAN_POINT ( 'NONE',  ( 11.69559063708295987, 5.086518862378000883, 7.194517870904999945 ) ) ;
#20643=ORIENTED_EDGE ( 'NONE', *, *, #27402, .F. ) ;
#20646=CARTESIAN_POINT ( 'NONE',  ( 10.72749279009019929, 3.774717370312400178, 6.663611138821799784 ) ) ;
#20691=CARTESIAN_POINT ( 'NONE',  ( 10.21684687351595677, 4.768183399968648040, 8.499583552997721725 ) ) ;
#20694=CARTESIAN_POINT ( 'NONE',  ( 9.956950584426998319, 4.344127791340399725, 8.295791434820300125 ) ) ;
#20724=CARTESIAN_POINT ( 'NONE',  ( 11.80233327354039830, 2.898463260143000042, 8.220500279733599314 ) ) ;
#20727=CARTESIAN_POINT ( 'NONE',  ( 11.07907162307749793, 3.185388239149200107, 7.825000000000000178 ) ) ;
#20739=CARTESIAN_POINT ( 'NONE',  ( 9.833267173155999075, 3.026371913119300316, 8.329718467866699783 ) ) ;
#20740=SURFACE_STYLE_USAGE ( .BOTH. , #6367 ) ;
#20752=CARTESIAN_POINT ( 'NONE',  ( 8.903317944506808246, 3.725094887964653267, 8.526233764311367480 ) ) ;
#20769=LINE ( 'NONE', #3646, #44806 ) ;
#20771=CARTESIAN_POINT ( 'NONE',  ( 10.14029229006299992, 5.106256438265999620, 8.142324746736500529 ) ) ;
#20833=APPLICATION_CONTEXT ( 'automotive_design' ) ;
#20865=CARTESIAN_POINT ( 'NONE',  ( 11.52166954483529793, 4.562096242626500597, 8.367285821793199574 ) ) ;
#20870=CARTESIAN_POINT ( 'NONE',  ( 11.62579573085663043, 5.239377455231000624, 7.285547569258399747 ) ) ;
#20889=DIRECTION ( 'NONE',  ( 0.000000000000000000, 1.000000000000000000, 0.000000000000000000 ) ) ;
#20901=CARTESIAN_POINT ( 'NONE',  ( 10.04184687351587613, 4.999583552997725278, 6.731816600031356401 ) ) ;
#20906=CARTESIAN_POINT ( 'NONE',  ( 10.84184687351628540, 3.000416447002276943, 8.268183399968647151 ) ) ;
#20960=CARTESIAN_POINT ( 'NONE',  ( 10.53057053952199951, 3.659587858614300249, 8.296503712697200328 ) ) ;
#20977=CARTESIAN_POINT ( 'NONE',  ( 10.30487885159599770, 4.996404279947399552, 7.618867373350600047 ) ) ;
#20988=CARTESIAN_POINT ( 'NONE',  ( 11.05391045180431675, 5.129049487418005704, 6.885461205208883051 ) ) ;
#20991=CARTESIAN_POINT ( 'NONE',  ( 10.99826088462129903, 4.001843064679911244, 8.366195817038299509 ) ) ;
#21038=CARTESIAN_POINT ( 'NONE',  ( 9.982279731608999285, 4.077800926195140008, 8.363513150096299142 ) ) ;
#21069=CARTESIAN_POINT ( 'NONE',  ( 11.26212378248529866, 3.384904051819500381, 8.663708617168998316 ) ) ;
#21086=CARTESIAN_POINT ( 'NONE',  ( 9.098721904869998767, 5.115452802765999785, 6.873781641694999500 ) ) ;
#21096=CARTESIAN_POINT ( 'NONE',  ( 9.784141369869628235, 4.423591863150092784, 6.734426879786121312 ) ) ;
#21117=CARTESIAN_POINT ( 'NONE',  ( 9.481734463323000739, 4.133249246727800141, 6.227746477418000026 ) ) ;
#21180=EDGE_CURVE ( 'NONE', #44978, #25385, #4928, .T. ) ;
#21205=CARTESIAN_POINT ( 'NONE',  ( 11.15278751119019773, 3.209519379020799867, 7.086443476450299706 ) ) ;
#21226=EDGE_LOOP ( 'NONE', ( #5630, #17543, #24386, #25521, #59838, #3547, #64642 ) ) ;
#21254=VERTEX_POINT ( 'NONE', #58673 ) ;
#21298=CARTESIAN_POINT ( 'NONE',  ( 10.85056919669530018, 4.830699382454300306, 7.254567470917099747 ) ) ;
#21313=CARTESIAN_POINT ( 'NONE',  ( 10.51810807141099779, 4.059045408506610109, 6.223352037434000117 ) ) ;
#21328=CARTESIAN_POINT ( 'NONE',  ( 11.38795122972049967, 4.398282450130399646, 8.421043941822800249 ) ) ;
#21357=CARTESIAN_POINT ( 'NONE',  ( 8.719734573340000239, 3.777330902948500047, 6.647493632115700102 ) ) ;
#21374=CARTESIAN_POINT ( 'NONE',  ( 9.880963142879998884, 4.848366390061300102, 7.678836273503299559 ) ) ;
#21416=VERTEX_POINT ( 'NONE', #59021 ) ;
#21417=CARTESIAN_POINT ( 'NONE',  ( 9.681292290062998518, 5.106256438265999620, 8.142324746736500529 ) ) ;
#21424=CARTESIAN_POINT ( 'NONE',  ( 9.201570984676626708, 3.555997837402618877, 6.746080675052237297 ) ) ;
#21425=CARTESIAN_POINT ( 'NONE',  ( 8.876902336861419940, 4.269588175475917957, 8.499844062317453819 ) ) ;
#21433=VERTEX_POINT ( 'NONE', #65633 ) ;
#21449=CARTESIAN_POINT ( 'NONE',  ( 10.06430484851600049, 5.163382381259999931, 6.968092280137199168 ) ) ;
#21470=ORIENTED_EDGE ( 'NONE', *, *, #15618, .T. ) ;
#21494=CARTESIAN_POINT ( 'NONE',  ( 11.59999999999999787, 3.205140046301731438, 7.924485708373446791 ) ) ;
#21546=CARTESIAN_POINT ( 'NONE',  ( 10.69057802013490033, 2.966773425016000054, 7.524052967375959966 ) ) ;
#21551=CARTESIAN_POINT ( 'NONE',  ( 10.07503300763299947, 4.881889043637199777, 6.575021251017499679 ) ) ;
#21576=CARTESIAN_POINT ( 'NONE',  ( 11.25740844561608611, 5.045781347359230118, 7.824999626888802240 ) ) ;
#21635=CARTESIAN_POINT ( 'NONE',  ( 11.41256651104150066, 4.098999650273559503, 8.498573944230598087 ) ) ;
#21649=CARTESIAN_POINT ( 'NONE',  ( 11.25656651104150008, 4.126085365637900182, 8.771777834828998976 ) ) ;
#21663=CARTESIAN_POINT ( 'NONE',  ( 10.69872335273220010, 4.349306362047499874, 6.559289673553299060 ) ) ;
#21694=CARTESIAN_POINT ( 'NONE',  ( 8.741252916288999586, 4.092558584984410608, 6.625425395127999550 ) ) ;
#21725=CARTESIAN_POINT ( 'NONE',  ( 11.02287616594229824, 3.738072157442200005, 8.325646653015098764 ) ) ;
#21743=CARTESIAN_POINT ( 'NONE',  ( 11.64633327354034797, 3.135095881599500256, 8.065722083251399610 ) ) ;
#21761=CARTESIAN_POINT ( 'NONE',  ( 10.50145247700547557, 3.917463882723016599, 8.370216864706282678 ) ) ;
#21771=CARTESIAN_POINT ( 'NONE',  ( 9.480191603681626944, 4.150249255682260774, 8.361949783971203587 ) ) ;
#21793=CARTESIAN_POINT ( 'NONE',  ( 11.01279632507519857, 4.624908853805600906, 6.341531314375999706 ) ) ;
#21795=CARTESIAN_POINT ( 'NONE',  ( 9.555709346417000205, 5.031430618794000331, 7.989780896525600085 ) ) ;
#21862=AXIS2_PLACEMENT_3D ( 'NONE', #33404, #27821, #44935 ) ;
#21890=VERTEX_POINT ( 'NONE', #51797 ) ;
#21979=CARTESIAN_POINT ( 'NONE',  ( 10.42795525820099911, 3.905250696375530239, 8.498986197235801399 ) ) ;
#21992=CARTESIAN_POINT ( 'NONE',  ( 10.76426088462129904, 4.002719309691810778, 8.778009775371000245 ) ) ;
#22002=EDGE_LOOP ( 'NONE', ( #36290, #8594, #7624 ) ) ;
#22005=ORIENTED_EDGE ( 'NONE', *, *, #51992, .T. ) ;
#22007=CARTESIAN_POINT ( 'NONE',  ( 10.67410807141119911, 4.046361247106100123, 6.497602131078999754 ) ) ;
#22019=ORIENTED_EDGE ( 'NONE', *, *, #48137, .T. ) ;
#22036=ADVANCED_FACE ( 'NONE', ( #35390 ), #1610, .F. ) ;
#22069=CARTESIAN_POINT ( 'NONE',  ( 11.09672200990539892, 3.182132064022000328, 7.785290430335599865 ) ) ;
#22089=CARTESIAN_POINT ( 'NONE',  ( 10.44125056272499918, 5.033400911533000510, 7.484684486284700178 ) ) ;
#22118=CARTESIAN_POINT ( 'NONE',  ( 10.18940772478662637, 3.446387339840331965, 6.822471183635139269 ) ) ;
#22141=CARTESIAN_POINT ( 'NONE',  ( 11.18923293495519822, 2.967327562101000016, 7.541513160549049744 ) ) ;
#22143=CARTESIAN_POINT ( 'NONE',  ( 9.809000818239997699, 2.989704013253000614, 6.967988282883199602 ) ) ;
#22193=CARTESIAN_POINT ( 'NONE',  ( 10.16455864497999961, 4.898932057185599653, 6.795973491698399371 ) ) ;
#22237=CARTESIAN_POINT ( 'NONE',  ( 10.48280513895999988, 4.903310631086600146, 8.002155910165599906 ) ) ;
#22256=ORIENTED_EDGE ( 'NONE', *, *, #65832, .T. ) ;
#22324=CARTESIAN_POINT ( 'NONE',  ( 11.38795122972049967, 4.398282450130399646, 8.421043941822800249 ) ) ;
#22342=CARTESIAN_POINT ( 'NONE',  ( 10.13662282008599824, 4.594711216567399781, 6.540749699823199315 ) ) ;
#22359=CARTESIAN_POINT ( 'NONE',  ( 11.53564291764652872, 3.004110626587600308, 7.623106493640399606 ) ) ;
#22397=CARTESIAN_POINT ( 'NONE',  ( 11.33810207955129812, 4.796537143354000499, 7.174999999999999822 ) ) ;
#22414=B_SPLINE_CURVE_WITH_KNOTS ( 'NONE', 3,
 ( #33491, #22636, #22985, #54804, #60052, #12853, #17401, #49556, #1668 ),
 .UNSPECIFIED., .F., .F.,
 ( 4, 1, 1, 1, 1, 1, 4 ),
 ( 0.000000000000000000, 0.1176715969261408201, 0.3173201826739890374, 0.5169687684225858781, 0.7166173541704341510, 0.9162659399182827569, 1.000000000000000000 ),
 .UNSPECIFIED. ) ;
#22420=CARTESIAN_POINT ( 'NONE',  ( 10.53057053952199951, 3.659587858614300249, 8.296503712697200328 ) ) ;
#22434=CARTESIAN_POINT ( 'NONE',  ( 10.39969598649000027, 4.888000489779200208, 6.971269690999399415 ) ) ;
#22452=CARTESIAN_POINT ( 'NONE',  ( 9.373082992855458428, 2.782568642349716459, 7.827172124334915715 ) ) ;
#22460=CARTESIAN_POINT ( 'NONE',  ( 9.758812222687625493, 4.162730299909893183, 6.640319176431033199 ) ) ;
#22483=CARTESIAN_POINT ( 'NONE',  ( 10.81524174883999834, 3.971581146373189597, 6.466884287543999577 ) ) ;
#22485=CARTESIAN_POINT ( 'NONE',  ( 10.16360887879199915, 3.741427262966100287, 8.612148635591999835 ) ) ;
#22529=ORIENTED_EDGE ( 'NONE', *, *, #55169, .F. ) ;
#22533=CARTESIAN_POINT ( 'NONE',  ( 9.887950584426999256, 4.398663815465100768, 8.421905343605699201 ) ) ;
#22540=CARTESIAN_POINT ( 'NONE',  ( 9.864633995697998259, 4.861719613449499988, 7.404358731173799946 ) ) ;
#22636=CARTESIAN_POINT ( 'NONE',  ( 11.56493925477931128, 5.173530340702487962, 7.051164236119339179 ) ) ;
#22669=CARTESIAN_POINT ( 'NONE',  ( 11.78179573085659904, 4.973133828855400118, 7.331616337578100051 ) ) ;
#22686=CARTESIAN_POINT ( 'NONE',  ( 10.81349144726329925, 3.261052100888700345, 8.542723541016000510 ) ) ;
#22700=CARTESIAN_POINT ( 'NONE',  ( 11.53148876160955005, 3.209326035813000022, 6.677731919207799294 ) ) ;
#22749=CARTESIAN_POINT ( 'NONE',  ( 8.994442991499997930, 3.945420918055940085, 8.365291319916600798 ) ) ;
#22767=CARTESIAN_POINT ( 'NONE',  ( 11.14595257254739913, 3.168263696564200149, 7.258104750172799768 ) ) ;
#22780=CARTESIAN_POINT ( 'NONE',  ( 10.89835090130999973, 4.878966983716200190, 6.956352367771000189 ) ) ;
#22808=ADVANCED_FACE ( 'NONE', ( #67968 ), #42439, .F. ) ;
#22830=EDGE_CURVE ( 'NONE', #16060, #21890, #20769, .T. ) ;
#22831=CARTESIAN_POINT ( 'NONE',  ( 10.98146005378009882, 4.911671201000399556, 7.986817550794899745 ) ) ;
#22834=CARTESIAN_POINT ( 'NONE',  ( 8.949822372493999367, 3.632306086542600010, 6.297150255604999636 ) ) ;
#22838=CARTESIAN_POINT ( 'NONE',  ( 10.50851354018319128, 3.836375382625529795, 6.250000000000000888 ) ) ;
#22844=DIRECTION ( 'NONE',  ( 0.000000000000000000, 1.000000000000000000, 0.000000000000000000 ) ) ;
#22882=ORIENTED_EDGE ( 'NONE', *, *, #56965, .F. ) ;
#22883=CARTESIAN_POINT ( 'NONE',  ( 9.356038493598999750, 4.726907342723099426, 8.193143574899998782 ) ) ;
#22888=CARTESIAN_POINT ( 'NONE',  ( 9.079430433046999482, 3.262177192690499883, 7.955330044604899342 ) ) ;
#22921=CARTESIAN_POINT ( 'NONE',  ( 11.01837338474678063, 3.735675910162961078, 8.333200082717626245 ) ) ;
#22964=B_SPLINE_SURFACE_WITH_KNOTS ( 'NONE', 3, 3, ( 
 ( #47348, #67970, #16208, #25326, #63752, #15531, #52237, #31960, #32308, #52583, #48029, #41754, #37196, #41413, #68653, #20084, #62719, #26018, #20771, #31611, #135, #21449, #10278, #57476, #26367, #47004, #10618, #9583, #5378, #63054, #4676, #42443, #30927, #4338, #68306, #15182, #26716, #42785, #36505, #58176, #63408, #47693, #57827, #69005, #21117, #36856, #15864, #64094, #37883, #59895, #1515, #11306, #5715, #53956, #44531, #6059, #17603, #6404, #65825, #65479, #7103, #16894, #27396, #65127, #28441, #64432, #22834 ),
 ( #43827, #59203, #27058, #27752, #44180, #28089, #38223, #48725, #60592, #49755, #17248, #55002, #6750, #38928, #22485, #54655, #32986, #49064, #826, #48371, #16554, #17951, #49403, #59551, #60250, #12352, #33685, #53618, #22143, #33340, #479, #1865, #39269, #11651, #32644, #12698, #38571, #23184, #21795, #43128, #43483, #64781, #54302, #1171, #12002, #56733, #19312, #67201, #35069, #29137, #3240, #23528, #24567, #2214, #3572, #55348, #50108, #60939, #7445, #67543, #66174, #39968, #13055, #50445, #24215, #18294, #28795 ),
 ( #44870, #8487, #34382, #45890, #62310, #40636, #45558, #29833, #24905, #40987, #14082, #66864, #46238, #13401, #61971, #35407, #8827, #18638, #55700, #39614, #18977, #56385, #30170, #51138, #51475, #2547, #50799, #34724, #19666, #34036, #29492, #7798, #23874, #61285, #45213, #66515, #8143, #56035, #2891, #40302, #61623, #13736, #15789, #57398, #42371, #47266, #58435, #9853, #4259, #25938, #26288, #36083, #68226, #57744, #9163, #26638, #14427, #4950, #68571, #62640, #63672, #42708, #41672, #5296, #47614, #37120, #46923 ),
 ( #25245, #31533, #67890, #10539, #4602, #68924, #52504, #9503, #30845, #46583, #20008, #58098, #41333, #52853, #35744, #21038, #20694, #10201, #47955, #21374, #31880, #42023, #54, #62978, #53196, #57063, #30500, #20345, #14766, #52156, #63324, #15453, #51813, #36776, #3911, #25597, #31199, #15105, #36427, #38846, #59465, #16132, #54575, #48643, #48291, #58777, #38138, #12275, #32231, #11916, #65398, #10886, #17517, #37801, #22749, #27667, #60170, #11562, #53877, #6318, #6671, #16470, #743, #32906, #53544, #7022, #64013 ) ),
 .UNSPECIFIED., .F., .F., .F.,
 ( 4, 4 ),
 ( 4, 1, 1, 1, 1, 1, 1, 1, 1, 1, 1, 1, 1, 1, 1, 1, 1, 1, 1, 1, 1, 1, 1, 1, 1, 1, 1, 1, 1, 1, 1, 1, 1, 1, 1, 1, 1, 1, 1, 1, 1, 1, 1, 1, 1, 1, 1, 1, 1, 1, 1, 1, 1, 1, 1, 1, 1, 1, 1, 1, 1, 1, 1, 1, 4 ),
 ( -0.02000000000000000042, 1.020000000000000018 ),
 ( -0.02000000000000000042, -0.003749999999999999861, 0.01250000000000000069, 0.02875000000000000125, 0.04499999999999999833, 0.06124999999999999889, 0.07749999999999999944, 0.09375000000000000000, 0.1100000000000000006, 0.1262500000000000011, 0.1424999999999999878, 0.1587500000000000022, 0.1749999999999999889, 0.1912500000000000033, 0.2074999999999999900, 0.2237500000000000044, 0.2399999999999999911, 0.2562499999999999778, 0.2725000000000000200, 0.2887500000000000067, 0.3049999999999999933, 0.3212499999999999800, 0.3375000000000000222, 0.3537500000000000089, 0.3699999999999999956, 0.3862499999999999822, 0.4025000000000000244, 0.4187500000000000111, 0.4349999999999999978, 0.4512499999999999845, 0.4675000000000000266, 0.4837500000000000133, 0.5000000000000000000, 0.5162499999999999867, 0.5324999999999999734, 0.5487499999999999600, 0.5649999999999999467, 0.5812500000000000444, 0.5975000000000000311, 0.6137500000000000178, 0.6300000000000000044, 0.6462499999999999911, 0.6624999999999999778, 0.6787499999999999645, 0.6949999999999999512, 0.7112500000000000488, 0.7275000000000000355, 0.7437500000000000222, 0.7600000000000000089, 0.7762499999999999956, 0.7924999999999999822, 0.8087499999999999689, 0.8249999999999999556, 0.8412500000000000533, 0.8575000000000000400, 0.8737500000000000266, 0.8900000000000000133, 0.9062500000000000000, 0.9224999999999999867, 0.9387499999999999734, 0.9549999999999999600, 0.9712499999999999467, 0.9875000000000000444, 1.003749999999999920, 1.020000000000000018 ),
 .UNSPECIFIED. ) ;
#22985=CARTESIAN_POINT ( 'NONE',  ( 11.54292372906208897, 5.032542535543790052, 6.730835578941808173 ) ) ;
#23018=CARTESIAN_POINT ( 'NONE',  ( 11.46179707368349909, 3.501542828836900156, 8.370914060838998694 ) ) ;
#23048=CARTESIAN_POINT ( 'NONE',  ( 10.71918447801630059, 5.140463864104999558, 7.525145395936648995 ) ) ;
#23116=CARTESIAN_POINT ( 'NONE',  ( 10.92441504065829960, 4.694414232677499577, 8.017771632862299214 ) ) ;
#23122=ADVANCED_FACE ( 'NONE', ( #13570 ), #65805, .F. ) ;
#23132=CARTESIAN_POINT ( 'NONE',  ( 11.39700581613019992, 4.869652672166700391, 6.941573685175900010 ) ) ;
#23180=CARTESIAN_POINT ( 'NONE',  ( 10.72702344389999851, 2.995605560827999891, 8.109550315577399360 ) ) ;
#23184=CARTESIAN_POINT ( 'NONE',  ( 9.581038493598999395, 4.826346105011899645, 8.287963554181398962 ) ) ;
#23195=DIRECTION ( 'NONE',  ( -1.000000000000000000, 0.000000000000000000, 0.000000000000000000 ) ) ;
#23207=EDGE_CURVE ( 'NONE', #61459, #26174, #37847, .T. ) ;
#23227=ORIENTED_EDGE ( 'NONE', *, *, #7818, .F. ) ;
#23236=CARTESIAN_POINT ( 'NONE',  ( 9.077417874593999514, 3.075647715286899953, 7.107043063332000088 ) ) ;
#23243=CARTESIAN_POINT ( 'NONE',  ( 9.256734463322999318, 4.090312251411050148, 6.637705594503099604 ) ) ;
#23277=CARTESIAN_POINT ( 'NONE',  ( 10.77222057153667656, 4.304280767886410786, 6.680547245655227506 ) ) ;
#23370=CARTESIAN_POINT ( 'NONE',  ( 11.26072066707849828, 4.976067344118500380, 8.090408888831799317 ) ) ;
#23385=CARTESIAN_POINT ( 'NONE',  ( 9.002376473208927976, 3.077871436655788440, 6.792422036439461408 ) ) ;
#23403=CARTESIAN_POINT ( 'NONE',  ( 10.62072335273219892, 4.397090433355999473, 6.430603299050000388 ) ) ;
#23456=CARTESIAN_POINT ( 'NONE',  ( 10.53521345716899837, 4.924890298941200228, 6.659120737011199331 ) ) ;
#23468=CARTESIAN_POINT ( 'NONE',  ( 10.79718447801629999, 5.003225587801999552, 7.522119512433738997 ) ) ;
#23481=CARTESIAN_POINT ( 'NONE',  ( 11.11123293495519881, 3.108594079907299967, 7.535834283667469435 ) ) ;
#23526=CARTESIAN_POINT ( 'NONE',  ( 11.64633327354034797, 3.135095881599500256, 8.065722083251399610 ) ) ;
#23528=CARTESIAN_POINT ( 'NONE',  ( 9.226430433046999724, 3.028322657068899915, 8.099647887697699389 ) ) ;
#23561=CARTESIAN_POINT ( 'NONE',  ( 9.099999931440999390, 5.064317881551000156, 6.844464000216799349 ) ) ;
#23573=CARTESIAN_POINT ( 'NONE',  ( 10.06324205624999912, 3.590523439766200031, 6.434137271007999814 ) ) ;
#23582=CARTESIAN_POINT ( 'NONE',  ( 8.952784697134999803, 4.470490447737899942, 8.228249052908999772 ) ) ;
#23587=CARTESIAN_POINT ( 'NONE',  ( 8.763353253171903390, 3.867553254011502961, 6.586646690369097890 ) ) ;
#23620=CARTESIAN_POINT ( 'NONE',  ( 10.27195525820100031, 3.879327850572200198, 8.772302877803999976 ) ) ;
#23701=CARTESIAN_POINT ( 'NONE',  ( 10.26990035061499817, 4.231093494672100164, 6.664354444139199529 ) ) ;
#23711=CARTESIAN_POINT ( 'NONE',  ( 11.65456516821461008, 4.802916961510000249, 6.689681884064299311 ) ) ;
#23743=CARTESIAN_POINT ( 'NONE',  ( 11.67918044953561996, 5.011483761127000669, 6.972563939641199582 ) ) ;
#23772=CIRCLE ( 'NONE', #4788, 0.7499999936418002555 ) ;
#23799=CARTESIAN_POINT ( 'NONE',  ( 10.38528584683667866, 4.732620749361601931, 6.833918148925947733 ) ) ;
#23811=CARTESIAN_POINT ( 'NONE',  ( 10.64949279009019989, 3.739015461786900030, 6.531063508962500208 ) ) ;
#23872=CARTESIAN_POINT ( 'NONE',  ( 11.56833327354034857, 3.253412192327699959, 7.988332985010599963 ) ) ;
#23874=CARTESIAN_POINT ( 'NONE',  ( 9.629684229509999582, 3.291972602441000095, 8.212418068717900255 ) ) ;
#23924=CARTESIAN_POINT ( 'NONE',  ( 9.075405316139999456, 3.757578743663700038, 6.384219384258999597 ) ) ;
#23929=CARTESIAN_POINT ( 'NONE',  ( 9.915292290062998504, 4.749786674456300872, 7.935348007132199122 ) ) ;
#23932=CARTESIAN_POINT ( 'NONE',  ( 11.41486084871699802, 2.792989229543000107, 7.174999999999999822 ) ) ;
#23956=VERTEX_POINT ( 'NONE', #56089 ) ;
#23962=VERTEX_POINT ( 'NONE', #67595 ) ;
#23967=CARTESIAN_POINT ( 'NONE',  ( 10.34580110216399973, 2.909301855364999856, 8.166103548914600552 ) ) ;
#23984=CARTESIAN_POINT ( 'NONE',  ( 10.14887885159599890, 5.269014563305000287, 7.651388779553199626 ) ) ;
#24056=CARTESIAN_POINT ( 'NONE',  ( 10.96533729122639933, 2.859653469230999612, 7.529998433785960010 ) ) ;
#24067=ORIENTED_EDGE ( 'NONE', *, *, #1178, .T. ) ;
#24071=CARTESIAN_POINT ( 'NONE',  ( 9.048601287889788125, 4.000000467705929985, 6.301404677806389465 ) ) ;
#24082=CARTESIAN_POINT ( 'NONE',  ( 9.666846873516668381, 4.768183399968648040, 8.499583552997725278 ) ) ;
#24084=EDGE_CURVE ( 'NONE', #68576, #68176, #39374, .T. ) ;
#24091=CARTESIAN_POINT ( 'NONE',  ( 11.55610404293055993, 3.497163090439000310, 6.476063885290000322 ) ) ;
#24093=CARTESIAN_POINT ( 'NONE',  ( 10.70851354018270030, 4.163624617374472869, 8.749999999999996447 ) ) ;
#24106=EDGE_CURVE ( 'NONE', #24944, #68576, #7680, .T. ) ;
#24128=CARTESIAN_POINT ( 'NONE',  ( 10.09393020684899867, 5.250000000000000000, 7.500000000000000000 ) ) ;
#24156=CARTESIAN_POINT ( 'NONE',  ( 10.45257053952200010, 3.605640676136899980, 8.422730500489899796 ) ) ;
#24183=CARTESIAN_POINT ( 'NONE',  ( 10.02145237372899800, 4.043732047787757189, 6.225919055146348136 ) ) ;
#24201=CARTESIAN_POINT ( 'NONE',  ( 11.30565467195989093, 2.863826994586553099, 8.088082908809447247 ) ) ;
#24215=CARTESIAN_POINT ( 'NONE',  ( 8.897151519676997466, 4.024693162376980382, 6.358456126310000123 ) ) ;
#24266=CARTESIAN_POINT ( 'NONE',  ( 8.746126402770999064, 5.068373778467000434, 7.902879529556599891 ) ) ;
#24276=VERTEX_POINT ( 'NONE', #29810 ) ;
#24310=CARTESIAN_POINT ( 'NONE',  ( 10.96118313518939935, 3.207251432249800249, 6.497569908212999401 ) ) ;
#24386=ORIENTED_EDGE ( 'NONE', *, *, #24951, .T. ) ;
#24392=CARTESIAN_POINT ( 'NONE',  ( 10.09259632033899834, 3.197262364844699611, 7.827597670336898794 ) ) ;
#24397=CARTESIAN_POINT ( 'NONE',  ( 11.55300581613033906, 5.107584469683000172, 6.788791567531699656 ) ) ;
#24402=CARTESIAN_POINT ( 'NONE',  ( 11.38379707368349969, 3.433355370490100533, 8.490052513816499058 ) ) ;
#24420=CARTESIAN_POINT ( 'NONE',  ( 8.975960865537832234, 2.874039072694928088, 7.353476508004328061 ) ) ;
#24437=CARTESIAN_POINT ( 'NONE',  ( 10.17764828895399809, 5.001141961424000471, 6.953185708700699408 ) ) ;
#24496=B_SPLINE_CURVE_WITH_KNOTS ( 'NONE', 3,
 ( #23456, #44793, #23799, #56987 ),
 .UNSPECIFIED., .F., .F.,
 ( 4, 4 ),
 ( 0.000000000000000000, 1.000000000000000000 ),
 .UNSPECIFIED. ) ;
#24506=CARTESIAN_POINT ( 'NONE',  ( 11.51102763632551884, 3.088851714329700293, 7.920427941950599404 ) ) ;
#24518=CARTESIAN_POINT ( 'NONE',  ( 10.44635971519499940, 4.459622816450200311, 8.264615166761799969 ) ) ;
#24565=CARTESIAN_POINT ( 'NONE',  ( 11.44366954483529852, 4.485203148598100320, 8.248643701125299543 ) ) ;
#24567=CARTESIAN_POINT ( 'NONE',  ( 9.201101285863998669, 3.264788442324599860, 8.373612278672599274 ) ) ;
#24587=SHAPE_REPRESENTATION ( 'Terminal Screw 2', ( #9676 ), #38794 ) ;
#24614=CARTESIAN_POINT ( 'NONE',  ( 9.531329965421999617, 3.206942993865000258, 6.678540912152799436 ) ) ;
#24624=CARTESIAN_POINT ( 'NONE',  ( 11.60000000000000142, 3.254367469151916659, 6.836536274993708417 ) ) ;
#24654=CARTESIAN_POINT ( 'NONE',  ( 10.05041772631199848, 4.549624259497900169, 6.368647051112000135 ) ) ;
#24677=ORIENTED_EDGE ( 'NONE', *, *, #7571, .F. ) ;
#24685=AXIS2_PLACEMENT_3D ( 'NONE', #51549, #63750, #24983 ) ;
#24694=CARTESIAN_POINT ( 'NONE',  ( 11.59999999999999964, 4.000000000000000000, 7.500000000000000000 ) ) ;
#24707=VERTEX_POINT ( 'NONE', #16880 ) ;
#24729=CARTESIAN_POINT ( 'NONE',  ( 10.84657802013509986, 2.684088780794000151, 7.530633716161349689 ) ) ;
#24735=CARTESIAN_POINT ( 'NONE',  ( 10.29522949779699914, 4.480999174483200065, 6.778648208007999720 ) ) ;
#24739=CARTESIAN_POINT ( 'NONE',  ( 11.10612378248509913, 3.517039242046199998, 8.413720204863100349 ) ) ;
#24745=CARTESIAN_POINT ( 'NONE',  ( 10.23103300763299828, 4.692441239783899931, 6.773725604892799623 ) ) ;
#24773=CARTESIAN_POINT ( 'NONE',  ( 9.864763540183249191, 2.782534154164605589, 7.172815144550902744 ) ) ;
#24776=CARTESIAN_POINT ( 'NONE',  ( 11.15810538575740019, 5.242981041160000188, 7.797177576385699638 ) ) ;
#24819=CARTESIAN_POINT ( 'NONE',  ( 10.29184687351566652, 3.000416447002276943, 8.268183399968645375 ) ) ;
#24847=CARTESIAN_POINT ( 'NONE',  ( 11.33872066707849768, 4.858611803369300652, 8.019361746728900897 ) ) ;
#24861=CARTESIAN_POINT ( 'NONE',  ( 11.21979841651039855, 3.695024856201900132, 6.689266534545799558 ) ) ;
#24905=CARTESIAN_POINT ( 'NONE',  ( 10.23758376188599861, 3.152987476450699766, 6.960174024681499816 ) ) ;
#24944=VERTEX_POINT ( 'NONE', #38 ) ;
#24951=EDGE_CURVE ( 'NONE', #25295, #24276, #30913, .T. ) ;
#24953=CARTESIAN_POINT ( 'NONE',  ( 9.657975701332999208, 4.837683410033799980, 6.724099908144899551 ) ) ;
#24961=CARTESIAN_POINT ( 'NONE',  ( 11.43028911132391556, 2.855999340945334808, 6.940988051967042161 ) ) ;
#24970=ORIENTED_EDGE ( 'NONE', *, *, #38370, .F. ) ;
#24983=DIRECTION ( 'NONE',  ( 0.000000000000000000, -1.000000000000000000, 0.000000000000000000 ) ) ;
#25044=ORIENTED_EDGE ( 'NONE', *, *, #6125, .F. ) ;
#25053=ORIENTED_EDGE ( 'NONE', *, *, #41784, .T. ) ;
#25071=CARTESIAN_POINT ( 'NONE',  ( 9.048601287889788125, 4.000000467705929985, 6.301404677806389465 ) ) ;
#25077=CARTESIAN_POINT ( 'NONE',  ( 10.80502344389999791, 2.874741265256000489, 8.182900850620900002 ) ) ;
#25083=CARTESIAN_POINT ( 'NONE',  ( 10.83810672858429847, 2.978701842912999886, 8.268288002587098617 ) ) ;
#25100=ORIENTED_EDGE ( 'NONE', *, *, #5054, .F. ) ;
#25116=CARTESIAN_POINT ( 'NONE',  ( 10.42380110216399913, 3.026453990125600235, 8.094557215852098864 ) ) ;
#25137=EDGE_CURVE ( 'NONE', #19063, #45676, #41802, .T. ) ;
#25148=B_SPLINE_CURVE_WITH_KNOTS ( 'NONE', 3,
 ( #50852, #34782, #23587, #55411 ),
 .UNSPECIFIED., .F., .F.,
 ( 4, 4 ),
 ( 0.000000000000000000, 0.8163836489557156906 ),
 .UNSPECIFIED. ) ;
#25169=CARTESIAN_POINT ( 'NONE',  ( 11.36749010443639918, 4.863785690678500195, 7.435402237490909449 ) ) ;
#25186=CARTESIAN_POINT ( 'NONE',  ( 11.28533594839949750, 4.750012929834699804, 8.359517726022600570 ) ) ;
#25200=CARTESIAN_POINT ( 'NONE',  ( 11.83518044953559922, 4.768048975940600620, 7.099502491684900107 ) ) ;
#25243=CARTESIAN_POINT ( 'NONE',  ( 10.73724174883999893, 3.975468761016990094, 6.608211443991299561 ) ) ;
#25245=CARTESIAN_POINT ( 'NONE',  ( 10.33688779216199904, 4.801941500727100021, 7.210800365544999480 ) ) ;
#25270=B_SPLINE_CURVE_WITH_KNOTS ( 'NONE', 3,
 ( #67840, #19961, #10154, #31482, #57015, #31830, #26238, #53146, #5247, #26586, #36032, #17107, #64654, #59415, #32514, #37408, #26927, #28300 ),
 .UNSPECIFIED., .F., .F.,
 ( 4, 2, 2, 2, 2, 2, 2, 2, 4 ),
 ( 0.000000000000000000, 0.1250000000000000000, 0.2500000000000000000, 0.3750000000000000000, 0.5000000000000000000, 0.6250000000000000000, 0.7500000000000000000, 0.8750000000000000000, 1.000000000000000000 ),
 .UNSPECIFIED. ) ;
#25283=CARTESIAN_POINT ( 'NONE',  ( 10.80502344389999791, 2.874741265256000489, 8.182900850620900002 ) ) ;
#25294=SURFACE_SIDE_STYLE ('',( #46283 ) ) ;
#25295=VERTEX_POINT ( 'NONE', #34044 ) ;
#25296=CARTESIAN_POINT ( 'NONE',  ( 9.807938025973999885, 3.334935831489500124, 8.592736948783000983 ) ) ;
#25301=ORIENTED_EDGE ( 'NONE', *, *, #55846, .F. ) ;
#25302=CARTESIAN_POINT ( 'NONE',  ( 11.49200216175158396, 3.580169417146517485, 6.297929225185963098 ) ) ;
#25323=ORIENTED_EDGE ( 'NONE', *, *, #18148, .T. ) ;
#25326=CARTESIAN_POINT ( 'NONE',  ( 10.52022949779799887, 4.709679768527199606, 6.435697190503999465 ) ) ;
#25374=CARTESIAN_POINT ( 'NONE',  ( 11.02319144466311052, 5.119973997747526262, 7.175010281093781472 ) ) ;
#25385=VERTEX_POINT ( 'NONE', #39976 ) ;
#25411=CARTESIAN_POINT ( 'NONE',  ( 11.59456039236534330, 5.314711678001000195, 7.436015812896529020 ) ) ;
#25420=ADVANCED_FACE ( 'NONE', ( #55357 ), #49764, .T. ) ;
#25422=CARTESIAN_POINT ( 'NONE',  ( 10.97635090131019986, 4.999207052587699707, 6.881982988766500497 ) ) ;
#25428=CARTESIAN_POINT ( 'NONE',  ( 11.37964291764649971, 2.731641218595000087, 7.656787697937099679 ) ) ;
#25457=CARTESIAN_POINT ( 'NONE',  ( 11.33041235500449950, 3.057642534728299832, 8.363295307663500822 ) ) ;
#25465=CARTESIAN_POINT ( 'NONE',  ( 11.37299956498129916, 2.792989229543000107, 7.825000000000000178 ) ) ;
#25518=CARTESIAN_POINT ( 'NONE',  ( 11.31825954179440075, 4.666231193203100425, 6.946434658287599540 ) ) ;
#25521=ORIENTED_EDGE ( 'NONE', *, *, #11924, .T. ) ;
#25531=CARTESIAN_POINT ( 'NONE',  ( 11.39975833414730033, 4.796537143354000499, 7.825000000000000178 ) ) ;
#25534=CARTESIAN_POINT ( 'NONE',  ( 10.89149144726329865, 3.340422662105400065, 8.430724369296298093 ) ) ;
#25549=CARTESIAN_POINT ( 'NONE',  ( 10.65364694612719809, 3.195501139158400061, 7.178938988280099132 ) ) ;
#25581=CARTESIAN_POINT ( 'NONE',  ( 11.14955063476181962, 4.976598135215293262, 8.326430086672807818 ) ) ;
#25597=CARTESIAN_POINT ( 'NONE',  ( 9.475696787962998968, 4.148886440911999429, 8.354131589521699652 ) ) ;
#25628=CARTESIAN_POINT ( 'NONE',  ( 11.22056920625029974, 4.047312782235129802, 8.815417147437999645 ) ) ;
#25630=CARTESIAN_POINT ( 'NONE',  ( 11.59999999999999964, 5.064318446328999634, 6.844464917182299324 ) ) ;
#25641=CARTESIAN_POINT ( 'NONE',  ( 8.516151519676999015, 4.027664626136379766, 6.221087886525999089 ) ) ;
#25725=DIRECTION ( 'NONE',  ( 0.000000000000000000, 0.8514547570628039352, -0.5244280662542016858 ) ) ;
#25761=ORIENTED_EDGE ( 'NONE', *, *, #47772, .F. ) ;
#25768=CARTESIAN_POINT ( 'NONE',  ( 11.01790547754519878, 5.174295865741999734, 7.462730980357120458 ) ) ;
#25774=CARTESIAN_POINT ( 'NONE',  ( 11.45348876160960039, 3.114179898019400206, 6.578783887955899523 ) ) ;
#25778=CARTESIAN_POINT ( 'NONE',  ( 8.737760194560385330, 3.933854210954582431, 6.629534018758290514 ) ) ;
#25857=CARTESIAN_POINT ( 'NONE',  ( 11.44133594839949986, 4.569506585117100173, 8.152656755002400502 ) ) ;
#25872=CARTESIAN_POINT ( 'NONE',  ( 10.54687750876899877, 3.382085645339300228, 6.541108991297599928 ) ) ;
#25890=CARTESIAN_POINT ( 'NONE',  ( 11.66287348028854964, 3.238044298475899918, 7.088026579158399620 ) ) ;
#25902=CARTESIAN_POINT ( 'NONE',  ( 10.98937577273788868, 3.538822733277925181, 6.300114087089553117 ) ) ;
#25938=CARTESIAN_POINT ( 'NONE',  ( 9.199088727410998700, 2.999102593977000186, 7.416055476975279781 ) ) ;
#25972=CARTESIAN_POINT ( 'NONE',  ( 11.01279632507519857, 4.624908853805600906, 6.341531314375999706 ) ) ;
#25997=CARTESIAN_POINT ( 'NONE',  ( 8.923129650240840149, 3.341122914829670609, 8.358757503607597172 ) ) ;
#26018=CARTESIAN_POINT ( 'NONE',  ( 10.16562143724499911, 4.849675135054999586, 8.456261759323901117 ) ) ;
#26114=CARTESIAN_POINT ( 'NONE',  ( 11.68277869730536977, 3.468607053297499743, 8.547856079839998955 ) ) ;
#26119=CARTESIAN_POINT ( 'NONE',  ( 10.51810807141099779, 4.059045408506610109, 6.223352037434000117 ) ) ;
#26158=CARTESIAN_POINT ( 'NONE',  ( 10.66476354018302608, 5.217465845835396188, 7.827184855449094592 ) ) ;
#26174=VERTEX_POINT ( 'NONE', #38953 ) ;
#26209=CARTESIAN_POINT ( 'NONE',  ( 10.72749279009019929, 3.774717370312400178, 6.663611138821799784 ) ) ;
#26225=CARTESIAN_POINT ( 'NONE',  ( 10.47303166480599934, 2.862083839376000416, 7.419769534118209720 ) ) ;
#26238=CARTESIAN_POINT ( 'NONE',  ( 9.427263540183332680, 3.370476274536375438, 6.407767014557179230 ) ) ;
#26241=CARTESIAN_POINT ( 'NONE',  ( 11.51518179236248862, 3.819003318705799899, 8.347076615013298451 ) ) ;
#26253=CARTESIAN_POINT ( 'NONE',  ( 11.40221299665285670, 4.908904393308908709, 7.175011619880304004 ) ) ;
#26288=CARTESIAN_POINT ( 'NONE',  ( 9.173759580228997734, 3.023107159668900312, 7.733500918284399894 ) ) ;
#26308=CARTESIAN_POINT ( 'NONE',  ( 11.59999999999999964, 3.182579051151299687, 7.825000000000000178 ) ) ;
#26318=CARTESIAN_POINT ( 'NONE',  ( 11.68277869730536977, 3.468607053297499743, 8.547856079839998955 ) ) ;
#26335=CARTESIAN_POINT ( 'NONE',  ( 9.301355082327999568, 3.427502311996299955, 8.643954013369999245 ) ) ;
#26367=CARTESIAN_POINT ( 'NONE',  ( 9.988317406969001055, 4.237919115995800290, 6.243107450209000042 ) ) ;
#26416=ORIENTED_EDGE ( 'NONE', *, *, #60222, .F. ) ;
#26420=AXIS2_PLACEMENT_3D ( 'NONE', #26484, #68080, #4796 ) ;
#26462=CARTESIAN_POINT ( 'NONE',  ( 10.32169598648999909, 4.766524664146899681, 7.043598424555200133 ) ) ;
#26467=CARTESIAN_POINT ( 'NONE',  ( 11.61759063708296047, 5.217265640542000149, 7.157757529645699890 ) ) ;
#26484=CARTESIAN_POINT ( 'NONE',  ( 11.59999999999999964, 4.000000000000000000, 7.500000000000000000 ) ) ;
#26497=ORIENTED_EDGE ( 'NONE', *, *, #57915, .F. ) ;
#26515=COLOUR_RGB ( '', 0.66274510, 0.83137255, 0.94901961) ;
#26546=DIRECTION ( 'NONE',  ( 1.000000000000000000, 0.000000000000000000, 0.000000000000000000 ) ) ;
#26555=CARTESIAN_POINT ( 'NONE',  ( 11.66287348028854964, 3.238044298475899918, 7.088026579158399620 ) ) ;
#26572=CARTESIAN_POINT ( 'NONE',  ( 10.64533863405319991, 4.703785194191100416, 6.602238051205399749 ) ) ;
#26586=CARTESIAN_POINT ( 'NONE',  ( 9.479346873516668381, 4.163624617374466652, 6.249999999999999112 ) ) ;
#26587=CARTESIAN_POINT ( 'NONE',  ( 11.48641235500450009, 3.260080192309100067, 8.177841818594698609 ) ) ;
#26638=CARTESIAN_POINT ( 'NONE',  ( 9.047113844317999920, 4.253652595614200393, 8.471855267550699509 ) ) ;
#26660=APPLICATION_CONTEXT ( 'automotive_design' ) ;
#26661=VERTEX_POINT ( 'NONE', #67830 ) ;
#26668=CARTESIAN_POINT ( 'NONE',  ( 11.63611496860034933, 5.171412538012999605, 8.100294210499798808 ) ) ;
#26684=CARTESIAN_POINT ( 'NONE',  ( 9.124051052051999733, 5.255397705012999410, 7.254315263553399618 ) ) ;
#26690=VERTEX_POINT ( 'NONE', #13681 ) ;
#26693=CARTESIAN_POINT ( 'NONE',  ( 10.24006601915162484, 3.957587222814286321, 6.626081523287773223 ) ) ;
#26716=CARTESIAN_POINT ( 'NONE',  ( 9.684367640780997988, 4.603017491986999943, 8.628164124510998789 ) ) ;
#26739=AXIS2_PLACEMENT_3D ( 'NONE', #47712, #63074, #42461 ) ;
#26807=DIRECTION ( 'NONE',  ( 0.000000000000000000, 1.000000000000000000, 0.000000000000000000 ) ) ;
#26811=CARTESIAN_POINT ( 'NONE',  ( 10.98656920625009903, 4.032067152264009913, 8.391549386185598536 ) ) ;
#26824=EDGE_LOOP ( 'NONE', ( #19763, #11447, #44253, #59244, #15272, #28133 ) ) ;
#26900=CARTESIAN_POINT ( 'NONE',  ( 10.62487750876920067, 3.456442671114800191, 6.656497609330299881 ) ) ;
#26913=CARTESIAN_POINT ( 'NONE',  ( 11.45348876160960039, 3.114179898019400206, 6.578783887955899523 ) ) ;
#26927=CARTESIAN_POINT ( 'NONE',  ( 9.583513540183334456, 5.250000000000000888, 7.336375382625531572 ) ) ;
#26928=CARTESIAN_POINT ( 'NONE',  ( 11.58487348028854846, 3.117292544139400157, 7.022738645480499642 ) ) ;
#26940=CARTESIAN_POINT ( 'NONE',  ( 10.91301932002725650, 2.749999999999998224, 7.200148911387370454 ) ) ;
#26973=CARTESIAN_POINT ( 'NONE',  ( 10.19601354018254291, 4.999583552997727054, 8.268183399968641822 ) ) ;
#26980=CARTESIAN_POINT ( 'NONE',  ( 10.99999970531878013, 2.901368254139102376, 7.402706825368051469 ) ) ;
#26988=CARTESIAN_POINT ( 'NONE',  ( 11.46595122972049907, 4.343798595649099425, 8.295047870239098842 ) ) ;
#27005=CARTESIAN_POINT ( 'NONE',  ( 11.23078751119019891, 3.084247107206000038, 7.020904658857499925 ) ) ;
#27043=DIRECTION ( 'NONE',  ( 0.000000000000000000, 1.000000000000000000, 0.000000000000000000 ) ) ;
#27054=CARTESIAN_POINT ( 'NONE',  ( 11.26212378248529866, 3.384904051819500381, 8.663708617168998316 ) ) ;
#27058=CARTESIAN_POINT ( 'NONE',  ( 10.46755864497999866, 4.898932057185599653, 6.795973491698399371 ) ) ;
#27092=EDGE_LOOP ( 'NONE', ( #37629, #36534, #58264, #1824 ) ) ;
#27099=CARTESIAN_POINT ( 'NONE',  ( 11.60000000000000142, 4.072982449166800301, 8.552611010855414975 ) ) ;
#27112=CARTESIAN_POINT ( 'NONE',  ( 11.30361999289329766, 3.455907502640805262, 8.657883396625690509 ) ) ;
#27189=DIRECTION ( 'NONE',  ( 1.000000000000000000, 0.000000000000000000, -0.000000000000000000 ) ) ;
#27239=CARTESIAN_POINT ( 'NONE',  ( 10.50180110216399854, 3.143606124884799957, 8.023010882787499298 ) ) ;
#27254=CARTESIAN_POINT ( 'NONE',  ( 10.44426222744799837, 3.013556901740999994, 6.687444528363699625 ) ) ;
#27269=CARTESIAN_POINT ( 'NONE',  ( 11.28949010443639978, 5.000675062740000065, 7.425165037173959703 ) ) ;
#27331=CARTESIAN_POINT ( 'NONE',  ( 11.71210404293059959, 3.618181340822599790, 6.722495590581700320 ) ) ;
#27347=CARTESIAN_POINT ( 'NONE',  ( 10.51925056272499859, 5.174767082365999471, 7.482589369563879877 ) ) ;
#27374=CARTESIAN_POINT ( 'NONE',  ( 10.11342028323962694, 3.127145521393861038, 7.560475846972328995 ) ) ;
#27394=CARTESIAN_POINT ( 'NONE',  ( 11.31389666366019853, 3.954123449088899900, 6.467512203247999913 ) ) ;
#27396=CARTESIAN_POINT ( 'NONE',  ( 9.025809814041000578, 4.782507962695600412, 6.488038963273999649 ) ) ;
#27402=EDGE_CURVE ( 'NONE', #43200, #50051, #12722, .T. ) ;
#27440=CARTESIAN_POINT ( 'NONE',  ( 11.60000000000000497, 3.359735910920771396, 8.191831084107850103 ) ) ;
#27446=CARTESIAN_POINT ( 'NONE',  ( 9.685317406968998455, 4.186809223719299311, 6.513113677132300161 ) ) ;
#27492=CARTESIAN_POINT ( 'NONE',  ( 11.23589666366019912, 3.960399224793059947, 6.608753462694600067 ) ) ;
#27537=CARTESIAN_POINT ( 'NONE',  ( 10.35987047770899672, 2.749999999999999556, 7.249610810850630749 ) ) ;
#27549=ORIENTED_EDGE ( 'NONE', *, *, #66932, .F. ) ;
#27582=CARTESIAN_POINT ( 'NONE',  ( 10.74795391537419853, 4.830118059977199785, 6.936213817702099327 ) ) ;
#27596=CARTESIAN_POINT ( 'NONE',  ( 11.05964426047339799, 4.687693494822500639, 6.422784126663999338 ) ) ;
#27611=CARTESIAN_POINT ( 'NONE',  ( 11.63410404293056999, 3.557672215630899970, 6.599279737936000423 ) ) ;
#27624=EDGE_CURVE ( 'NONE', #26174, #10742, #7771, .T. ) ;
#27636=CIRCLE ( 'NONE', #29899, 1.250000000000000444 ) ;
#27667=CARTESIAN_POINT ( 'NONE',  ( 8.969113844317998741, 4.218953675027299788, 8.338908357746399602 ) ) ;
#27682=CARTESIAN_POINT ( 'NONE',  ( 10.80133863405319872, 4.534404523786000674, 6.818303296693398963 ) ) ;
#27683=VECTOR ( 'NONE', #7306, 1000.000000000000000 ) ;
#27698=CARTESIAN_POINT ( 'NONE',  ( 11.60988784977536348, 3.148894096305599799, 7.548634759728509280 ) ) ;
#27714=( NAMED_UNIT ( * ) PLANE_ANGLE_UNIT ( ) SI_UNIT ( $, .RADIAN. ) );
#27750=CARTESIAN_POINT ( 'NONE',  ( 11.39189666366029918, 3.947847673382490541, 6.326270943800999191 ) ) ;
#27752=CARTESIAN_POINT ( 'NONE',  ( 10.44222949779799947, 4.633452903845899584, 6.550014196338999284 ) ) ;
#27759=DIRECTION ( 'NONE',  ( -1.000000000000000000, 0.000000000000000000, 0.000000000000000000 ) ) ;
#27762=FACE_OUTER_BOUND ( 'NONE', #66171, .T. ) ;
#27771=EDGE_LOOP ( 'NONE', ( #59787, #39118, #9673, #14827 ) ) ;
#27775=CARTESIAN_POINT ( 'NONE',  ( 8.751496707488000126, 4.081676005979390176, 6.643597378104299622 ) ) ;
#27792=ORIENTED_EDGE ( 'NONE', *, *, #7571, .T. ) ;
#27803=CARTESIAN_POINT ( 'NONE',  ( 9.052088727410998459, 2.999102593977000186, 7.416055476975279781 ) ) ;
#27809=CARTESIAN_POINT ( 'NONE',  ( 9.813975701332999790, 4.636077325177999420, 6.910836541441499392 ) ) ;
#27821=DIRECTION ( 'NONE',  ( -1.000000000000000000, 0.000000000000000000, 0.000000000000000000 ) ) ;
#27847=CARTESIAN_POINT ( 'NONE',  ( 10.65413259636999932, 3.216622244594500302, 7.073141822156699732 ) ) ;
#27930=EDGE_CURVE ( 'NONE', #24707, #66054, #10495, .T. ) ;
#27933=CARTESIAN_POINT ( 'NONE',  ( 11.60948876160955479, 3.304472173606900043, 6.776679950459500112 ) ) ;
#27948=CARTESIAN_POINT ( 'NONE',  ( 10.96118313518939935, 3.207251432249800249, 6.497569908212999401 ) ) ;
#27964=CARTESIAN_POINT ( 'NONE',  ( 10.30903300763299946, 4.597717337857299746, 6.873077781830399857 ) ) ;
#27992=CARTESIAN_POINT ( 'NONE',  ( 9.099999931440999390, 5.246365646610000155, 7.595250590283559866 ) ) ;
#28002=CARTESIAN_POINT ( 'NONE',  ( 11.59999999999999964, 3.116215992411100366, 7.174999999999999822 ) ) ;
#28027=AXIS2_PLACEMENT_3D ( 'NONE', #10848, #10168, #361 ) ;
#28030=CARTESIAN_POINT ( 'NONE',  ( 11.66287348028854964, 3.238044298475899918, 7.088026579158399620 ) ) ;
#28042=CARTESIAN_POINT ( 'NONE',  ( 11.31900581613029821, 4.750686773407899466, 7.017964743997199939 ) ) ;
#28087=CARTESIAN_POINT ( 'NONE',  ( 10.37199293566600034, 4.633387186021100668, 6.723009541442299231 ) ) ;
#28089=CARTESIAN_POINT ( 'NONE',  ( 10.39157120343299923, 3.944651031655580287, 6.359530327585999565 ) ) ;
#28133=ORIENTED_EDGE ( 'NONE', *, *, #55169, .T. ) ;
#28138=CARTESIAN_POINT ( 'NONE',  ( 9.710646554150999421, 4.486270025758400060, 6.621146336197599958 ) ) ;
#28140=AXIS2_PLACEMENT_3D ( 'NONE', #24694, #46017, #55479 ) ;
#28141=CARTESIAN_POINT ( 'NONE',  ( 9.591846873515667227, 4.999583552997727054, 6.731816600031356401 ) ) ;
#28145=CARTESIAN_POINT ( 'NONE',  ( 10.14124205625000030, 3.639798001706899822, 6.562398383267799673 ) ) ;
#28227=CARTESIAN_POINT ( 'NONE',  ( 10.50333291544900050, 4.531093146757585899, 6.341063066638221279 ) ) ;
#28271=CARTESIAN_POINT ( 'NONE',  ( 11.63410404293056999, 3.557672215630899970, 6.599279737936000423 ) ) ;
#28300=CARTESIAN_POINT ( 'NONE',  ( 9.593930206849998754, 5.250000000000000000, 7.500000000000000000 ) ) ;
#28301=CARTESIAN_POINT ( 'NONE',  ( 11.23610538575739959, 5.109472165990999848, 7.765257665594799796 ) ) ;
#28315=CARTESIAN_POINT ( 'NONE',  ( 11.00000000000000000, 4.991767524623399233, 7.825000000000000178 ) ) ;
#28330=CARTESIAN_POINT ( 'NONE',  ( 9.293111399473126255, 2.988705873519680090, 8.251846359484561688 ) ) ;
#28345=CARTESIAN_POINT ( 'NONE',  ( 11.14975833414749928, 3.203462856645999945, 7.174999999999999822 ) ) ;
#28375=CARTESIAN_POINT ( 'NONE',  ( 10.97364560330029981, 4.265439025801100570, 8.324524538096799375 ) ) ;
#28389=CARTESIAN_POINT ( 'NONE',  ( 11.19434208742519843, 3.521141233577200325, 6.747282993577999655 ) ) ;
#28404=CARTESIAN_POINT ( 'NONE',  ( 11.16486084871730000, 5.207010770456999893, 7.825000000000000178 ) ) ;
#28439=CARTESIAN_POINT ( 'NONE',  ( 11.60477869730532774, 3.532552483170099844, 8.421761806503198500 ) ) ;
#28441=CARTESIAN_POINT ( 'NONE',  ( 8.975151519677000422, 4.027664626136379766, 6.221087886525999089 ) ) ;
#28488=CARTESIAN_POINT ( 'NONE',  ( 9.153405316139998860, 3.786750623988900166, 6.518487389810699639 ) ) ;
#28491=CARTESIAN_POINT ( 'NONE',  ( 9.602263540182329749, 5.092232985442822546, 6.870476274536374106 ) ) ;
#28496=CARTESIAN_POINT ( 'NONE',  ( 9.763317406968999634, 4.161254277581000416, 6.648116790593900483 ) ) ;
#28536=CARTESIAN_POINT ( 'NONE',  ( 10.81349144726329925, 3.261052100888700345, 8.542723541016000510 ) ) ;
#28585=EDGE_LOOP ( 'NONE', ( #8393, #14146, #48748, #62548 ) ) ;
#28626=CARTESIAN_POINT ( 'NONE',  ( 11.28533594839949750, 4.750012929834699804, 8.359517726022600570 ) ) ;
#28658=CARTESIAN_POINT ( 'NONE',  ( 10.28026357027499849, 4.985299147223100746, 7.309904858193100097 ) ) ;
#28710=CARTESIAN_POINT ( 'NONE',  ( 9.893930206848997599, 2.750000000000000000, 7.500000000000000000 ) ) ;
#28725=CARTESIAN_POINT ( 'NONE',  ( 11.48641235500450009, 3.260080192309100067, 8.177841818594698609 ) ) ;
#28793=CARTESIAN_POINT ( 'NONE',  ( 11.27234208742519783, 3.445253572379500362, 6.627995351445298944 ) ) ;
#28795=CARTESIAN_POINT ( 'NONE',  ( 8.871822372493998188, 3.671800173070400408, 6.426348619097999482 ) ) ;
#28847=CARTESIAN_POINT ( 'NONE',  ( 9.280051052051998539, 4.985712601322500603, 7.307093369932900373 ) ) ;
#28849=CARTESIAN_POINT ( 'NONE',  ( 9.446013540182333301, 3.000416447002273834, 6.731816600031359066 ) ) ;
#28853=CARTESIAN_POINT ( 'NONE',  ( 9.358051052051999719, 4.850870049477099322, 7.333482423122699601 ) ) ;
#28979=CARTESIAN_POINT ( 'NONE',  ( 10.20641772631199906, 4.431553727090300043, 6.611684804099500212 ) ) ;
#29014=CARTESIAN_POINT ( 'NONE',  ( 10.55103166480599874, 2.999015536536000504, 7.429424106427209296 ) ) ;
#29016=CARTESIAN_POINT ( 'NONE',  ( 10.76059687351619765, 3.370476274536378547, 8.592232985442823434 ) ) ;
#29033=FACE_OUTER_BOUND ( 'NONE', #43124, .T. ) ;
#29076=CARTESIAN_POINT ( 'NONE',  ( 11.43718179236249988, 3.790319673775199849, 8.481317998227099864 ) ) ;
#29108=CARTESIAN_POINT ( 'NONE',  ( 9.154341692891298621, 5.250000716804954948, 7.663628708442515425 ) ) ;
#29135=CARTESIAN_POINT ( 'NONE',  ( 11.60988784977536348, 3.148894096305599799, 7.548634759728509280 ) ) ;
#29137=CARTESIAN_POINT ( 'NONE',  ( 9.277088727410998104, 2.862182806015999947, 7.404572115919599185 ) ) ;
#29148=CARTESIAN_POINT ( 'NONE',  ( 10.27195525820100031, 3.879327850572200198, 8.772302877803999976 ) ) ;
#29183=CARTESIAN_POINT ( 'NONE',  ( 9.151392757686998891, 4.770706668257700400, 6.657535947657399866 ) ) ;
#29189=CARTESIAN_POINT ( 'NONE',  ( 10.21722949779699974, 4.557226039164599563, 6.664331202173499946 ) ) ;
#29192=CARTESIAN_POINT ( 'NONE',  ( 11.56914347478616634, 4.748726180097643912, 6.470125748842363578 ) ) ;
#29223=CARTESIAN_POINT ( 'NONE',  ( 10.89529697814178100, 4.826567894363762434, 7.784385510031588851 ) ) ;
#29246=CARTESIAN_POINT ( 'NONE',  ( 11.60118044953561878, 5.133201153721000054, 6.909094663619399945 ) ) ;
#29259=CARTESIAN_POINT ( 'NONE',  ( 10.14393020684899938, 5.250000000000000000, 7.500000000000000000 ) ) ;
#29262=DIRECTION ( 'NONE',  ( 1.000000000000000000, 0.000000000000000000, 0.000000000000000000 ) ) ;
#29264=CARTESIAN_POINT ( 'NONE',  ( 11.59999999999999964, 5.250000000000000000, 7.500000000000000000 ) ) ;
#29288=ADVANCED_FACE ( 'NONE', ( #3427 ), #35607, .T. ) ;
#29308=CARTESIAN_POINT ( 'NONE',  ( 10.19391290906799874, 3.451408805716100314, 6.828616613600999585 ) ) ;
#29317=CARTESIAN_POINT ( 'NONE',  ( 11.43302763632549990, 2.964209339073000216, 7.977941233841399971 ) ) ;
#29353=CARTESIAN_POINT ( 'NONE',  ( 11.18687482311539938, 5.057677595549000316, 7.072673169413499217 ) ) ;
#29383=PRODUCT_DEFINITION_SHAPE ( 'NONE', 'NONE',  #46633 ) ;
#29424=CARTESIAN_POINT ( 'NONE',  ( 11.68333460557258796, 4.162011815820000571, 6.509695444280099608 ) ) ;
#29469=CARTESIAN_POINT ( 'NONE',  ( 8.973608660036624940, 4.220957842099207546, 8.346587208109317757 ) ) ;
#29472=CARTESIAN_POINT ( 'NONE',  ( 10.55478570706233299, 5.131706358131709500, 6.886599490775120458 ) ) ;
#29490=CARTESIAN_POINT ( 'NONE',  ( 10.65413259636999932, 3.216622244594500302, 7.073141822156699732 ) ) ;
#29492=CARTESIAN_POINT ( 'NONE',  ( 9.680342523874998051, 3.007153757386999526, 7.651982363644999730 ) ) ;
#29539=CARTESIAN_POINT ( 'NONE',  ( 8.822113844317998499, 4.288351516201100111, 8.604802177355001191 ) ) ;
#29580=CARTESIAN_POINT ( 'NONE',  ( 10.44426222744799837, 3.013556901740999994, 6.687444528363699625 ) ) ;
#29639=CARTESIAN_POINT ( 'NONE',  ( 11.59999999999999964, 4.000000000000000000, 7.500000000000000000 ) ) ;
#29660=CARTESIAN_POINT ( 'NONE',  ( 10.16858376188599955, 3.268856270222099791, 7.034020612385399218 ) ) ;
#29670=CARTESIAN_POINT ( 'NONE',  ( 10.47303166480599934, 2.862083839376000416, 7.419769534118209720 ) ) ;
#29704=CARTESIAN_POINT ( 'NONE',  ( 10.52641638348499953, 3.025038519517300184, 7.737488872214999702 ) ) ;
#29768=CARTESIAN_POINT ( 'NONE',  ( 11.14179841651039915, 3.646693590264900031, 6.560784671286499226 ) ) ;
#29810=CARTESIAN_POINT ( 'NONE',  ( 8.710288521113000115, 3.647046440108700160, 6.715449042252499723 ) ) ;
#29830=CARTESIAN_POINT ( 'NONE',  ( 11.40211496860029783, 4.793947479907100018, 7.906860999147899527 ) ) ;
#29833=CARTESIAN_POINT ( 'NONE',  ( 10.26291290906799958, 3.364470222553300083, 6.722218404915299317 ) ) ;
#29881=CARTESIAN_POINT ( 'NONE',  ( 9.581988259785999773, 3.850604015305000072, 6.368003848175999515 ) ) ;
#29889=CARTESIAN_POINT ( 'NONE',  ( 11.59999999999999964, 3.528833218773708591, 6.561154158729442187 ) ) ;
#29899=AXIS2_PLACEMENT_3D ( 'NONE', #55138, #7585, #25725 ) ;
#29918=CARTESIAN_POINT ( 'NONE',  ( 10.41964694612699915, 2.813019656517000477, 7.026297514493899499 ) ) ;
#29956=CARTESIAN_POINT ( 'NONE',  ( 11.60000000000000142, 4.363617849674655602, 8.530211724564095377 ) ) ;
#29959=CARTESIAN_POINT ( 'NONE',  ( 9.664763540182335078, 5.217465845835396188, 7.827184855449094592 ) ) ;
#30006=CARTESIAN_POINT ( 'NONE',  ( 10.72191429142990060, 4.025072603369280522, 8.816028813488999916 ) ) ;
#30012=CARTESIAN_POINT ( 'NONE',  ( 10.98995257254739855, 2.904643075091000171, 7.181435527216799564 ) ) ;
#30038=CARTESIAN_POINT ( 'NONE',  ( 9.593930206849998754, 5.250000000000000000, 7.500000000000000000 ) ) ;
#30044=CARTESIAN_POINT ( 'NONE',  ( 11.23195122972050086, 4.507250159094099651, 8.673036084990000560 ) ) ;
#30051=CARTESIAN_POINT ( 'NONE',  ( 11.59999999999999964, 4.000000000000000000, 7.500000000000000000 ) ) ;
#30084=CARTESIAN_POINT ( 'NONE',  ( 10.20851354018233437, 4.163624617374472869, 8.749999999999996447 ) ) ;
#30111=CARTESIAN_POINT ( 'NONE',  ( 10.94487616594229884, 3.696562859151900415, 8.456491899811199531 ) ) ;
#30126=CARTESIAN_POINT ( 'NONE',  ( 10.85056919669530018, 4.830699382454300306, 7.254567470917099747 ) ) ;
#30138=CARTESIAN_POINT ( 'NONE',  ( 8.856495485442710702, 4.349453410998743941, 6.546761994161411913 ) ) ;
#30168=CARTESIAN_POINT ( 'NONE',  ( 10.57102344389999971, 3.237334151971200225, 7.962849245488699879 ) ) ;
#30170=CARTESIAN_POINT ( 'NONE',  ( 9.882975701332998852, 4.736880367605800224, 6.817468224793199916 ) ) ;
#30213=CARTESIAN_POINT ( 'NONE',  ( 9.328696787962998727, 4.196076320588900010, 8.624850445389000697 ) ) ;
#30220=CARTESIAN_POINT ( 'NONE',  ( 11.47657389914466464, 3.351225026288215947, 6.404407512144050685 ) ) ;
#30255=CARTESIAN_POINT ( 'NONE',  ( 11.14975833414749928, 3.203462856645999945, 7.174999999999999822 ) ) ;
#30290=CARTESIAN_POINT ( 'NONE',  ( 11.59999999999999787, 5.087332147730433185, 8.017651347927678529 ) ) ;
#30315=EDGE_CURVE ( 'NONE', #19590, #66054, #25270, .T. ) ;
#30327=CARTESIAN_POINT ( 'NONE',  ( 11.76588784977539781, 2.879134238109999799, 7.564049652083489228 ) ) ;
#30334=CARTESIAN_POINT ( 'NONE',  ( 10.32055864497999842, 4.682585200569199912, 6.965412239408199646 ) ) ;
#30338=CARTESIAN_POINT ( 'NONE',  ( 10.51925056272499859, 5.174767082365999471, 7.482589369563879877 ) ) ;
#30344=CARTESIAN_POINT ( 'NONE',  ( 11.40425819896749893, 2.744109752373000255, 7.263238376356399684 ) ) ;
#30369=B_SPLINE_CURVE_WITH_KNOTS ( 'NONE', 3,
 ( #49717, #50761, #34344, #24183, #44494, #60901, #11963, #65787, #60555, #17912 ),
 .UNSPECIFIED., .F., .F.,
 ( 4, 2, 2, 2, 4 ),
 ( 0.000000000000000000, 0.2500000000000000000, 0.5000000000000000000, 0.7500000000000000000, 1.000000000000000000 ),
 .UNSPECIFIED. ) ;
#30373=CARTESIAN_POINT ( 'NONE',  ( 11.10887482311539998, 5.184953745778000389, 7.021250586468399391 ) ) ;
#30427=CARTESIAN_POINT ( 'NONE',  ( 10.67826222744820086, 3.331419131587999960, 6.949274830123499669 ) ) ;
#30442=CARTESIAN_POINT ( 'NONE',  ( 11.58071932425156980, 3.832730087831799803, 6.371589232479998977 ) ) ;
#30486=CARTESIAN_POINT ( 'NONE',  ( 11.18424042080583369, 4.544092497359196514, 8.657883396625685180 ) ) ;
#30498=CARTESIAN_POINT ( 'NONE',  ( 11.59603632436369125, 3.157359628034400068, 7.696781148700499564 ) ) ;
#30500=CARTESIAN_POINT ( 'NONE',  ( 9.703659112603999048, 3.623260508844300176, 6.719118894894999805 ) ) ;
#30503=CARTESIAN_POINT ( 'NONE',  ( 8.599999986286999132, 4.750000013710600655, 7.499999999961952213 ) ) ;
#30533=CARTESIAN_POINT ( 'NONE',  ( 11.76588784977539781, 2.879134238109999799, 7.564049652083489228 ) ) ;
#30547=CARTESIAN_POINT ( 'NONE',  ( 10.01057120343299900, 3.937990586507050139, 6.222291352336999815 ) ) ;
#30623=CARTESIAN_POINT ( 'NONE',  ( 11.59999999999999609, 4.866008700487510552, 8.272804384030438385 ) ) ;
#30663=FACE_OUTER_BOUND ( 'NONE', #27092, .T. ) ;
#30669=CARTESIAN_POINT ( 'NONE',  ( 9.091433907306445406, 4.945719512329345591, 6.668243572402049679 ) ) ;
#30670=EDGE_LOOP ( 'NONE', ( #32447, #37712, #25044, #34824, #66487, #14265, #53404, #16009, #67313, #10654 ) ) ;
#30674=CARTESIAN_POINT ( 'NONE',  ( 10.76857802013509868, 2.825431102905000103, 7.527343341769989316 ) ) ;
#30679=CARTESIAN_POINT ( 'NONE',  ( 10.27610941423800028, 4.844410192686099847, 8.266982106121901097 ) ) ;
#30710=CARTESIAN_POINT ( 'NONE',  ( 11.35502763632549872, 2.839566963815999934, 8.035454525731699604 ) ) ;
#30727=MANIFOLD_SOLID_BREP ( 'Stock-MAS-678-1', #47056 ) ;
#30741=CARTESIAN_POINT ( 'NONE',  ( 10.53521345716899837, 4.924890298941200228, 6.659120737011199331 ) ) ;
#30753=CARTESIAN_POINT ( 'NONE',  ( 10.34393020684899867, 2.750000000000000000, 7.500000000000000000 ) ) ;
#30765=CARTESIAN_POINT ( 'NONE',  ( 11.83518044953559922, 4.768048975940600620, 7.099502491684900107 ) ) ;
#30781=CARTESIAN_POINT ( 'NONE',  ( 10.79303032197930001, 4.663532080728800544, 8.427909097977700270 ) ) ;
#30795=CARTESIAN_POINT ( 'NONE',  ( 11.63825819896753977, 3.148796120250299868, 7.339530235223699073 ) ) ;
#30842=CARTESIAN_POINT ( 'NONE',  ( 10.34184687351645771, 3.000416447002276943, 8.268183399968647151 ) ) ;
#30845=CARTESIAN_POINT ( 'NONE',  ( 10.15958376188599921, 3.268856270222099791, 7.034020612385399218 ) ) ;
#30864=CARTESIAN_POINT ( 'NONE',  ( 9.048601287889788125, 4.000000467705929985, 6.301404677806389465 ) ) ;
#30880=CARTESIAN_POINT ( 'NONE',  ( 11.72433327354039889, 3.016779570871600313, 8.143111181492699302 ) ) ;
#30891=( LENGTH_UNIT ( ) NAMED_UNIT ( * ) SI_UNIT ( .MILLI., .METRE. ) );
#30893=CARTESIAN_POINT ( 'NONE',  ( 9.377342523874999003, 2.735516931877000513, 7.693563834190999984 ) ) ;
#30913=B_SPLINE_CURVE_WITH_KNOTS ( 'NONE', 3,
 ( #20328, #16114, #379, #37439 ),
 .UNSPECIFIED., .F., .F.,
 ( 4, 4 ),
 ( 0.1836163425310829433, 1.000000000000000000 ),
 .UNSPECIFIED. ) ;
#30927=CARTESIAN_POINT ( 'NONE',  ( 9.785684229509998389, 3.098260518542999886, 8.407331414124799451 ) ) ;
#30951=CARTESIAN_POINT ( 'NONE',  ( 10.24733997687999931, 4.272363749081500295, 8.748653021963999521 ) ) ;
#30960=STYLED_ITEM ( 'NONE', ( #20392 ), #46039 ) ;
#31016=CARTESIAN_POINT ( 'NONE',  ( 11.30367835872029936, 2.886444435522000251, 8.201822467543799178 ) ) ;
#31027=CARTESIAN_POINT ( 'NONE',  ( 11.10101463001529964, 4.622233839778099984, 8.496586578655598743 ) ) ;
#31033=CARTESIAN_POINT ( 'NONE',  ( 10.69041504065829962, 5.024558373595999328, 8.263934892306599167 ) ) ;
#31058=CARTESIAN_POINT ( 'NONE',  ( 9.979346873516126593, 4.163624617374466652, 6.249999999999999112 ) ) ;
#31065=CARTESIAN_POINT ( 'NONE',  ( 10.87309687351627652, 2.782534154164606921, 7.827184855449101697 ) ) ;
#31121=CARTESIAN_POINT ( 'NONE',  ( 10.94903032197929882, 4.503839166471300004, 8.204588308639600314 ) ) ;
#31138=CARTESIAN_POINT ( 'NONE',  ( 10.66995391537419913, 4.943675741382899780, 6.859089544950699668 ) ) ;
#31154=CARTESIAN_POINT ( 'NONE',  ( 11.02287616594229824, 3.738072157442200005, 8.325646653015098764 ) ) ;
#31160=ADVANCED_FACE ( 'NONE', ( #41593 ), #18300, .T. ) ;
#31197=CARTESIAN_POINT ( 'NONE',  ( 10.28976354018291239, 3.672815144550904076, 8.717465845835395299 ) ) ;
#31199=CARTESIAN_POINT ( 'NONE',  ( 9.450367640780999778, 4.408706755790200660, 8.264635032075899446 ) ) ;
#31229=CARTESIAN_POINT ( 'NONE',  ( 11.35034208742529849, 3.369365911179700301, 6.508707709313799050 ) ) ;
#31243=CARTESIAN_POINT ( 'NONE',  ( 8.490822372493999737, 3.632306086542600010, 6.297150255604999636 ) ) ;
#31282=B_SPLINE_SURFACE_WITH_KNOTS ( 'NONE', 3, 3, ( 
 ( #49691, #12291, #59477, #44468, #60185, #44116, #10900, #27331, #59829, #28030, #5646, #48996, #32246, #11934, #32577, #65055, #59137, #26988, #54233, #49337, #48304, #11577, #53889, #39204, #33619, #65413, #17535, #33273, #5991, #54938, #22767, #6333, #22069, #1798, #410, #21725, #37816, #28375, #6685, #23116, #43419, #54590, #16487, #64714, #27682, #11240, #16827, #1452, #7040, #38864, #17885, #48654, #1108, #65762, #38151, #22420, #17173, #43761, #38505, #18576, #19249, #39551, #45490, #46174, #8082, #67138, #66805 ),
 ( #61560, #40577, #13676, #51074, #55634, #29424, #39903, #18917, #8426, #3509, #60875, #67482, #24506, #28725, #19605, #29076, #66109, #18226, #33965, #24847, #12990, #60526, #35005, #61904, #61222, #51414, #56321, #29768, #40242, #3177, #13338, #45827, #34313, #55288, #14020, #30111, #12635, #7383, #66455, #50041, #2150, #23468, #35347, #56663, #8769, #44805, #7733, #23811, #50386, #2486, #45144, #34662, #55975, #50732, #2826, #24156, #47896, #63614, #4197, #47480, #68856, #20977, #9789, #41956, #20285, #15040, #9104 ),
 ( #41613, #20631, #53135, #40924, #10139, #46520, #30442, #62247, #36718, #51753, #42312, #35688, #15730, #52441, #31815, #63263, #10474, #3847, #25186, #67825, #41268, #19947, #47206, #58039, #62582, #14364, #14703, #5234, #37058, #47555, #36021, #57002, #52789, #58372, #25534, #57336, #62920, #9438, #30781, #52092, #36367, #46862, #57679, #31138, #26572, #68165, #4883, #4536, #25872, #68508, #15391, #26225, #31470, #54507, #32845, #17092, #32165, #43337, #64641, #59064, #53478, #44030, #10821, #17453, #59402, #22342, #49259 ),
 ( #38075, #682, #29246, #11501, #63953, #5572, #11851, #5913, #26913, #16063, #16407, #6606, #64290, #38424, #48228, #39728, #21649, #48922, #1369, #54157, #65334, #16748, #1030, #6257, #27596, #48577, #61045, #334, #27948, #42983, #58718, #37393, #43681, #64978, #22686, #50556, #21992, #13166, #37738, #34495, #11165, #59749, #33189, #55807, #32500, #7908, #21313, #42643, #53815, #27254, #36188, #14184, #35172, #9261, #3338, #51576, #14865, #30951, #41093, #8248, #40079, #23984, #67644, #61388, #51917, #66626, #46689 ) ),
 .UNSPECIFIED., .F., .F., .F.,
 ( 4, 4 ),
 ( 4, 1, 1, 1, 1, 1, 1, 1, 1, 1, 1, 1, 1, 1, 1, 1, 1, 1, 1, 1, 1, 1, 1, 1, 1, 1, 1, 1, 1, 1, 1, 1, 1, 1, 1, 1, 1, 1, 1, 1, 1, 1, 1, 1, 1, 1, 1, 1, 1, 1, 1, 1, 1, 1, 1, 1, 1, 1, 1, 1, 1, 1, 1, 1, 4 ),
 ( -0.02000000000000000042, 1.020000000000000018 ),
 ( 0.008747244164287000176, 0.02453926110774999961, 0.04033127805120999970, 0.05612329499467000327, 0.07191531193812999989, 0.08770732888158999652, 0.1034993458251000087, 0.1192913627684999978, 0.1350833797120000179, 0.1508753966553999792, 0.1666674135988999994, 0.1824594305423999918, 0.1982514474858000086, 0.2140434644293000011, 0.2298354813727000179, 0.2456274983162000103, 0.2614195152596999749, 0.2772115322030999640, 0.2930035491465999842, 0.3087955660900000288, 0.3245875830334999934, 0.3403795999769999581, 0.3561716169204000026, 0.3719636338639000228, 0.3877556508073999875, 0.4035476677507999765, 0.4193396846942999967, 0.4351317016376999858, 0.4509237185811999504, 0.4667157355247000261, 0.4825077524681000152, 0.4982997694115999798, 0.5140917863550000799, 0.5298838032985000446, 0.5456758202420000092, 0.5614678371854000538, 0.5772598541289000185, 0.5930518710723000630, 0.6088438880158000277, 0.6246359049592999924, 0.6404279219027000369, 0.6562199388462000016, 0.6720119557896999662, 0.6878039727331000108, 0.7035959896765999755, 0.7193880066200000201, 0.7351800235634999847, 0.7509720405069999494, 0.7667640574504001050, 0.7825560743939000696, 0.7983480913373000032, 0.8141401082808000789, 0.8299321252243000435, 0.8457241421676999771, 0.8615161591112000528, 0.8773081760545999863, 0.8931001929981000620, 0.9088922099416000266, 0.9246842268849999602, 0.9404762438285000359, 0.9562682607720000005, 0.9720602777153999341, 0.9878522946589000098, 1.003644311601999961, 1.019436328545999970 ),
 .UNSPECIFIED. ) ;
#31354=CARTESIAN_POINT ( 'NONE',  ( 11.67766954483535891, 4.715882430684499305, 8.604570063127999546 ) ) ;
#31366=CARTESIAN_POINT ( 'NONE',  ( 10.68546886766499959, 3.433493735705800187, 8.529286361367999447 ) ) ;
#31371=CARTESIAN_POINT ( 'NONE',  ( 10.32118582084299874, 3.163839350524900063, 8.466515260542900378 ) ) ;
#31383=CARTESIAN_POINT ( 'NONE',  ( 8.761230081853241813, 4.521411717137521435, 6.718925885376237694 ) ) ;
#31455=CARTESIAN_POINT ( 'NONE',  ( 11.09672200990539892, 3.182132064022000328, 7.785290430335599865 ) ) ;
#31470=CARTESIAN_POINT ( 'NONE',  ( 10.44841638348500013, 2.891666689023999925, 7.769976643522699788 ) ) ;
#31479=ORIENTED_EDGE ( 'NONE', *, *, #52640, .T. ) ;
#31482=CARTESIAN_POINT ( 'NONE',  ( 9.385596873516666605, 2.907767014557175678, 6.870476274536375882 ) ) ;
#31533=CARTESIAN_POINT ( 'NONE',  ( 10.32844474310100047, 4.771257858050099721, 7.125715588371799747 ) ) ;
#31566=CARTESIAN_POINT ( 'NONE',  ( 11.38678751119029897, 2.833702563575000166, 6.889827023674499173 ) ) ;
#31582=CARTESIAN_POINT ( 'NONE',  ( 9.630633995698000049, 5.271405458160000279, 7.358888170452400068 ) ) ;
#31611=CARTESIAN_POINT ( 'NONE',  ( 10.11496314287999887, 5.251703735191999733, 7.763860089407599752 ) ) ;
#31656=VECTOR ( 'NONE', #6264, 1000.000000000000000 ) ;
#31708=CARTESIAN_POINT ( 'NONE',  ( 10.39969598649000027, 4.888000489779200208, 6.971269690999399415 ) ) ;
#31714=CARTESIAN_POINT ( 'NONE',  ( 11.05964426047339799, 4.687693494822500639, 6.422784126663999338 ) ) ;
#31727=CARTESIAN_POINT ( 'NONE',  ( 8.798455008774128672, 4.948455060776569603, 7.263673592043552674 ) ) ;
#31792=PRODUCT_DEFINITION_CONTEXT ( 'detailed design', #20833, 'design' ) ;
#31801=CARTESIAN_POINT ( 'NONE',  ( 11.12133729122639991, 3.134101783108900197, 7.522778681411049995 ) ) ;
#31815=CARTESIAN_POINT ( 'NONE',  ( 11.38379707368349969, 3.433355370490100533, 8.490052513816499058 ) ) ;
#31830=CARTESIAN_POINT ( 'NONE',  ( 9.416846873516664829, 3.231816600031355069, 6.500416447002274722 ) ) ;
#31832=CARTESIAN_POINT ( 'NONE',  ( 10.64949279009019989, 3.739015461786900030, 6.531063508962500208 ) ) ;
#31843=CYLINDRICAL_SURFACE ( 'NONE', #28027, 1.250000000000000222 ) ;
#31860=CARTESIAN_POINT ( 'NONE',  ( 8.719914745407999490, 3.934662526658240012, 6.596431033727998994 ) ) ;
#31877=CARTESIAN_POINT ( 'NONE',  ( 10.22726354018266370, 4.629523725463627670, 8.592232985442818105 ) ) ;
#31880=CARTESIAN_POINT ( 'NONE',  ( 9.855633995697999694, 4.861719613449499988, 7.404358731173799946 ) ) ;
#31912=CARTESIAN_POINT ( 'NONE',  ( 11.83003632436370012, 2.756744593645999775, 7.790336465152099876 ) ) ;
#31927=CARTESIAN_POINT ( 'NONE',  ( 9.529317406968999649, 4.237919115995800290, 6.243107450209000042 ) ) ;
#31938=CARTESIAN_POINT ( 'NONE',  ( 9.682824781140627834, 3.392296711160748490, 6.870532779523098377 ) ) ;
#31939=CARTESIAN_POINT ( 'NONE',  ( 8.863694533038728451, 4.511314481744639338, 8.385421723231823776 ) ) ;
#31945=DIRECTION ( 'NONE',  ( -1.000000000000000000, 0.000000000000000000, 0.000000000000000000 ) ) ;
#31960=CARTESIAN_POINT ( 'NONE',  ( 10.41891290906799838, 3.190593056227700064, 6.509421987543800192 ) ) ;
#32008=CARTESIAN_POINT ( 'NONE',  ( 11.60000000000000497, 3.695216987067942327, 8.455673667202294297 ) ) ;
#32012=CARTESIAN_POINT ( 'NONE',  ( 11.07299956498199833, 5.207010770456999893, 7.174999999999999822 ) ) ;
#32058=CARTESIAN_POINT ( 'NONE',  ( 10.86190547754509872, 4.891676932241900033, 7.471700551735359852 ) ) ;
#32149=CARTESIAN_POINT ( 'NONE',  ( 10.64949279009019989, 3.739015461786900030, 6.531063508962500208 ) ) ;
#32165=CARTESIAN_POINT ( 'NONE',  ( 10.34995525820099971, 3.892289273474800471, 8.635644537520001052 ) ) ;
#32179=CARTESIAN_POINT ( 'NONE',  ( 11.43718179236249988, 3.790319673775199849, 8.481317998227099864 ) ) ;
#32210=CARTESIAN_POINT ( 'NONE',  ( 8.734200250017998712, 4.093844212487689482, 6.613277660092100163 ) ) ;
#32221=LINE ( 'NONE', #28002, #1461 ) ;
#32231=CARTESIAN_POINT ( 'NONE',  ( 9.146417874593998576, 3.202096358337300330, 7.160798403412399260 ) ) ;
#32246=CARTESIAN_POINT ( 'NONE',  ( 11.58902763632552002, 3.213494089586499847, 7.862914650060299770 ) ) ;
#32260=CARTESIAN_POINT ( 'NONE',  ( 10.47769598648999967, 5.009476315410999803, 6.898940957443399746 ) ) ;
#32308=CARTESIAN_POINT ( 'NONE',  ( 10.39358376188600097, 2.921249888908000081, 6.812480849273599759 ) ) ;
#32349=CARTESIAN_POINT ( 'NONE',  ( 11.59999999999999964, 4.016704963253245886, 8.547709597963843109 ) ) ;
#32360=CARTESIAN_POINT ( 'NONE',  ( 11.28627509987130040, 3.727547057523676433, 8.749999999999998224 ) ) ;
#32381=EDGE_CURVE ( 'NONE', #12913, #43427, #59307, .T. ) ;
#32399=CARTESIAN_POINT ( 'NONE',  ( 10.93990547754509812, 5.032986398992000510, 7.467215766047949899 ) ) ;
#32447=ORIENTED_EDGE ( 'NONE', *, *, #38092, .F. ) ;
#32486=CARTESIAN_POINT ( 'NONE',  ( 10.52641638348499953, 3.025038519517300184, 7.737488872214999702 ) ) ;
#32500=CARTESIAN_POINT ( 'NONE',  ( 10.56733863405299800, 4.788475529394700558, 6.494205428462000107 ) ) ;
#32514=CARTESIAN_POINT ( 'NONE',  ( 9.552263540183332680, 5.092232985442822546, 6.870476274536374994 ) ) ;
#32515=CARTESIAN_POINT ( 'NONE',  ( 10.48133997687999930, 4.184599793140999502, 8.346298710230199092 ) ) ;
#32577=CARTESIAN_POINT ( 'NONE',  ( 11.53979707368350027, 3.569730287184500472, 8.251775607861899786 ) ) ;
#32593=CARTESIAN_POINT ( 'NONE',  ( 11.27234208742519783, 3.445253572379500362, 6.627995351445298944 ) ) ;
#32603=VERTEX_POINT ( 'NONE', #56773 ) ;
#32622=CARTESIAN_POINT ( 'NONE',  ( 9.226900131858625898, 3.814237572305042345, 6.645000240129933289 ) ) ;
#32642=CARTESIAN_POINT ( 'NONE',  ( 11.13746005378019888, 5.161099018038999731, 8.120007936598501175 ) ) ;
#32644=CARTESIAN_POINT ( 'NONE',  ( 9.657025935145998830, 3.834207658792500251, 8.629711178834000407 ) ) ;
#32692=CARTESIAN_POINT ( 'NONE',  ( 8.722809814040999754, 4.614409247670200109, 6.705428891605899722 ) ) ;
#32700=B_SPLINE_CURVE_WITH_KNOTS ( 'NONE', 3,
 ( #25465, #11703, #59253, #27112, #32360, #37587, #16263, #43535, #5770, #46798 ),
 .UNSPECIFIED., .F., .F.,
 ( 4, 2, 2, 2, 4 ),
 ( 0.000000000000000000, 0.2500000000000002220, 0.5000000000000004441, 0.7500000000000002220, 1.000000000000000000 ),
 .UNSPECIFIED. ) ;
#32776=ORIENTED_EDGE ( 'NONE', *, *, #8990, .F. ) ;
#32821=CARTESIAN_POINT ( 'NONE',  ( 11.51961669203094196, 5.030276287827526005, 7.824983907773938263 ) ) ;
#32826=CARTESIAN_POINT ( 'NONE',  ( 11.36333594839950045, 4.659759757475400832, 8.256087240512899328 ) ) ;
#32845=CARTESIAN_POINT ( 'NONE',  ( 10.39918582084299992, 3.253651555277099927, 8.362701637490498996 ) ) ;
#32859=CARTESIAN_POINT ( 'NONE',  ( 11.19102897915239936, 4.256858847510399890, 6.529961657816500065 ) ) ;
#32897=CARTESIAN_POINT ( 'NONE',  ( 11.21253483539785556, 3.661009989788314822, 6.691360637068768824 ) ) ;
#32906=CARTESIAN_POINT ( 'NONE',  ( 8.766480666858997850, 4.289077172771600388, 6.682599852064000423 ) ) ;
#32910=EDGE_LOOP ( 'NONE', ( #66817, #56956, #58856, #43971, #63568, #26497, #1768, #11679, #22529, #65831, #48203, #47389 ) ) ;
#32938=CARTESIAN_POINT ( 'NONE',  ( 10.52435971519499880, 4.532462039660099862, 8.385788382729799650 ) ) ;
#32953=SURFACE_STYLE_FILL_AREA ( #59517 ) ;
#32964=CARTESIAN_POINT ( 'NONE',  ( 9.809470517051625649, 4.641899585206984646, 6.905443702049931964 ) ) ;
#32984=CARTESIAN_POINT ( 'NONE',  ( 11.06456920625009843, 4.037149028919880145, 8.532838639935999225 ) ) ;
#32986=CARTESIAN_POINT ( 'NONE',  ( 10.11295058442699890, 4.453199839589800035, 8.548019252390998801 ) ) ;
#33037=CARTESIAN_POINT ( 'NONE',  ( 9.330709346416998784, 4.907312911337299965, 7.930842873041400232 ) ) ;
#33043=CARTESIAN_POINT ( 'NONE',  ( 9.104759580228998672, 3.156743194445300382, 7.701558687214699717 ) ) ;
#33086=CARTESIAN_POINT ( 'NONE',  ( 11.02812378248509795, 3.583106837161099900, 8.288725998710999576 ) ) ;
#33107=CARTESIAN_POINT ( 'NONE',  ( 11.23052404082913291, 2.954319127720149041, 7.824990945864982450 ) ) ;
#33129=B_SPLINE_CURVE_WITH_KNOTS ( 'NONE', 3,
 ( #41391, #46982, #10597, #57117, #42077, #25997, #9218, #20752, #20405, #15511, #21425, #31939, #63388, #36143, #68631, #68285 ),
 .UNSPECIFIED., .F., .F.,
 ( 4, 2, 2, 2, 2, 2, 2, 4 ),
 ( 0.000000000000000000, 0.1250000000000002498, 0.2500000000000004996, 0.3750000000000007772, 0.5000000000000009992, 0.6250000000000004441, 0.7499999999999998890, 1.000000000000000000 ),
 .UNSPECIFIED. ) ;
#33174=CARTESIAN_POINT ( 'NONE',  ( 10.72333863405319931, 4.619094858989799768, 6.710270673950399889 ) ) ;
#33189=CARTESIAN_POINT ( 'NONE',  ( 10.61656919669529842, 5.225637333137999718, 7.137881914002699446 ) ) ;
#33205=CARTESIAN_POINT ( 'NONE',  ( 10.50595525820100029, 3.918212119278319694, 8.362327856951900173 ) ) ;
#33208=CARTESIAN_POINT ( 'NONE',  ( 10.59393020684899867, 5.250000000000000000, 7.500000000000000000 ) ) ;
#33228=CARTESIAN_POINT ( 'NONE',  ( 8.762289945692000259, 3.761977284103799946, 6.588711079851200303 ) ) ;
#33250=CARTESIAN_POINT ( 'NONE',  ( 11.00000000000000000, 5.079754677601000523, 7.174999999999999822 ) ) ;
#33273=CARTESIAN_POINT ( 'NONE',  ( 11.21979841651039855, 3.695024856201900132, 6.689266534545799558 ) ) ;
#33283=VERTEX_POINT ( 'NONE', #61945 ) ;
#33288=CARTESIAN_POINT ( 'NONE',  ( 11.06456920625009843, 4.037149028919880145, 8.532838639935999225 ) ) ;
#33304=CARTESIAN_POINT ( 'NONE',  ( 10.31021345716899873, 4.636538040886300394, 6.921280946186199934 ) ) ;
#33338=CARTESIAN_POINT ( 'NONE',  ( 10.52435971519499880, 4.532462039660099862, 8.385788382729799650 ) ) ;
#33340=CARTESIAN_POINT ( 'NONE',  ( 9.783671671056998420, 2.873958896683999953, 7.310881302803900361 ) ) ;
#33387=CARTESIAN_POINT ( 'NONE',  ( 8.849455549952999434, 4.781695603001899997, 8.130709350565298976 ) ) ;
#33392=CARTESIAN_POINT ( 'NONE',  ( 9.332721904869998752, 4.756019688173900306, 7.075568408810499754 ) ) ;
#33404=CARTESIAN_POINT ( 'NONE',  ( 8.599999952505998024, 4.000000000000000000, 7.500000000000000000 ) ) ;
#33463=VERTEX_POINT ( 'NONE', #19989 ) ;
#33491=CARTESIAN_POINT ( 'NONE',  ( 11.57299956498156845, 5.207010770456999893, 7.174999999999999822 ) ) ;
#33516=CARTESIAN_POINT ( 'NONE',  ( 11.42834208742529967, 3.293478249981899975, 6.389420067180999752 ) ) ;
#33521=CARTESIAN_POINT ( 'NONE',  ( 10.79718447801629999, 5.003225587801999552, 7.522119512433738997 ) ) ;
#33551=CARTESIAN_POINT ( 'NONE',  ( 10.89149144726329865, 3.340422662105400065, 8.430724369296298093 ) ) ;
#33565=CARTESIAN_POINT ( 'NONE',  ( 10.31021345716899873, 4.636538040886300394, 6.921280946186199934 ) ) ;
#33573=CARTESIAN_POINT ( 'NONE',  ( 8.811649685568998080, 4.101356036306899711, 6.542299367266399379 ) ) ;
#33619=CARTESIAN_POINT ( 'NONE',  ( 11.29364426047339975, 4.466097552695299733, 6.769896129503799820 ) ) ;
#33636=CARTESIAN_POINT ( 'NONE',  ( 10.89324174884020024, 3.967693531726030010, 6.325557131097000685 ) ) ;
#33651=( NAMED_UNIT ( * ) PLANE_ANGLE_UNIT ( ) SI_UNIT ( $, .RADIAN. ) );
#33663=CARTESIAN_POINT ( 'NONE',  ( 8.821633776942626071, 4.724939341952408611, 7.010106850326409678 ) ) ;
#33682=CARTESIAN_POINT ( 'NONE',  ( 10.89324174884020024, 3.967693531726030010, 6.325557131097000685 ) ) ;
#33685=CARTESIAN_POINT ( 'NONE',  ( 9.859659112603999631, 3.503852111758100296, 6.471616938597000157 ) ) ;
#33689=CARTESIAN_POINT ( 'NONE',  ( 10.47726354018323214, 3.370476274536374106, 6.407767014557177454 ) ) ;
#33732=CARTESIAN_POINT ( 'NONE',  ( 11.00000000000000000, 2.941427501403999667, 7.174999999999999822 ) ) ;
#33734=CARTESIAN_POINT ( 'NONE',  ( 9.558671671056998775, 3.009461603020800347, 7.333638993632098924 ) ) ;
#33737=CARTESIAN_POINT ( 'NONE',  ( 9.508513540182335078, 3.836375382625529795, 6.250000000000000888 ) ) ;
#33742=CARTESIAN_POINT ( 'NONE',  ( 10.01459632033899894, 3.070047649444500149, 7.879514065647800436 ) ) ;
#33778=CARTESIAN_POINT ( 'NONE',  ( 10.32118582084299874, 3.163839350524900063, 8.466515260542900378 ) ) ;
#33810=ORIENTED_EDGE ( 'NONE', *, *, #30315, .T. ) ;
#33862=CARTESIAN_POINT ( 'NONE',  ( 11.01279632507519857, 4.624908853805600906, 6.341531314375999706 ) ) ;
#33867=CARTESIAN_POINT ( 'NONE',  ( 10.69456919669529960, 5.093991349577000172, 7.176777099639999768 ) ) ;
#33881=ADVANCED_FACE ( 'NONE', ( #6044 ), #68992, .T. ) ;
#33883=ORIENTED_EDGE ( 'NONE', *, *, #65959, .T. ) ;
#33892=CARTESIAN_POINT ( 'NONE',  ( 9.791846873516664829, 3.000416447002276943, 8.268183399968645375 ) ) ;
#33900=CARTESIAN_POINT ( 'NONE',  ( 11.43302763632549990, 2.964209339073000216, 7.977941233841399971 ) ) ;
#33925=CARTESIAN_POINT ( 'NONE',  ( 9.343930206849998754, 2.750000000000000000, 7.500000000000000000 ) ) ;
#33965=CARTESIAN_POINT ( 'NONE',  ( 11.36333594839950045, 4.659759757475400832, 8.256087240512899328 ) ) ;
#34015=CARTESIAN_POINT ( 'NONE',  ( 9.593930206849998754, 5.250000000000000000, 7.500000000000000000 ) ) ;
#34033=CARTESIAN_POINT ( 'NONE',  ( 11.43345123989529810, 4.540230239159599890, 6.456682674800999777 ) ) ;
#34036=CARTESIAN_POINT ( 'NONE',  ( 9.705671671056999017, 3.009461603020800347, 7.333638993632098924 ) ) ;
#34040=CARTESIAN_POINT ( 'NONE',  ( 10.46684687351657672, 3.231816600031355069, 6.500416447002276499 ) ) ;
#34044=CARTESIAN_POINT ( 'NONE',  ( 8.731616107288068918, 4.000002263255225898, 6.618420992905501343 ) ) ;
#34081=CARTESIAN_POINT ( 'NONE',  ( 9.735975701333000387, 4.736880367605900588, 6.817468224793199916 ) ) ;
#34086=CARTESIAN_POINT ( 'NONE',  ( 9.963938025973998691, 3.477805217445600228, 8.357994702431799539 ) ) ;
#34125=CARTESIAN_POINT ( 'NONE',  ( 10.61656919669529842, 5.225637333137999718, 7.137881914002699446 ) ) ;
#34215=CARTESIAN_POINT ( 'NONE',  ( 10.34995525820099971, 3.892289273474800471, 8.635644537520001052 ) ) ;
#34246=CARTESIAN_POINT ( 'NONE',  ( 10.86687616594229944, 3.655053560864600204, 8.587337146608000182 ) ) ;
#34265=VECTOR ( 'NONE', #4354, 1000.000000000000000 ) ;
#34268=CARTESIAN_POINT ( 'NONE',  ( 8.720712484379999907, 3.780467314030099946, 6.659501631675699862 ) ) ;
#34275=CARTESIAN_POINT ( 'NONE',  ( 9.181310023244000362, 4.573021367100345458, 8.622334741229296995 ) ) ;
#34292=EDGE_CURVE ( 'NONE', #26174, #8994, #69080, .T. ) ;
#34312=( GEOMETRIC_REPRESENTATION_CONTEXT ( 3 ) GLOBAL_UNCERTAINTY_ASSIGNED_CONTEXT ( ( #65829 ) ) GLOBAL_UNIT_ASSIGNED_CONTEXT ( ( #52898, #27714, #59168 ) ) REPRESENTATION_CONTEXT ( 'NONE', 'WORKASPACE' ) );
#34313=CARTESIAN_POINT ( 'NONE',  ( 11.01872200990539952, 3.052519557825900343, 7.830502140005199507 ) ) ;
#34328=ORIENTED_EDGE ( 'NONE', *, *, #65959, .F. ) ;
#34343=VERTEX_POINT ( 'NONE', #62624 ) ;
#34344=CARTESIAN_POINT ( 'NONE',  ( 10.05333291544899943, 4.531093146757585011, 6.341063066638221279 ) ) ;
#34380=CARTESIAN_POINT ( 'NONE',  ( 11.68788784977535933, 3.014014167207800465, 7.556342205905759890 ) ) ;
#34382=CARTESIAN_POINT ( 'NONE',  ( 10.38955864497999926, 4.790758628877400227, 6.880692865553299953 ) ) ;
#34432=CARTESIAN_POINT ( 'NONE',  ( 9.934583761885999564, 2.921249888908000081, 6.812480849273599759 ) ) ;
#34439=CARTESIAN_POINT ( 'NONE',  ( 9.687329965421998423, 3.397808798486600335, 6.876242273533999416 ) ) ;
#34441=ORIENTED_EDGE ( 'NONE', *, *, #43404, .T. ) ;
#34495=CARTESIAN_POINT ( 'NONE',  ( 10.69041504065829962, 5.024558373595999328, 8.263934892306599167 ) ) ;
#34534=DIRECTION ( 'NONE',  ( 0.000000000000000000, 1.000000000000000000, 0.000000000000000000 ) ) ;
#34556=CARTESIAN_POINT ( 'NONE',  ( 9.991279731608999626, 4.077800926195140008, 8.363513150096299142 ) ) ;
#34565=CARTESIAN_POINT ( 'NONE',  ( 11.13764426047339917, 4.613828180779599997, 6.538488127609999978 ) ) ;
#34599=CARTESIAN_POINT ( 'NONE',  ( 10.45257053952200010, 3.605640676136899980, 8.422730500489899796 ) ) ;
#34609=ORIENTED_EDGE ( 'NONE', *, *, #62589, .T. ) ;
#34620=CARTESIAN_POINT ( 'NONE',  ( 8.797364180957998769, 3.929432544163579788, 6.524104241236299728 ) ) ;
#34625=CARTESIAN_POINT ( 'NONE',  ( 9.303275160948496492, 2.900329483618105719, 8.115397037630309285 ) ) ;
#34662=CARTESIAN_POINT ( 'NONE',  ( 10.55103166480599874, 2.999015536536000504, 7.429424106427209296 ) ) ;
#34724=CARTESIAN_POINT ( 'NONE',  ( 9.756329965421999262, 3.302375896175799852, 6.777391592843399870 ) ) ;
#34769=B_SPLINE_CURVE_WITH_KNOTS ( 'NONE', 3,
 ( #747, #26980, #399, #64354 ),
 .UNSPECIFIED., .F., .F.,
 ( 4, 4 ),
 ( 0.000000000000000000, 1.000000000000000000 ),
 .UNSPECIFIED. ) ;
#34771=CARTESIAN_POINT ( 'NONE',  ( 9.632646554151000018, 4.552790318865400643, 6.500921769151600138 ) ) ;
#34774=CARTESIAN_POINT ( 'NONE',  ( 9.571013540182331525, 4.768183399968643599, 6.500416447002274722 ) ) ;
#34780=CARTESIAN_POINT ( 'NONE',  ( 11.60000000000000320, 3.125502297258556883, 7.130791426018634915 ) ) ;
#34782=CARTESIAN_POINT ( 'NONE',  ( 8.736820887142258130, 3.746718250072767820, 6.641515014115457305 ) ) ;
#34813=CARTESIAN_POINT ( 'NONE',  ( 10.07503300763299947, 4.881889043637199777, 6.575021251017499679 ) ) ;
#34824=ORIENTED_EDGE ( 'NONE', *, *, #30315, .F. ) ;
#34838=ORIENTED_EDGE ( 'NONE', *, *, #3103, .F. ) ;
#34891=CARTESIAN_POINT ( 'NONE',  ( 10.34588779216199939, 4.801941500727100021, 7.210800365544999480 ) ) ;
#34896=CARTESIAN_POINT ( 'NONE',  ( 11.83003632436370012, 2.756744593645999775, 7.790336465152099876 ) ) ;
#34901=CARTESIAN_POINT ( 'NONE',  ( 11.03918313518939875, 3.292400735470800033, 6.605241151424599444 ) ) ;
#34929=CARTESIAN_POINT ( 'NONE',  ( 9.677263540183332680, 4.629523725463628558, 8.592232985442819881 ) ) ;
#34935=CARTESIAN_POINT ( 'NONE',  ( 11.62994988689359843, 4.518136976474400157, 6.483720595741000459 ) ) ;
#34938=CARTESIAN_POINT ( 'NONE',  ( 10.77101354018289925, 3.231816600031359066, 8.499583552997725278 ) ) ;
#35000=ORIENTED_EDGE ( 'NONE', *, *, #7177, .T. ) ;
#35005=CARTESIAN_POINT ( 'NONE',  ( 11.26487482311540056, 4.930401445321599851, 7.124095752359899336 ) ) ;
#35036=B_SPLINE_CURVE_WITH_KNOTS ( 'NONE', 3,
 ( #59380, #32821, #54486, #6586 ),
 .UNSPECIFIED., .F., .F.,
 ( 4, 4 ),
 ( 0.000000000000000000, 1.000000000000000000 ),
 .UNSPECIFIED. ) ;
#35037=CARTESIAN_POINT ( 'NONE',  ( 8.929547492598356229, 4.733899445644309978, 6.695580748437408580 ) ) ;
#35067=CARTESIAN_POINT ( 'NONE',  ( 11.36056039236529891, 4.891071240644300211, 7.456633480985620288 ) ) ;
#35069=CARTESIAN_POINT ( 'NONE',  ( 9.302417874593999159, 2.949199072237000063, 7.053287723251499663 ) ) ;
#35117=CARTESIAN_POINT ( 'NONE',  ( 8.847442991499999465, 3.928121959910110483, 8.639547276484998761 ) ) ;
#35154=CARTESIAN_POINT ( 'NONE',  ( 10.91195257254739914, 2.772832764353999835, 7.143100915737699452 ) ) ;
#35166=CARTESIAN_POINT ( 'NONE',  ( 10.64393020684969926, 5.250000000000000000, 7.500000000000000000 ) ) ;
#35172=CARTESIAN_POINT ( 'NONE',  ( 10.37041638348499895, 2.758294858530000226, 7.802464414828100381 ) ) ;
#35191=CARTESIAN_POINT ( 'NONE',  ( 11.60000000000000320, 4.804380105966679082, 8.322973907256262294 ) ) ;
#35241=CARTESIAN_POINT ( 'NONE',  ( 11.23078751119019891, 3.084247107206000038, 7.020904658857499925 ) ) ;
#35246=CARTESIAN_POINT ( 'NONE',  ( 10.84226088462129844, 4.002427228022017225, 8.640738455926999961 ) ) ;
#35278=CARTESIAN_POINT ( 'NONE',  ( 10.32533997688000049, 4.243109097101799954, 8.614534918052999757 ) ) ;
#35347=CARTESIAN_POINT ( 'NONE',  ( 10.77256919669529900, 4.962345366016100101, 7.215672285280100517 ) ) ;
#35359=CARTESIAN_POINT ( 'NONE',  ( 10.94501463001509833, 4.472480213525599879, 8.256737112932800216 ) ) ;
#35361=CARTESIAN_POINT ( 'NONE',  ( 10.92441504065829960, 4.694414232677499577, 8.017771632862299214 ) ) ;
#35390=FACE_OUTER_BOUND ( 'NONE', #61326, .T. ) ;
#35402=ORIENTED_EDGE ( 'NONE', *, *, #55846, .T. ) ;
#35407=CARTESIAN_POINT ( 'NONE',  ( 10.06027973160899869, 4.090130512164860122, 8.500359330993999762 ) ) ;
#35410=EDGE_CURVE ( 'NONE', #60390, #5246, #3693, .T. ) ;
#35453=FILL_AREA_STYLE ('',( #14126 ) ) ;
#35455=CARTESIAN_POINT ( 'NONE',  ( 9.050076168957998490, 3.420574098817999786, 6.516130052788599691 ) ) ;
#35463=CARTESIAN_POINT ( 'NONE',  ( 11.52285868696541549, 4.059810388505518119, 6.228129494253469289 ) ) ;
#35572=CARTESIAN_POINT ( 'NONE',  ( 11.55300581613033906, 5.107584469683000172, 6.788791567531699656 ) ) ;
#35579=CARTESIAN_POINT ( 'NONE',  ( 10.11792546752099931, 3.135062625344399834, 7.559927309296559983 ) ) ;
#35583=CARTESIAN_POINT ( 'NONE',  ( 11.51656039236534923, 5.173498198882000132, 7.442888368925779652 ) ) ;
#35590=CARTESIAN_POINT ( 'NONE',  ( 11.42887348028849992, 2.875789035466000065, 6.892162778124999889 ) ) ;
#35594=CARTESIAN_POINT ( 'NONE',  ( 11.57299956498156845, 5.207010770456999893, 7.174999999999999822 ) ) ;
#35607=CYLINDRICAL_SURFACE ( 'NONE', #46098, 1.250000000000000222 ) ;
#35615=EDGE_CURVE ( 'NONE', #10441, #43157, #11563, .T. ) ;
#35623=CARTESIAN_POINT ( 'NONE',  ( 10.98579841651039857, 3.550031058388499972, 6.303820944768999901 ) ) ;
#35625=CARTESIAN_POINT ( 'NONE',  ( 10.84393020684979980, 2.750000000000000000, 7.500000000000000000 ) ) ;
#35664=CARTESIAN_POINT ( 'NONE',  ( 11.46021572556888657, 2.954248811040025124, 7.824997386306807634 ) ) ;
#35688=CARTESIAN_POINT ( 'NONE',  ( 11.45764291764649911, 2.867875922590999771, 7.639947095788999221 ) ) ;
#35701=CARTESIAN_POINT ( 'NONE',  ( 11.34287482311539996, 4.803125295093300551, 7.175518335304800210 ) ) ;
#35738=CARTESIAN_POINT ( 'NONE',  ( 8.599999986286999132, 3.249999986289399789, 7.500000000038047787 ) ) ;
#35742=CARTESIAN_POINT ( 'NONE',  ( 10.61257802013489737, 3.108115747127599970, 7.520762592984879369 ) ) ;
#35744=CARTESIAN_POINT ( 'NONE',  ( 10.00760887879199856, 3.803658216258800184, 8.344486736701099971 ) ) ;
#35792=CARTESIAN_POINT ( 'NONE',  ( 9.784621437244998887, 4.758411336345700349, 8.353549467159899322 ) ) ;
#35830=DIRECTION ( 'NONE',  ( -1.000000000000000000, 0.000000000000000000, 0.000000000000000000 ) ) ;
#35862=CARTESIAN_POINT ( 'NONE',  ( 10.12435795695566476, 5.250000000000000000, 7.192559817601734906 ) ) ;
#35865=DIRECTION ( 'NONE',  ( 0.000000000000000000, 0.000000000000000000, -1.000000000000000000 ) ) ;
#35888=DIRECTION ( 'NONE',  ( -1.000000000000000000, 0.000000000000000000, 0.000000000000000000 ) ) ;
#35914=CARTESIAN_POINT ( 'NONE',  ( 10.81013259637009938, 2.968328969579000276, 6.937848198857199833 ) ) ;
#35921=CARTESIAN_POINT ( 'NONE',  ( 11.35502763632549872, 2.839566963815999934, 8.035454525731699604 ) ) ;
#35950=CARTESIAN_POINT ( 'NONE',  ( 10.20226357027499908, 5.120085139777000194, 7.283900408233900059 ) ) ;
#36005=CARTESIAN_POINT ( 'NONE',  ( 10.55518582084299872, 3.433275964779900047, 8.155074391384399490 ) ) ;
#36021=CARTESIAN_POINT ( 'NONE',  ( 10.98995257254739855, 2.904643075091000171, 7.181435527216799564 ) ) ;
#36032=CARTESIAN_POINT ( 'NONE',  ( 9.489763540183334456, 4.327184855449099921, 6.282534154164604701 ) ) ;
#36033=CARTESIAN_POINT ( 'NONE',  ( 11.56441235500451015, 3.361299021099800388, 8.085115074060599483 ) ) ;
#36083=CARTESIAN_POINT ( 'NONE',  ( 9.148430433047000321, 3.145249924879699677, 8.027488966151301142 ) ) ;
#36089=ORIENTED_EDGE ( 'NONE', *, *, #27624, .T. ) ;
#36115=CARTESIAN_POINT ( 'NONE',  ( 11.46989666366029859, 3.941571897678119996, 6.185029684353999357 ) ) ;
#36130=CARTESIAN_POINT ( 'NONE',  ( 9.022734463322999332, 4.133249246727800141, 6.227746477418000026 ) ) ;
#36143=CARTESIAN_POINT ( 'NONE',  ( 8.837278925393343698, 4.883321897350202612, 8.012901425336814043 ) ) ;
#36188=CARTESIAN_POINT ( 'NONE',  ( 10.41964694612699915, 2.813019656517000477, 7.026297514493899499 ) ) ;
#36246=CARTESIAN_POINT ( 'NONE',  ( 11.46989666366029859, 3.941571897678119996, 6.185029684353999357 ) ) ;
#36257=CARTESIAN_POINT ( 'NONE',  ( 11.56322412107030928, 4.054600656575539475, 8.532060764998998792 ) ) ;
#36259=ORIENTED_EDGE ( 'NONE', *, *, #66129, .T. ) ;
#36262=CARTESIAN_POINT ( 'NONE',  ( 10.56733863405299800, 4.788475529394700558, 6.494205428462000107 ) ) ;
#36289=CARTESIAN_POINT ( 'NONE',  ( 9.948096873516250938, 3.672815144550898303, 6.282534154164604701 ) ) ;
#36290=ORIENTED_EDGE ( 'NONE', *, *, #7482, .F. ) ;
#36349=CARTESIAN_POINT ( 'NONE',  ( 10.99826088462129903, 4.001843064679911244, 8.366195817038299509 ) ) ;
#36367=CARTESIAN_POINT ( 'NONE',  ( 10.74379975933729980, 5.078682052940000524, 7.871126858273000515 ) ) ;
#36425=CARTESIAN_POINT ( 'NONE',  ( 10.31059687351633158, 3.370476274536378103, 8.592232985442823434 ) ) ;
#36427=CARTESIAN_POINT ( 'NONE',  ( 9.399709346416997846, 4.783195203880800328, 7.871904849557299855 ) ) ;
#36458=CARTESIAN_POINT ( 'NONE',  ( 10.88813259637009878, 2.844182332072999753, 6.870201387206400057 ) ) ;
#36472=CARTESIAN_POINT ( 'NONE',  ( 8.794772138681999252, 3.523984281974800403, 8.687347221188998603 ) ) ;
#36494=CARTESIAN_POINT ( 'NONE',  ( 9.938608878791999501, 3.772542739612499751, 8.478317686146800369 ) ) ;
#36505=CARTESIAN_POINT ( 'NONE',  ( 9.633709346416999608, 5.155548326249999924, 8.048718920009699573 ) ) ;
#36534=ORIENTED_EDGE ( 'NONE', *, *, #43735, .T. ) ;
#36556=VERTEX_POINT ( 'NONE', #51533 ) ;
#36587=AXIS2_PLACEMENT_3D ( 'NONE', #17613, #27759, #1182 ) ;
#36593=CARTESIAN_POINT ( 'NONE',  ( 11.42834208742529967, 3.293478249981899975, 6.389420067180999752 ) ) ;
#36604=CARTESIAN_POINT ( 'NONE',  ( 11.35034208742529849, 3.369365911179700301, 6.508707709313799050 ) ) ;
#36610=CARTESIAN_POINT ( 'NONE',  ( 10.39503166480599994, 2.725152142215999884, 7.410114961806599787 ) ) ;
#36615=EDGE_CURVE ( 'NONE', #24944, #68176, #1416, .T. ) ;
#36701=CARTESIAN_POINT ( 'NONE',  ( 11.71210404293059959, 3.618181340822599790, 6.722495590581700320 ) ) ;
#36706=ADVANCED_FACE ( 'NONE', ( #19903 ), #20243, .F. ) ;
#36718=CARTESIAN_POINT ( 'NONE',  ( 11.53148876160955005, 3.209326035813000022, 6.677731919207799294 ) ) ;
#36733=CARTESIAN_POINT ( 'NONE',  ( 11.76133460557259980, 4.139849081322200419, 6.645166161828299778 ) ) ;
#36744=FACE_OUTER_BOUND ( 'NONE', #22002, .T. ) ;
#36760=CARTESIAN_POINT ( 'NONE',  ( 8.734020077949999461, 3.936452720224709712, 6.621188087644399367 ) ) ;
#36776=CARTESIAN_POINT ( 'NONE',  ( 9.526355082327999213, 3.611978631017199959, 8.275336934318801241 ) ) ;
#36812=CARTESIAN_POINT ( 'NONE',  ( 11.59966954483535773, 4.638989336656000440, 8.485927942460499196 ) ) ;
#36856=CARTESIAN_POINT ( 'NONE',  ( 9.456405316140999773, 3.728406863338599830, 6.249951378708000327 ) ) ;
#36902=CARTESIAN_POINT ( 'NONE',  ( 11.60000000000000142, 3.599560744838743886, 8.403338258880264533 ) ) ;
#36959=CARTESIAN_POINT ( 'NONE',  ( 10.17764828895399809, 5.001141961424000471, 6.953185708700699408 ) ) ;
#36988=CARTESIAN_POINT ( 'NONE',  ( 10.05226354018249779, 5.092232985442822546, 6.870476274536374994 ) ) ;
#37042=CARTESIAN_POINT ( 'NONE',  ( 11.81056516821459823, 4.609678151793300316, 6.884701936848800052 ) ) ;
#37058=CARTESIAN_POINT ( 'NONE',  ( 11.03918313518939875, 3.292400735470800033, 6.605241151424599444 ) ) ;
#37073=CARTESIAN_POINT ( 'NONE',  ( 10.84641504065830020, 4.804462279649600376, 8.099826052678000821 ) ) ;
#37102=CARTESIAN_POINT ( 'NONE',  ( 8.741072744221000335, 3.937347817007940343, 6.633566614602499634 ) ) ;
#37118=CARTESIAN_POINT ( 'NONE',  ( 10.15434687351570631, 5.250000000000002665, 7.663624617374463988 ) ) ;
#37120=CARTESIAN_POINT ( 'NONE',  ( 8.802265421554999136, 3.811499292588199861, 6.524915741324599949 ) ) ;
#37163=CARTESIAN_POINT ( 'NONE',  ( 8.845430433046999497, 2.911395389258000233, 8.171806809244198888 ) ) ;
#37173=CARTESIAN_POINT ( 'NONE',  ( 9.277558426223626142, 4.358884483112399622, 6.702043737600841489 ) ) ;
#37175=CARTESIAN_POINT ( 'NONE',  ( 11.59999999999999964, 3.116215992411100366, 7.174999999999999822 ) ) ;
#37196=CARTESIAN_POINT ( 'NONE',  ( 10.29226717315700057, 3.026371913119300316, 8.329718467866699783 ) ) ;
#37201=DIRECTION ( 'NONE',  ( 0.000000000000000000, -1.000000000000000000, 0.000000000000000000 ) ) ;
#37239=CARTESIAN_POINT ( 'NONE',  ( 11.59999999999999787, 3.905927825748639837, 8.528759793293470892 ) ) ;
#37252=VERTEX_POINT ( 'NONE', #48800 ) ;
#37295=CARTESIAN_POINT ( 'NONE',  ( 10.29657053952199952, 3.497746311184500190, 8.675184076076000395 ) ) ;
#37329=CARTESIAN_POINT ( 'NONE',  ( 10.88351354018293904, 2.750000000000000000, 7.663624617374469317 ) ) ;
#37380=CARTESIAN_POINT ( 'NONE',  ( 11.85979573085659844, 4.840012015667699785, 7.354650721737899133 ) ) ;
#37393=CARTESIAN_POINT ( 'NONE',  ( 10.88733729122639993, 2.722429312291999803, 7.533608309972310124 ) ) ;
#37408=CARTESIAN_POINT ( 'NONE',  ( 9.573096873516668381, 5.217465845835396188, 7.172815144550900968 ) ) ;
#37410=CARTESIAN_POINT ( 'NONE',  ( 10.60026222744819790, 3.225465054973100099, 6.861998062869400172 ) ) ;
#37439=CARTESIAN_POINT ( 'NONE',  ( 8.710288521113000115, 3.647046440108700160, 6.715449042252499723 ) ) ;
#37454=CARTESIAN_POINT ( 'NONE',  ( 10.39393020684999946, 2.750000000000000000, 7.500000000000000000 ) ) ;
#37486=CARTESIAN_POINT ( 'NONE',  ( 11.84388784977539899, 2.744254309011999737, 7.571757098260779806 ) ) ;
#37488=VECTOR ( 'NONE', #38037, 1000.000000000000000 ) ;
#37504=AXIS2_PLACEMENT_3D ( 'NONE', #68018, #47748, #42499 ) ;
#37512=CARTESIAN_POINT ( 'NONE',  ( 9.505520750864626223, 3.872956735472087964, 8.365674464137100586 ) ) ;
#37576=ADVANCED_FACE ( 'NONE', ( #16889 ), #11640, .T. ) ;
#37587=CARTESIAN_POINT ( 'NONE',  ( 11.25158531382730054, 4.272452942476326676, 8.749999999999998224 ) ) ;
#37627=CARTESIAN_POINT ( 'NONE',  ( 11.11123293495519881, 3.108594079907299967, 7.535834283667469435 ) ) ;
#37629=ORIENTED_EDGE ( 'NONE', *, *, #32381, .F. ) ;
#37637=CARTESIAN_POINT ( 'NONE',  ( 8.710288521113000115, 3.647046440108700160, 6.715449042252499723 ) ) ;
#37712=ORIENTED_EDGE ( 'NONE', *, *, #18338, .F. ) ;
#37721=CARTESIAN_POINT ( 'NONE',  ( 10.87103032197929942, 4.583685623598699799, 8.316248703309600643 ) ) ;
#37729=CYLINDRICAL_SURFACE ( 'NONE', #54610, 1.250000000000000222 ) ;
#37738=CARTESIAN_POINT ( 'NONE',  ( 10.71503032197929883, 4.743378537856500543, 8.539569492647999027 ) ) ;
#37752=CARTESIAN_POINT ( 'NONE',  ( 11.26487482311540056, 4.930401445321599851, 7.124095752359899336 ) ) ;
#37801=CARTESIAN_POINT ( 'NONE',  ( 9.019772138681998896, 3.677371150249499898, 8.304747519296199698 ) ) ;
#37816=CARTESIAN_POINT ( 'NONE',  ( 10.99826088462129903, 4.001843064679911244, 8.366195817038299509 ) ) ;
#37830=CARTESIAN_POINT ( 'NONE',  ( 10.73213259636989925, 3.092475607087700418, 7.005495010505599751 ) ) ;
#37847=LINE ( 'NONE', #28404, #62692 ) ;
#37849=CARTESIAN_POINT ( 'NONE',  ( 10.40299135172147693, 4.795252583382552558, 7.862853843651285146 ) ) ;
#37859=CARTESIAN_POINT ( 'NONE',  ( 10.30371347217102596, 4.589291630936049415, 6.869346568680468224 ) ) ;
#37881=CARTESIAN_POINT ( 'NONE',  ( 11.51145123989532948, 4.605239108938600445, 6.331134574721999364 ) ) ;
#37883=CARTESIAN_POINT ( 'NONE',  ( 9.380417874594000338, 2.822750429186000165, 6.999532383170999239 ) ) ;
#37924=CARTESIAN_POINT ( 'NONE',  ( 11.14975833414749928, 3.203462856645999945, 7.174999999999999822 ) ) ;
#37929=CARTESIAN_POINT ( 'NONE',  ( 9.584000818238999742, 3.111278474435999808, 7.032008172796599510 ) ) ;
#37973=CARTESIAN_POINT ( 'NONE',  ( 11.52677869730533011, 3.596497913043499750, 8.295667533166499297 ) ) ;
#38009=B_SPLINE_SURFACE_WITH_KNOTS ( 'NONE', 3, 3, ( 
 ( #33573, #34620, #1406, #17842 ),
 ( #54893, #11888, #33228, #66064 ),
 ( #55240, #18183, #54547, #39505 ),
 ( #12942, #2441, #34268, #7691 ) ),
 .UNSPECIFIED., .F., .F., .F.,
 ( 4, 4 ),
 ( 4, 4 ),
 ( 0.7363163806532000422, 1.013499456067999960 ),
 ( -0.0005287450254680999126, 0.02696599629895000266 ),
 .UNSPECIFIED. ) ;
#38011=PLANE ( 'NONE',  #65618 ) ;
#38037=DIRECTION ( 'NONE',  ( -1.000000000000000000, 0.000000000000000000, 2.886579864060000134E-14 ) ) ;
#38061=CARTESIAN_POINT ( 'NONE',  ( 11.51102763632551884, 3.088851714329700293, 7.920427941950599404 ) ) ;
#38075=CARTESIAN_POINT ( 'NONE',  ( 11.62579573085663043, 5.239377455231000624, 7.285547569258399747 ) ) ;
#38089=CARTESIAN_POINT ( 'NONE',  ( 10.33364828895399867, 4.760196147278000112, 7.084788038520800413 ) ) ;
#38092=EDGE_CURVE ( 'NONE', #23962, #23956, #7981, .T. ) ;
#38138=CARTESIAN_POINT ( 'NONE',  ( 9.197076168957998732, 3.560025096655699883, 6.752918994396699404 ) ) ;
#38151=CARTESIAN_POINT ( 'NONE',  ( 10.55518582084299872, 3.433275964779900047, 8.155074391384399490 ) ) ;
#38166=CARTESIAN_POINT ( 'NONE',  ( 10.85168717260509830, 3.386210853237200169, 6.498190316041999814 ) ) ;
#38185=FILL_AREA_STYLE_COLOUR ( '', #49532 ) ;
#38186=CARTESIAN_POINT ( 'NONE',  ( 10.74760529021567734, 4.040385281810796592, 6.626811228128840270 ) ) ;
#38198=CARTESIAN_POINT ( 'NONE',  ( 9.936116252963625328, 4.581155023945095550, 8.154057418782388211 ) ) ;
#38221=CARTESIAN_POINT ( 'NONE',  ( 11.26723293495529887, 2.826061044294000180, 7.547192037433419820 ) ) ;
#38223=CARTESIAN_POINT ( 'NONE',  ( 10.36624205625100004, 3.590523439766200031, 6.434137271007999814 ) ) ;
#38266=CARTESIAN_POINT ( 'NONE',  ( 11.60000000000000142, 3.430179236374870655, 8.269794803757207546 ) ) ;
#38267=CARTESIAN_POINT ( 'NONE',  ( 11.27769289846838241, 2.954326301843319680, 7.175017342370984430 ) ) ;
#38272=CARTESIAN_POINT ( 'NONE',  ( 9.987254614702999689, 2.893436332050999926, 7.218483930889299849 ) ) ;
#38279=CARTESIAN_POINT ( 'NONE',  ( 10.19190035061499877, 4.267716286314199969, 6.531924610394499453 ) ) ;
#38305=EDGE_CURVE ( 'NONE', #52369, #21254, #44619, .T. ) ;
#38317=CARTESIAN_POINT ( 'NONE',  ( 10.90346005378009941, 4.786957292481900161, 7.920222357891399945 ) ) ;
#38355=B_SPLINE_CURVE_WITH_KNOTS ( 'NONE', 3,
 ( #30255, #14170, #9591, #67288, #40729, #62054 ),
 .UNSPECIFIED., .F., .F.,
 ( 4, 1, 1, 4 ),
 ( 0.000000000000000000, 0.3333333333333000081, 0.6666666666667000474, 1.000000000000000000 ),
 .UNSPECIFIED. ) ;
#38370=EDGE_CURVE ( 'NONE', #26690, #56577, #41291, .T. ) ;
#38409=CARTESIAN_POINT ( 'NONE',  ( 10.99410672858429905, 3.198097575668700010, 8.103244025831999764 ) ) ;
#38424=CARTESIAN_POINT ( 'NONE',  ( 11.33041235500449950, 3.057642534728299832, 8.363295307663500822 ) ) ;
#38436=LINE ( 'NONE', #61409, #31656 ) ;
#38442=CARTESIAN_POINT ( 'NONE',  ( 10.89564560330029863, 4.307504762655200103, 8.455191956516999952 ) ) ;
#38481=CARTESIAN_POINT ( 'NONE',  ( 11.32240614981507854, 4.732436490098000270, 7.017906081141798147 ) ) ;
#38505=CARTESIAN_POINT ( 'NONE',  ( 10.45672469555900008, 4.433465011431599656, 8.249937779480299938 ) ) ;
#38521=CARTESIAN_POINT ( 'NONE',  ( 11.36056039236529891, 4.891071240644300211, 7.456633480985620288 ) ) ;
#38539=CARTESIAN_POINT ( 'NONE',  ( 10.33103907547007694, 4.774162136902415199, 7.100484084056944312 ) ) ;
#38540=CARTESIAN_POINT ( 'NONE',  ( 9.341834235717472623, 3.000408294236256435, 8.268200207948643410 ) ) ;
#38549=CARTESIAN_POINT ( 'NONE',  ( 10.13874943042162613, 3.152062997842154157, 7.284280020558234980 ) ) ;
#38567=CARTESIAN_POINT ( 'NONE',  ( 10.64902344389989963, 3.116469856398800253, 8.036199780531900316 ) ) ;
#38571=CARTESIAN_POINT ( 'NONE',  ( 9.606367640780998585, 4.538247246588100303, 8.506987760366000018 ) ) ;
#38622=CARTESIAN_POINT ( 'NONE',  ( 8.773468108405998223, 4.966402032527499344, 7.226304214866999587 ) ) ;
#38629=CARTESIAN_POINT ( 'NONE',  ( 10.24255864497999902, 4.790758628877400227, 6.880692865553299953 ) ) ;
#38762=CARTESIAN_POINT ( 'NONE',  ( 11.11718313518939816, 3.377550038693600154, 6.712912394634500401 ) ) ;
#38792=CARTESIAN_POINT ( 'NONE',  ( 10.32949413291699869, 4.912929163218899831, 7.916546720849799712 ) ) ;
#38794=( GEOMETRIC_REPRESENTATION_CONTEXT ( 3 ) GLOBAL_UNCERTAINTY_ASSIGNED_CONTEXT ( ( #2218 ) ) GLOBAL_UNIT_ASSIGNED_CONTEXT ( ( #30891, #52548, #68272 ) ) REPRESENTATION_CONTEXT ( 'NONE', 'WORKASPACE' ) );
#38846=CARTESIAN_POINT ( 'NONE',  ( 9.374380199233998567, 4.860242402105300563, 7.608124715612800237 ) ) ;
#38864=CARTESIAN_POINT ( 'NONE',  ( 10.67826222744820086, 3.331419131587999960, 6.949274830123499669 ) ) ;
#38877=CARTESIAN_POINT ( 'NONE',  ( 11.48522412107029922, 4.047131449166419870, 8.390877922225699947 ) ) ;
#38926=CARTESIAN_POINT ( 'NONE',  ( 11.22567835872029995, 3.006051690924700370, 8.126439557340900066 ) ) ;
#38928=CARTESIAN_POINT ( 'NONE',  ( 10.18893802597399834, 3.406370524467499994, 8.475365825607600101 ) ) ;
#38953=CARTESIAN_POINT ( 'NONE',  ( 11.11486084871780022, 5.207010770456999893, 7.825000000000000178 ) ) ;
#38977=CARTESIAN_POINT ( 'NONE',  ( 8.900113844317997902, 4.253652595614200393, 8.471855267550699509 ) ) ;
#38983=CARTESIAN_POINT ( 'NONE',  ( 9.155417874594000693, 3.202096358337300330, 7.160798403412399260 ) ) ;
#39018=CARTESIAN_POINT ( 'NONE',  ( 10.94452754078378121, 4.508448539877488059, 8.211034235888378774 ) ) ;
#39090=VERTEX_POINT ( 'NONE', #27775 ) ;
#39101=CARTESIAN_POINT ( 'NONE',  ( 11.09590547754519996, 5.315605332491999846, 7.458246194669389872 ) ) ;
#39106=CARTESIAN_POINT ( 'NONE',  ( 10.86687616594229944, 3.655053560864600204, 8.587337146608000182 ) ) ;
#39118=ORIENTED_EDGE ( 'NONE', *, *, #38305, .T. ) ;
#39135=CARTESIAN_POINT ( 'NONE',  ( 10.25564828895399927, 4.880669054351300495, 7.018986873610899124 ) ) ;
#39165=CARTESIAN_POINT ( 'NONE',  ( 9.150818738817875442, 4.951062758656399332, 8.326721469190600189 ) ) ;
#39204=CARTESIAN_POINT ( 'NONE',  ( 11.31825954179440075, 4.666231193203100425, 6.946434658287599540 ) ) ;
#39217=CARTESIAN_POINT ( 'NONE',  ( 11.60477869730532774, 3.532552483170099844, 8.421761806503198500 ) ) ;
#39236=CARTESIAN_POINT ( 'NONE',  ( 9.289752973821549631, 3.672827138550766257, 8.717426404466650069 ) ) ;
#39267=CARTESIAN_POINT ( 'NONE',  ( 10.97635090131019986, 4.999207052587699707, 6.881982988766500497 ) ) ;
#39269=CARTESIAN_POINT ( 'NONE',  ( 9.707684229509998985, 3.195116560491999991, 8.309874741421300115 ) ) ;
#39317=CARTESIAN_POINT ( 'NONE',  ( 8.925442991499998868, 3.936771438983030169, 8.502419298200999620 ) ) ;
#39323=CARTESIAN_POINT ( 'NONE',  ( 9.307392757686999474, 4.585219941293200208, 6.860292594369099106 ) ) ;
#39374=B_SPLINE_CURVE_WITH_KNOTS ( 'NONE', 3,
 ( #61677, #66917, #29192, #51867, #35463, #25302, #30220, #2604, #24961, #23932 ),
 .UNSPECIFIED., .F., .F.,
 ( 4, 2, 2, 2, 4 ),
 ( 0.000000000000000000, 0.2499999999999995559, 0.4999999999999991118, 0.7499999999999995559, 1.000000000000000000 ),
 .UNSPECIFIED. ) ;
#39436=AXIS2_PLACEMENT_3D ( 'NONE', #40589, #56331, #51085 ) ;
#39445=CARTESIAN_POINT ( 'NONE',  ( 10.92968717260509948, 3.312350236372100021, 6.377637058250999580 ) ) ;
#39452=CARTESIAN_POINT ( 'NONE',  ( 10.59610807141099897, 4.052703327804870526, 6.360477084256999980 ) ) ;
#39467=CARTESIAN_POINT ( 'NONE',  ( 8.969356963619999235, 2.880642974985999860, 7.500000000085178087 ) ) ;
#39485=CARTESIAN_POINT ( 'NONE',  ( 11.03918313518939875, 3.292400735470800033, 6.605241151424599444 ) ) ;
#39504=CARTESIAN_POINT ( 'NONE',  ( 11.28192504596561996, 4.908977993420656105, 7.174999814284952926 ) ) ;
#39505=CARTESIAN_POINT ( 'NONE',  ( 8.727215710425999973, 3.626036035117899736, 6.691239224408199071 ) ) ;
#39540=ORIENTED_EDGE ( 'NONE', *, *, #43735, .F. ) ;
#39551=CARTESIAN_POINT ( 'NONE',  ( 10.38287885159599888, 4.860099138268600072, 7.602606670248799325 ) ) ;
#39578=( LENGTH_UNIT ( ) NAMED_UNIT ( * ) SI_UNIT ( .MILLI., .METRE. ) );
#39581=CARTESIAN_POINT ( 'NONE',  ( 9.279336721442295044, 3.836368765436817263, 8.749993199158911494 ) ) ;
#39591=CARTESIAN_POINT ( 'NONE',  ( 8.897621218489625505, 4.818672874536578554, 7.808718305523518310 ) ) ;
#39611=CARTESIAN_POINT ( 'NONE',  ( 11.35034208742529849, 3.369365911179700301, 6.508707709313799050 ) ) ;
#39614=CARTESIAN_POINT ( 'NONE',  ( 9.958963142879998287, 4.982812171771600518, 7.707177545471399327 ) ) ;
#39620=ORIENTED_EDGE ( 'NONE', *, *, #17175, .T. ) ;
#39643=ORIENTED_EDGE ( 'NONE', *, *, #18338, .T. ) ;
#39662=CARTESIAN_POINT ( 'NONE',  ( 9.455342523874998406, 2.871335344632000020, 7.672773098917999413 ) ) ;
#39671=CARTESIAN_POINT ( 'NONE',  ( 9.636671671056999955, 3.144964309357700216, 7.356396684460199786 ) ) ;
#39690=DIRECTION ( 'NONE',  ( -1.000000000000000000, 0.000000000000000000, 0.000000000000000000 ) ) ;
#39704=CARTESIAN_POINT ( 'NONE',  ( 11.08126742035591228, 3.231380926423224054, 7.893373809886144343 ) ) ;
#39710=CARTESIAN_POINT ( 'NONE',  ( 10.76426088462129904, 4.002719309691810778, 8.778009775371000245 ) ) ;
#39728=CARTESIAN_POINT ( 'NONE',  ( 11.28118179236249929, 3.732952383914999839, 8.749800764654999341 ) ) ;
#39746=CARTESIAN_POINT ( 'NONE',  ( 9.748096873515667227, 4.327184855449106138, 8.717465845835393523 ) ) ;
#39799=CARTESIAN_POINT ( 'NONE',  ( 11.35918179236250047, 3.761636028845500412, 8.615559381441000752 ) ) ;
#39816=CARTESIAN_POINT ( 'NONE',  ( 8.982564767455604837, 2.896581991245594789, 7.204352198296668064 ) ) ;
#39833=CARTESIAN_POINT ( 'NONE',  ( 10.40333997687999990, 4.213854445120500003, 8.480416814141699788 ) ) ;
#39862=CARTESIAN_POINT ( 'NONE',  ( 9.171146261768624797, 4.712741083356099203, 8.539225147222756718 ) ) ;
#39903=CARTESIAN_POINT ( 'NONE',  ( 11.65871932425156920, 3.852858594438699935, 6.507377093516500288 ) ) ;
#39917=CARTESIAN_POINT ( 'NONE',  ( 10.48791429142999831, 4.016993441347180394, 8.391963954669400039 ) ) ;
#39933=CARTESIAN_POINT ( 'NONE',  ( 9.321001730958840881, 3.231794228473278352, 8.499596153627864581 ) ) ;
#39968=CARTESIAN_POINT ( 'NONE',  ( 8.973138961223998677, 4.946050868436800307, 6.860686042446299204 ) ) ;
#39976=CARTESIAN_POINT ( 'NONE',  ( 11.33810207955129812, 4.796537143354000499, 7.174999999999999822 ) ) ;
#40016=CARTESIAN_POINT ( 'NONE',  ( 9.202051052051999136, 5.120555153167999585, 7.280704316743199733 ) ) ;
#40018=CARTESIAN_POINT ( 'NONE',  ( 9.477263540182331525, 3.370476274536374106, 6.407767014557177454 ) ) ;
#40079=CARTESIAN_POINT ( 'NONE',  ( 10.17349413291699811, 5.162701151235999930, 8.030511425625498134 ) ) ;
#40147=CARTESIAN_POINT ( 'NONE',  ( 10.79303032197930001, 4.663532080728800544, 8.427909097977700270 ) ) ;
#40179=CARTESIAN_POINT ( 'NONE',  ( 10.23103300763299828, 4.692441239783899931, 6.773725604892799623 ) ) ;
#40239=CARTESIAN_POINT ( 'NONE',  ( 11.59999999999999964, 5.179498027601999510, 7.825000000000000178 ) ) ;
#40242=CARTESIAN_POINT ( 'NONE',  ( 11.11718313518939816, 3.377550038693600154, 6.712912394634500401 ) ) ;
#40274=CARTESIAN_POINT ( 'NONE',  ( 9.075651506909604649, 5.234436409784954947, 7.432209138388947700 ) ) ;
#40302=CARTESIAN_POINT ( 'NONE',  ( 9.452380199233999747, 4.996570247675600207, 7.625259896924899472 ) ) ;
#40345=CARTESIAN_POINT ( 'NONE',  ( 0.000000000000000000, 0.000000000000000000, 0.000000000000000000 ) ) ;
#40348=CARTESIAN_POINT ( 'NONE',  ( 10.11188779216199940, 5.183207142131999845, 7.073306690476799830 ) ) ;
#40385=CARTESIAN_POINT ( 'NONE',  ( 10.19810941423799910, 4.946022705791000007, 8.359277272599898723 ) ) ;
#40430=ORIENTED_EDGE ( 'NONE', *, *, #24084, .T. ) ;
#40466=CARTESIAN_POINT ( 'NONE',  ( 11.59456039236534330, 5.314711678001000195, 7.436015812896529020 ) ) ;
#40473=CARTESIAN_POINT ( 'NONE',  ( 10.32533997688000049, 4.243109097101799954, 8.614534918052999757 ) ) ;
#40507=CARTESIAN_POINT ( 'NONE',  ( 11.61759063708296047, 5.217265640542000149, 7.157757529645699890 ) ) ;
#40509=CARTESIAN_POINT ( 'NONE',  ( 10.82309687351639660, 2.782534154164606921, 7.827184855449101697 ) ) ;
#40513=DIRECTION ( 'NONE',  ( -1.000000000000000000, 0.000000000000000000, 0.000000000000000000 ) ) ;
#40577=CARTESIAN_POINT ( 'NONE',  ( 11.77359063708300013, 4.955772084214699724, 7.231278212164300001 ) ) ;
#40589=CARTESIAN_POINT ( 'NONE',  ( 9.099999931440999390, 4.000000000000000000, 7.500000000000000000 ) ) ;
#40634=CARTESIAN_POINT ( 'NONE',  ( 10.36325056272499978, 4.892034740700499817, 7.486779603004729111 ) ) ;
#40636=CARTESIAN_POINT ( 'NONE',  ( 10.31357120343299982, 3.951311476804090006, 6.496769302834999316 ) ) ;
#40642=EDGE_CURVE ( 'NONE', #21416, #46623, #17877, .T. ) ;
#40686=CARTESIAN_POINT ( 'NONE',  ( 9.683304848515998486, 5.038423216181000086, 7.025224608805800131 ) ) ;
#40729=CARTESIAN_POINT ( 'NONE',  ( 11.01811411617009817, 2.973039408543999951, 7.174999999999999822 ) ) ;
#40761=ORIENTED_EDGE ( 'NONE', *, *, #62774, .T. ) ;
#40785=FACE_OUTER_BOUND ( 'NONE', #56075, .T. ) ;
#40803=CARTESIAN_POINT ( 'NONE',  ( 10.68035971519489813, 4.678140486081599825, 8.628134814664999652 ) ) ;
#40813=CARTESIAN_POINT ( 'NONE',  ( 10.59725056272499977, 5.316133253199000208, 7.480494252843770120 ) ) ;
#40818=CARTESIAN_POINT ( 'NONE',  ( 11.03502897915239878, 4.327133900127000388, 6.264564938179000286 ) ) ;
#40852=CARTESIAN_POINT ( 'NONE',  ( 11.03502897915239878, 4.327133900127000388, 6.264564938179000286 ) ) ;
#40921=CARTESIAN_POINT ( 'NONE',  ( 11.58810207955109917, 3.203462856645999945, 7.825000000000000178 ) ) ;
#40924=CARTESIAN_POINT ( 'NONE',  ( 11.65456516821461008, 4.802916961510000249, 6.689681884064299311 ) ) ;
#40938=CARTESIAN_POINT ( 'NONE',  ( 11.24441369783139777, 3.956299011112040187, 6.634905315059499209 ) ) ;
#40985=CARTESIAN_POINT ( 'NONE',  ( 11.27745123989519982, 4.410212499603100689, 6.707778874960499849 ) ) ;
#40987=CARTESIAN_POINT ( 'NONE',  ( 10.21225461470299933, 3.026595211686900377, 7.252360304610999897 ) ) ;
#41004=LINE ( 'NONE', #4970, #52431 ) ;
#41033=CARTESIAN_POINT ( 'NONE',  ( 10.08655864497999843, 5.007105485494000696, 6.711254117843599154 ) ) ;
#41065=EDGE_CURVE ( 'NONE', #24944, #19063, #32221, .T. ) ;
#41093=CARTESIAN_POINT ( 'NONE',  ( 10.22272469555899832, 4.639546521693399761, 8.606479382885998675 ) ) ;
#41103=EDGE_CURVE ( 'NONE', #25385, #32603, #48445, .T. ) ;
#41159=CARTESIAN_POINT ( 'NONE',  ( 11.72433327354039889, 3.016779570871600313, 8.143111181492699302 ) ) ;
#41168=CARTESIAN_POINT ( 'NONE',  ( 10.85168717260509830, 3.386210853237200169, 6.498190316041999814 ) ) ;
#41173=CARTESIAN_POINT ( 'NONE',  ( 10.66579975933730040, 5.208485784810999775, 7.915786590091300035 ) ) ;
#41176=ORIENTED_EDGE ( 'NONE', *, *, #16251, .T. ) ;
#41203=CARTESIAN_POINT ( 'NONE',  ( 11.55194988689359903, 4.580487242693600081, 6.361426117087999543 ) ) ;
#41241=CARTESIAN_POINT ( 'NONE',  ( 10.16684687351567007, 4.768183399968648040, 8.499583552997725278 ) ) ;
#41252=CARTESIAN_POINT ( 'NONE',  ( 11.21979841651039855, 3.695024856201900132, 6.689266534545799558 ) ) ;
#41268=CARTESIAN_POINT ( 'NONE',  ( 11.23610538575739959, 5.109472165990999848, 7.765257665594799796 ) ) ;
#41291=B_SPLINE_CURVE_WITH_KNOTS ( 'NONE', 3,
 ( #8231, #39704, #55784, #49493, #22921, #55439, #17693, #39018, #7532, #29223, #12442, #55089, #7196, #49845, #23277, #38186, #44150, #48339, #59519, #16522, #11614, #48689, #64399, #1140, #49369, #21761, #17568, #43793, #59862, #37849, #49032, #60216, #38539, #11968, #33304 ),
 .UNSPECIFIED., .F., .F.,
 ( 4, 1, 1, 1, 1, 1, 1, 1, 1, 1, 1, 1, 1, 1, 1, 1, 1, 1, 1, 1, 1, 1, 1, 1, 1, 1, 1, 1, 1, 1, 1, 1, 4 ),
 ( 0.000000000000000000, 0.02634724210002143546, 0.05799096732718442282, 0.08963469255434740324, 0.1212784177813101688, 0.1529221430084731492, 0.1845658682354359148, 0.2162095934625989091, 0.2478533186897619034, 0.2794970439167246412, 0.3111407691438876633, 0.3427844943710506298, 0.3744282195980133676, 0.4060719448251763897, 0.4377156700521391275, 0.4693593952793021495, 0.5010031205064651161, 0.5326468457334281315, 0.5642905709605910980, 0.5959342961875536693, 0.6275780214147168579, 0.6592217466418798244, 0.6908654718688423957, 0.7225091970960055843, 0.7541529223229681556, 0.7857966475501313441, 0.8174403727772943107, 0.8490840980042568820, 0.8807278232314200705, 0.9123715484585830371, 0.9440152736855456084, 0.9756589989127087970, 1.000000000000000000 ),
 .UNSPECIFIED. ) ;
#41315=ADVANCED_FACE ( 'NONE', ( #4851 ), #9756, .T. ) ;
#41331=CARTESIAN_POINT ( 'NONE',  ( 10.77879632507499785, 4.423544049216699747, 6.714825466131699727 ) ) ;
#41333=CARTESIAN_POINT ( 'NONE',  ( 10.05826717315599872, 3.340104753140699767, 8.062357722167599050 ) ) ;
#41367=CARTESIAN_POINT ( 'NONE',  ( 10.68035971519489813, 4.678140486081599825, 8.628134814664999652 ) ) ;
#41380=ORIENTED_EDGE ( 'NONE', *, *, #57915, .T. ) ;
#41381=CARTESIAN_POINT ( 'NONE',  ( 9.149380199233998923, 5.269225938816000543, 7.659530259549099718 ) ) ;
#41391=CARTESIAN_POINT ( 'NONE',  ( 8.969356963619999235, 2.880642974985999860, 7.500000000085178087 ) ) ;
#41413=CARTESIAN_POINT ( 'NONE',  ( 10.26693802597399952, 3.334935831489500124, 8.592736948783000983 ) ) ;
#41418=PLANE ( 'NONE',  #58122 ) ;
#41451=CARTESIAN_POINT ( 'NONE',  ( 11.03443712336079940, 5.057168833716702672, 7.824978679112010838 ) ) ;
#41493=CARTESIAN_POINT ( 'NONE',  ( 10.92968717260509948, 3.312350236372100021, 6.377637058250999580 ) ) ;
#41501=CARTESIAN_POINT ( 'NONE',  ( 11.47500581613029880, 4.988618570924500339, 6.865182626353099948 ) ) ;
#41507=CARTESIAN_POINT ( 'NONE',  ( 11.23195122972050086, 4.507250159094099651, 8.673036084990000560 ) ) ;
#41534=CARTESIAN_POINT ( 'NONE',  ( 9.927263540182998725, 3.370476274536375438, 6.407767014557179230 ) ) ;
#41538=CARTESIAN_POINT ( 'NONE',  ( 11.50271932425157040, 3.812601581225100400, 6.235801371442999397 ) ) ;
#41542=CARTESIAN_POINT ( 'NONE',  ( 10.82101354018296391, 3.231816600031359510, 8.499583552997727054 ) ) ;
#41568=DIRECTION ( 'NONE',  ( 0.000000000000000000, 0.000000000000000000, -1.000000000000000000 ) ) ;
#41593=FACE_OUTER_BOUND ( 'NONE', #26824, .T. ) ;
#41595=CARTESIAN_POINT ( 'NONE',  ( 11.24441369783139777, 3.956299011112040187, 6.634905315059499209 ) ) ;
#41600=ADVANCED_FACE ( 'NONE', ( #54396 ), #5888, .T. ) ;
#41613=CARTESIAN_POINT ( 'NONE',  ( 11.70379573085659786, 5.106255642043000087, 7.308581953418300081 ) ) ;
#41626=CARTESIAN_POINT ( 'NONE',  ( 10.57980110216399972, 3.260758259645400337, 7.951464549725199227 ) ) ;
#41668=ORIENTED_EDGE ( 'NONE', *, *, #49386, .T. ) ;
#41670=CARTESIAN_POINT ( 'NONE',  ( 10.38351354018329253, 2.750000000000000000, 7.663624617374469317 ) ) ;
#41672=CARTESIAN_POINT ( 'NONE',  ( 8.869809814040998219, 4.614409247670200109, 6.705428891605899722 ) ) ;
#41705=CARTESIAN_POINT ( 'NONE',  ( 11.47500581613029880, 4.988618570924500339, 6.865182626353099948 ) ) ;
#41720=CARTESIAN_POINT ( 'NONE',  ( 9.883925467520999320, 2.723846966067000164, 7.588418444866789514 ) ) ;
#41754=CARTESIAN_POINT ( 'NONE',  ( 10.31759632033899976, 2.815618218644000414, 7.983346856269500691 ) ) ;
#41784=EDGE_CURVE ( 'NONE', #26661, #13504, #23772, .T. ) ;
#41802=LINE ( 'NONE', #16258, #42078 ) ;
#41835=CARTESIAN_POINT ( 'NONE',  ( 11.22056920625029974, 4.047312782235129802, 8.815417147437999645 ) ) ;
#41846=CARTESIAN_POINT ( 'NONE',  ( 11.68788784977535933, 3.014014167207800465, 7.556342205905759890 ) ) ;
#41851=CARTESIAN_POINT ( 'NONE',  ( 10.93656785386839836, 2.939720539848000413, 6.786470850652599474 ) ) ;
#41869=CARTESIAN_POINT ( 'NONE',  ( 11.59999999999999964, 4.000000000000000000, 7.500000000000000000 ) ) ;
#41930=CARTESIAN_POINT ( 'NONE',  ( 9.099999931440999390, 4.000000000000000000, 7.500000000000000000 ) ) ;
#41939=CARTESIAN_POINT ( 'NONE',  ( 10.35826357027499789, 4.850513154668600002, 7.335909308151700614 ) ) ;
#41942=ORIENTED_EDGE ( 'NONE', *, *, #50582, .T. ) ;
#41956=CARTESIAN_POINT ( 'NONE',  ( 10.25564828895399927, 4.880669054351300495, 7.018986873610899124 ) ) ;
#41957=ORIENTED_EDGE ( 'NONE', *, *, #21180, .F. ) ;
#41970=CARTESIAN_POINT ( 'NONE',  ( 11.46595122972049907, 4.343798595649099425, 8.295047870239098842 ) ) ;
#42017=CARTESIAN_POINT ( 'NONE',  ( 8.801820635884373800, 4.060146622106553416, 6.549596649571864937 ) ) ;
#42021=CARTESIAN_POINT ( 'NONE',  ( 10.14393020684899938, 5.250000000000000000, 7.500000000000000000 ) ) ;
#42023=CARTESIAN_POINT ( 'NONE',  ( 9.830304848515998728, 4.788504886021700102, 7.139489266142899915 ) ) ;
#42042=CARTESIAN_POINT ( 'NONE',  ( 11.59213512191444018, 3.196550831395155168, 7.825049263296810054 ) ) ;
#42052=CARTESIAN_POINT ( 'NONE',  ( 11.42834208742529967, 3.293478249981899975, 6.389420067180999752 ) ) ;
#42067=CARTESIAN_POINT ( 'NONE',  ( 9.731950584426998674, 4.507735863714500191, 8.674133161175999973 ) ) ;
#42077=CARTESIAN_POINT ( 'NONE',  ( 8.936337454063531638, 3.131903168333550536, 8.168216413461584224 ) ) ;
#42078=VECTOR ( 'NONE', #63457, 1000.000000000000000 ) ;
#42086=B_SPLINE_CURVE_WITH_KNOTS ( 'NONE', 3,
 ( #12149, #27537, #1653, #623, #48862, #64918, #17032, #28227, #49894, #44321 ),
 .UNSPECIFIED., .F., .F.,
 ( 4, 2, 2, 2, 4 ),
 ( 0.000000000000000000, 0.2500000000000000000, 0.5000000000000000000, 0.7500000000000000000, 1.000000000000000000 ),
 .UNSPECIFIED. ) ;
#42099=DIRECTION ( 'NONE',  ( -1.000000000000000000, 0.000000000000000000, -1.275169027325000072E-14 ) ) ;
#42160=LINE ( 'NONE', #63461, #48688 ) ;
#42203=CARTESIAN_POINT ( 'NONE',  ( 11.56833327354034857, 3.253412192327699959, 7.988332985010599963 ) ) ;
#42209=CARTESIAN_POINT ( 'NONE',  ( 10.44426222744799837, 3.013556901740999994, 6.687444528363699625 ) ) ;
#42243=CARTESIAN_POINT ( 'NONE',  ( 10.81059687351629961, 3.370476274536378103, 8.592232985442823434 ) ) ;
#42298=CARTESIAN_POINT ( 'NONE',  ( 10.50595525820100029, 3.918212119278319694, 8.362327856951900173 ) ) ;
#42312=CARTESIAN_POINT ( 'NONE',  ( 11.48225819896749833, 2.879005208331999910, 7.288668995979000087 ) ) ;
#42327=CARTESIAN_POINT ( 'NONE',  ( 11.75718044953559804, 4.889766368533900120, 7.036033215662999218 ) ) ;
#42355=CARTESIAN_POINT ( 'NONE',  ( 8.698396402458998367, 3.630894432589700127, 6.701746336527099501 ) ) ;
#42371=CARTESIAN_POINT ( 'NONE',  ( 9.325734463322998380, 4.104624583183299258, 6.501052555474699624 ) ) ;
#42413=CARTESIAN_POINT ( 'NONE',  ( 8.896088727410999653, 2.725263018055000153, 7.393088754863899936 ) ) ;
#42439=PLANE ( 'NONE',  #24685 ) ;
#42443=CARTESIAN_POINT ( 'NONE',  ( 9.811013376692999444, 2.859607053196999704, 8.079558723821699928 ) ) ;
#42461=DIRECTION ( 'NONE',  ( 0.000000000000000000, 1.000000000000000000, 0.000000000000000000 ) ) ;
#42499=DIRECTION ( 'NONE',  ( -1.000000000000000000, 0.000000000000000000, 0.000000000000000000 ) ) ;
#42514=ORIENTED_EDGE ( 'NONE', *, *, #24951, .F. ) ;
#42544=CARTESIAN_POINT ( 'NONE',  ( 10.31021345716899873, 4.636538040886300394, 6.921280946186199934 ) ) ;
#42628=CARTESIAN_POINT ( 'NONE',  ( 11.73671932425159881, 3.872987101045399783, 6.643164954553199664 ) ) ;
#42643=CARTESIAN_POINT ( 'NONE',  ( 10.49349279008999858, 3.667611644732699627, 6.265968249244999733 ) ) ;
#42652=CARTESIAN_POINT ( 'NONE',  ( 11.07299956498199833, 5.207010770456999893, 7.174999999999999822 ) ) ;
#42656=CARTESIAN_POINT ( 'NONE',  ( 10.82179975933729921, 4.948878321068100661, 7.826467126457498757 ) ) ;
#42660=DIRECTION ( 'NONE',  ( -1.000000000000000000, 0.000000000000000000, 0.000000000000000000 ) ) ;
#42708=CARTESIAN_POINT ( 'NONE',  ( 8.895138961223999274, 4.832207374954999857, 6.937618199889199033 ) ) ;
#42737=CARTESIAN_POINT ( 'NONE',  ( 10.92968717260509948, 3.312350236372100021, 6.377637058250999580 ) ) ;
#42752=CARTESIAN_POINT ( 'NONE',  ( 9.655963142879999239, 5.251703735191999733, 7.763860089407599752 ) ) ;
#42785=CARTESIAN_POINT ( 'NONE',  ( 9.659038493598998798, 4.925784867300699865, 8.382783533462799141 ) ) ;
#42882=CARTESIAN_POINT ( 'NONE',  ( 10.94501463001509833, 4.472480213525599879, 8.256737112932800216 ) ) ;
#42887=CARTESIAN_POINT ( 'NONE',  ( 10.24733997687999931, 4.272363749081500295, 8.748653021963999521 ) ) ;
#42922=CARTESIAN_POINT ( 'NONE',  ( 10.85226354018294792, 2.907767014557178342, 8.129523725463624118 ) ) ;
#42970=CARTESIAN_POINT ( 'NONE',  ( 11.28949010443639978, 5.000675062740000065, 7.425165037173959703 ) ) ;
#42983=CARTESIAN_POINT ( 'NONE',  ( 10.93656785386839836, 2.939720539848000413, 6.786470850652599474 ) ) ;
#42997=CARTESIAN_POINT ( 'NONE',  ( 10.55518582084299872, 3.433275964779900047, 8.155074391384399490 ) ) ;
#43030=CARTESIAN_POINT ( 'NONE',  ( 8.726787239609997471, 3.780467314030099946, 6.659501631675699862 ) ) ;
#43060=FACE_OUTER_BOUND ( 'NONE', #12030, .T. ) ;
#43075=CARTESIAN_POINT ( 'NONE',  ( 10.93990547754509812, 5.032986398992000510, 7.467215766047949899 ) ) ;
#43107=CARTESIAN_POINT ( 'NONE',  ( 9.125583543129625497, 3.128114063008116563, 7.426875573188317148 ) ) ;
#43112=ORIENTED_EDGE ( 'NONE', *, *, #24106, .F. ) ;
#43118=B_SPLINE_CURVE_WITH_KNOTS ( 'NONE', 3,
 ( #9688, #25778, #68406, #37637 ),
 .UNSPECIFIED., .F., .F.,
 ( 4, 4 ),
 ( 0.000000000000000000, 1.000000000000000000 ),
 .UNSPECIFIED. ) ;
#43124=EDGE_LOOP ( 'NONE', ( #52352, #25761, #63464, #67243 ) ) ;
#43128=CARTESIAN_POINT ( 'NONE',  ( 9.530380199233999150, 5.132898093246000215, 7.642395078236999595 ) ) ;
#43157=VERTEX_POINT ( 'NONE', #46669 ) ;
#43200=VERTEX_POINT ( 'NONE', #48375 ) ;
#43223=CARTESIAN_POINT ( 'NONE',  ( 10.73213259636989925, 3.092475607087700418, 7.005495010505599751 ) ) ;
#43320=CARTESIAN_POINT ( 'NONE',  ( 10.40333997687999990, 4.213854445120500003, 8.480416814141699788 ) ) ;
#43337=CARTESIAN_POINT ( 'NONE',  ( 10.32533997688000049, 4.243109097101799954, 8.614534918052999757 ) ) ;
#43355=CARTESIAN_POINT ( 'NONE',  ( 10.28441772631199846, 4.372518460886800185, 6.733203680593099705 ) ) ;
#43369=CARTESIAN_POINT ( 'NONE',  ( 11.48052502238429895, 5.045683737783986267, 7.175009015034043536 ) ) ;
#43404=EDGE_CURVE ( 'NONE', #16060, #33283, #19163, .T. ) ;
#43419=CARTESIAN_POINT ( 'NONE',  ( 10.89979975933730039, 4.819074589197400726, 7.781807394638899922 ) ) ;
#43427=VERTEX_POINT ( 'NONE', #47532 ) ;
#43434=CARTESIAN_POINT ( 'NONE',  ( 11.01790547754519878, 5.174295865741999734, 7.462730980357120458 ) ) ;
#43463=CARTESIAN_POINT ( 'NONE',  ( 10.06276198887462847, 3.334064478527818842, 8.067505198359821605 ) ) ;
#43481=CARTESIAN_POINT ( 'NONE',  ( 11.14767835872009982, 3.125658946326500320, 8.051056647135798272 ) ) ;
#43483=CARTESIAN_POINT ( 'NONE',  ( 9.505051052051998184, 5.120555153167999585, 7.280704316743199733 ) ) ;
#43488=CARTESIAN_POINT ( 'NONE',  ( 10.43559687351661758, 2.907767014557176566, 6.870476274536375882 ) ) ;
#43530=CARTESIAN_POINT ( 'NONE',  ( 10.03791290906799993, 3.277531639390499851, 6.615820196229499572 ) ) ;
#43535=CARTESIAN_POINT ( 'NONE',  ( 11.19955063476130164, 4.976598135215295038, 8.326430086672804265 ) ) ;
#43575=CARTESIAN_POINT ( 'NONE',  ( 10.89835090130999973, 4.878966983716200190, 6.956352367771000189 ) ) ;
#43666=CARTESIAN_POINT ( 'NONE',  ( 11.26487482311540056, 4.930401445321599851, 7.124095752359899336 ) ) ;
#43681=CARTESIAN_POINT ( 'NONE',  ( 10.86272200990529946, 2.793294545435000220, 7.920925559347199219 ) ) ;
#43697=CARTESIAN_POINT ( 'NONE',  ( 11.77359063708300013, 4.955772084214699724, 7.231278212164300001 ) ) ;
#43699=CARTESIAN_POINT ( 'NONE',  ( 10.60434687351569494, 5.250000000000001776, 7.663624617374461323 ) ) ;
#43735=EDGE_CURVE ( 'NONE', #12913, #6746, #35036, .T. ) ;
#43736=CARTESIAN_POINT ( 'NONE',  ( 11.27531844363630320, 4.339035105373933554, 6.691304915923900865 ) ) ;
#43740=CARTESIAN_POINT ( 'NONE',  ( 11.00008140503725329, 5.084125838812211917, 7.632269737612043414 ) ) ;
#43761=CARTESIAN_POINT ( 'NONE',  ( 10.48133997687999930, 4.184599793140999502, 8.346298710230199092 ) ) ;
#43776=CARTESIAN_POINT ( 'NONE',  ( 11.59603632436369125, 3.157359628034400068, 7.696781148700499564 ) ) ;
#43793=CARTESIAN_POINT ( 'NONE',  ( 10.45222191436347714, 4.437430566769827500, 8.256798586434323184 ) ) ;
#43800=ADVANCED_FACE ( 'NONE', ( #61457 ), #15503, .F. ) ;
#43805=CARTESIAN_POINT ( 'NONE',  ( 9.404204162135625822, 4.790364090350968773, 7.875309037467246753 ) ) ;
#43825=CARTESIAN_POINT ( 'NONE',  ( 10.77368717260499942, 3.460071470104900015, 6.618743573831199711 ) ) ;
#43827=CARTESIAN_POINT ( 'NONE',  ( 10.49288779216199785, 5.056118594996999782, 7.119137915499500480 ) ) ;
#43832=CARTESIAN_POINT ( 'NONE',  ( 10.39393020684999946, 2.750000000000000000, 7.500000000000000000 ) ) ;
#43872=CARTESIAN_POINT ( 'NONE',  ( 9.204063610504999104, 4.411988005505000032, 6.583971515917899531 ) ) ;
#43880=CARTESIAN_POINT ( 'NONE',  ( 9.839304848515999069, 4.788504886021700102, 7.139489266142899915 ) ) ;
#43971=ORIENTED_EDGE ( 'NONE', *, *, #12313, .T. ) ;
#44012=CARTESIAN_POINT ( 'NONE',  ( 10.96949144726329806, 3.419793223320000131, 8.318725197575499664 ) ) ;
#44030=CARTESIAN_POINT ( 'NONE',  ( 10.22687885159599830, 5.132709421626000079, 7.635128076451499268 ) ) ;
#44045=CARTESIAN_POINT ( 'NONE',  ( 11.50687348028854906, 2.996540789803000315, 6.957450711802899868 ) ) ;
#44092=CARTESIAN_POINT ( 'NONE',  ( 11.00009108335970609, 5.118893581675404647, 7.402342568044064208 ) ) ;
#44116=CARTESIAN_POINT ( 'NONE',  ( 11.76133460557259980, 4.139849081322200419, 6.645166161828299778 ) ) ;
#44129=ORIENTED_EDGE ( 'NONE', *, *, #6464, .T. ) ;
#44130=CARTESIAN_POINT ( 'NONE',  ( 11.10612378248509913, 3.517039242046199998, 8.413720204863100349 ) ) ;
#44150=CARTESIAN_POINT ( 'NONE',  ( 10.72299000889467635, 3.772656371820692911, 6.655959434011009535 ) ) ;
#44159=CARTESIAN_POINT ( 'NONE',  ( 8.757986382567201744, 4.151567127026601689, 6.650284907739020035 ) ) ;
#44178=CARTESIAN_POINT ( 'NONE',  ( 10.73213259636989925, 3.092475607087700418, 7.005495010505599751 ) ) ;
#44180=CARTESIAN_POINT ( 'NONE',  ( 10.41690035061499842, 4.304339077956200299, 6.399494776650000105 ) ) ;
#44234=CARTESIAN_POINT ( 'NONE',  ( 9.862621437244998290, 4.667147537636399335, 8.250837174995698575 ) ) ;
#44239=CARTESIAN_POINT ( 'NONE',  ( 9.611342523874998989, 3.142972170141900001, 7.631191628371899682 ) ) ;
#44253=ORIENTED_EDGE ( 'NONE', *, *, #35615, .F. ) ;
#44321=CARTESIAN_POINT ( 'NONE',  ( 10.53521345716899837, 4.924890298941200228, 6.659120737011199331 ) ) ;
#44349=ORIENTED_EDGE ( 'NONE', *, *, #16472, .F. ) ;
#44360=CARTESIAN_POINT ( 'NONE',  ( 11.26212378248529866, 3.384904051819500381, 8.663708617168998316 ) ) ;
#44366=CARTESIAN_POINT ( 'NONE',  ( 11.06795257254739973, 3.036453385827900142, 7.219770138693499817 ) ) ;
#44398=CARTESIAN_POINT ( 'NONE',  ( 11.33456651104149948, 4.112542507956200133, 8.635175889530000148 ) ) ;
#44419=ADVANCED_FACE ( 'NONE', ( #27762 ), #65489, .T. ) ;
#44468=CARTESIAN_POINT ( 'NONE',  ( 11.81056516821459823, 4.609678151793300316, 6.884701936848800052 ) ) ;
#44483=CARTESIAN_POINT ( 'NONE',  ( 11.68788784977535933, 3.014014167207800465, 7.556342205905759890 ) ) ;
#44494=CARTESIAN_POINT ( 'NONE',  ( 10.00551210286899995, 3.782771630962269871, 6.243812680477911492 ) ) ;
#44508=CARTESIAN_POINT ( 'NONE',  ( 8.872292071306626227, 4.874163933583397501, 7.537009346329285542 ) ) ;
#44529=CARTESIAN_POINT ( 'NONE',  ( 10.64391429142989765, 4.022379549362480766, 8.674673860548999471 ) ) ;
#44531=CARTESIAN_POINT ( 'NONE',  ( 9.228442991499999692, 3.919472480837189909, 8.776675254768999679 ) ) ;
#44543=FACE_OUTER_BOUND ( 'NONE', #57502, .T. ) ;
#44580=CARTESIAN_POINT ( 'NONE',  ( 8.874784697134998623, 4.545051930576500254, 8.343659109631099469 ) ) ;
#44586=CARTESIAN_POINT ( 'NONE',  ( 9.989267173155999657, 3.235527139800300045, 8.151477970733999712 ) ) ;
#44619=LINE ( 'NONE', #2296, #17275 ) ;
#44624=CARTESIAN_POINT ( 'NONE',  ( 10.78887616594230003, 3.613544262574699850, 8.718182393403999697 ) ) ;
#44710=CARTESIAN_POINT ( 'NONE',  ( 11.06379841651039797, 3.598362324325699912, 6.432302808027999141 ) ) ;
#44735=CARTESIAN_POINT ( 'NONE',  ( 9.833513540183332680, 2.750000000000000000, 7.663624617374469317 ) ) ;
#44741=CARTESIAN_POINT ( 'NONE',  ( 10.59610807141099897, 4.052703327804870526, 6.360477084256999980 ) ) ;
#44743=CARTESIAN_POINT ( 'NONE',  ( 10.83351354018309820, 2.750000000000000000, 7.663624617374469317 ) ) ;
#44793=CARTESIAN_POINT ( 'NONE',  ( 10.46029575260939026, 4.828733415692241238, 6.746534734305132730 ) ) ;
#44805=CARTESIAN_POINT ( 'NONE',  ( 10.69872335273220010, 4.349306362047499874, 6.559289673553299060 ) ) ;
#44806=VECTOR ( 'NONE', #42099, 1000.000000000000000 ) ;
#44820=CARTESIAN_POINT ( 'NONE',  ( 10.82035090130999855, 4.758726914843000699, 7.030721746772699454 ) ) ;
#44855=DIRECTION ( 'NONE',  ( 0.000000000000000000, 1.000000000000000000, 0.000000000000000000 ) ) ;
#44867=CARTESIAN_POINT ( 'NONE',  ( 11.55811496860034815, 5.045590851977999947, 8.035816473382100256 ) ) ;
#44870=CARTESIAN_POINT ( 'NONE',  ( 10.41488779216199845, 4.929030047862200448, 7.164969140522200242 ) ) ;
#44880=DIRECTION ( 'NONE',  ( 0.7071067617951957152, 0.000000000000000000, -0.7071068005778986532 ) ) ;
#44916=CARTESIAN_POINT ( 'NONE',  ( 9.506000818238998562, 2.989704013253000614, 6.967988282883199602 ) ) ;
#44921=CARTESIAN_POINT ( 'NONE',  ( 8.927455549952998837, 4.674761969675400586, 8.044430187461498960 ) ) ;
#44935=DIRECTION ( 'NONE',  ( 0.000000000000000000, -1.000000000000000000, 0.000000000000000000 ) ) ;
#44960=CARTESIAN_POINT ( 'NONE',  ( 10.66579975933730040, 5.208485784810999775, 7.915786590091300035 ) ) ;
#44978=VERTEX_POINT ( 'NONE', #18058 ) ;
#44993=CARTESIAN_POINT ( 'NONE',  ( 9.893930206848997599, 2.750000000000000000, 7.500000000000000000 ) ) ;
#44994=CYLINDRICAL_SURFACE ( 'NONE', #28140, 1.250000000000000222 ) ;
#45046=CARTESIAN_POINT ( 'NONE',  ( 11.55610404293055993, 3.497163090439000310, 6.476063885290000322 ) ) ;
#45081=CARTESIAN_POINT ( 'NONE',  ( 11.28533594839949750, 4.750012929834699804, 8.359517726022600570 ) ) ;
#45144=CARTESIAN_POINT ( 'NONE',  ( 10.57564694612699974, 3.068007311611700150, 7.128058497017000228 ) ) ;
#45161=CARTESIAN_POINT ( 'NONE',  ( 10.90346005378009941, 4.786957292481900161, 7.920222357891399945 ) ) ;
#45188=CARTESIAN_POINT ( 'NONE',  ( 8.796304629759626792, 4.535214477905362251, 6.807845768027799060 ) ) ;
#45213=CARTESIAN_POINT ( 'NONE',  ( 9.579025935145997650, 3.854158361175799907, 8.493766832166899761 ) ) ;
#45259=CARTESIAN_POINT ( 'NONE',  ( 8.771455549952998254, 4.888629236328500660, 8.216988513669100769 ) ) ;
#45265=CARTESIAN_POINT ( 'NONE',  ( 8.851468108405999402, 4.834201109053600121, 7.263744984161399465 ) ) ;
#45302=CARTESIAN_POINT ( 'NONE',  ( 10.14887885159599890, 5.269014563305000287, 7.651388779553199626 ) ) ;
#45338=CARTESIAN_POINT ( 'NONE',  ( 9.727263540182331525, 4.629523725463627670, 8.592232985442818105 ) ) ;
#45351=ORIENTED_EDGE ( 'NONE', *, *, #38305, .F. ) ;
#45389=CARTESIAN_POINT ( 'NONE',  ( 11.50687348028854906, 2.996540789803000315, 6.957450711802899868 ) ) ;
#45408=CARTESIAN_POINT ( 'NONE',  ( 8.995772571291155373, 2.998508658148200556, 6.923765800360898837 ) ) ;
#45418=CARTESIAN_POINT ( 'NONE',  ( 9.802263540183334456, 2.907767014557178786, 8.129523725463625894 ) ) ;
#45424=CARTESIAN_POINT ( 'NONE',  ( 10.94072200990529886, 2.922907051630999842, 7.875713849677398848 ) ) ;
#45426=CARTESIAN_POINT ( 'NONE',  ( 10.72934687351609639, 3.836375382625535124, 8.750000000000000000 ) ) ;
#45444=CARTESIAN_POINT ( 'NONE',  ( 11.12299956498149811, 5.207010770456999893, 7.174999999999999822 ) ) ;
#45463=CARTESIAN_POINT ( 'NONE',  ( 10.23976354018233259, 3.672815144550903632, 8.717465845835395299 ) ) ;
#45490=CARTESIAN_POINT ( 'NONE',  ( 10.35826357027499789, 4.850513154668600002, 7.335909308151700614 ) ) ;
#45519=ORIENTED_EDGE ( 'NONE', *, *, #63473, .F. ) ;
#45558=CARTESIAN_POINT ( 'NONE',  ( 10.28824205624999877, 3.639798001706899822, 6.562398383267799673 ) ) ;
#45603=CARTESIAN_POINT ( 'NONE',  ( 8.695468108405998819, 5.098602956001000663, 7.188863445572599709 ) ) ;
#45650=ORIENTED_EDGE ( 'NONE', *, *, #41065, .T. ) ;
#45676=VERTEX_POINT ( 'NONE', #35594 ) ;
#45680=CARTESIAN_POINT ( 'NONE',  ( 9.852263540182327972, 2.907767014557178342, 8.129523725463624118 ) ) ;
#45727=CARTESIAN_POINT ( 'NONE',  ( 11.51145123989532948, 4.605239108938600445, 6.331134574721999364 ) ) ;
#45732=CARTESIAN_POINT ( 'NONE',  ( 10.57149279008999798, 3.703313553258400059, 6.398515879103999993 ) ) ;
#45757=CARTESIAN_POINT ( 'NONE',  ( 9.729346873516670158, 3.836375382625535124, 8.750000000000000000 ) ) ;
#45763=CARTESIAN_POINT ( 'NONE',  ( 11.62579573085663043, 5.239377455231000624, 7.285547569258399747 ) ) ;
#45800=CARTESIAN_POINT ( 'NONE',  ( 10.17726354018233437, 4.629523725463628558, 8.592232985442819881 ) ) ;
#45827=CARTESIAN_POINT ( 'NONE',  ( 11.04333729122639873, 2.996877626170000308, 7.526388557597149642 ) ) ;
#45888=CARTESIAN_POINT ( 'NONE',  ( 11.06967835872019812, 3.245266201729799960, 7.975673736933100777 ) ) ;
#45890=CARTESIAN_POINT ( 'NONE',  ( 10.36422949779699820, 4.557226039164599563, 6.664331202173499946 ) ) ;
#45937=CARTESIAN_POINT ( 'NONE',  ( 9.733963142879998642, 5.117257953482000410, 7.735518817439499983 ) ) ;
#45995=ORIENTED_EDGE ( 'NONE', *, *, #9550, .F. ) ;
#46005=EDGE_CURVE ( 'NONE', #39090, #24276, #43118, .T. ) ;
#46017=DIRECTION ( 'NONE',  ( -1.000000000000000000, 0.000000000000000000, 0.000000000000000000 ) ) ;
#46038=CYLINDRICAL_SURFACE ( 'NONE', #7116, 1.250000000000000222 ) ;
#46039=ADVANCED_BREP_SHAPE_REPRESENTATION ( '', ( #30727, #9676 ), #38794 ) ;
#46055=CARTESIAN_POINT ( 'NONE',  ( 10.80502344389999791, 2.874741265256000489, 8.182900850620900002 ) ) ;
#46062=CARTESIAN_POINT ( 'NONE',  ( 10.21924205624999971, 3.689072563647699976, 6.690659495528099576 ) ) ;
#46066=CARTESIAN_POINT ( 'NONE',  ( 11.06456920625009843, 4.037149028919880145, 8.532838639935999225 ) ) ;
#46071=CARTESIAN_POINT ( 'NONE',  ( 11.48225819896749833, 2.879005208331999910, 7.288668995979000087 ) ) ;
#46098=AXIS2_PLACEMENT_3D ( 'NONE', #41869, #3764, #20889 ) ;
#46100=CARTESIAN_POINT ( 'NONE',  ( 9.989763540182750035, 4.327184855449099921, 6.282534154164604701 ) ) ;
#46103=CARTESIAN_POINT ( 'NONE',  ( 11.13349010443639919, 5.274453806861999716, 7.404690636538299842 ) ) ;
#46174=CARTESIAN_POINT ( 'NONE',  ( 10.33364828895399867, 4.760196147278000112, 7.084788038520800413 ) ) ;
#46189=CARTESIAN_POINT ( 'NONE',  ( 11.17056785386839834, 3.281375110759499947, 7.016391833292499491 ) ) ;
#46238=CARTESIAN_POINT ( 'NONE',  ( 10.13626717315599990, 3.235527139800300045, 8.151477970733999712 ) ) ;
#46283=SURFACE_STYLE_FILL_AREA ( #35453 ) ;
#46285=CARTESIAN_POINT ( 'NONE',  ( 8.872772138681998655, 3.575113238066399912, 8.559813987224998755 ) ) ;
#46325=CARTESIAN_POINT ( 'NONE',  ( 11.59999999999999964, 4.000000000000000000, 7.500000000000000000 ) ) ;
#46400=CARTESIAN_POINT ( 'NONE',  ( 10.52799293566599914, 4.806678152079100208, 6.510429574318199464 ) ) ;
#46411=CARTESIAN_POINT ( 'NONE',  ( 10.51414141025500015, 4.615773412711500434, 6.403245959303999868 ) ) ;
#46416=CARTESIAN_POINT ( 'NONE',  ( 10.81349144726329925, 3.261052100888700345, 8.542723541016000510 ) ) ;
#46440=ORIENTED_EDGE ( 'NONE', *, *, #54208, .F. ) ;
#46448=CARTESIAN_POINT ( 'NONE',  ( 10.30072469555899950, 4.570852684939899824, 8.487632181750699445 ) ) ;
#46504=CARTESIAN_POINT ( 'NONE',  ( 11.63825819896753977, 3.148796120250299868, 7.339530235223699073 ) ) ;
#46520=CARTESIAN_POINT ( 'NONE',  ( 11.60533460557258323, 4.184174550317700358, 6.374224726731999802 ) ) ;
#46581=CARTESIAN_POINT ( 'NONE',  ( 11.11123293495519881, 3.108594079907299967, 7.535834283667469435 ) ) ;
#46583=CARTESIAN_POINT ( 'NONE',  ( 10.13425461470299993, 3.159754091322399816, 7.286236678332599581 ) ) ;
#46617=CARTESIAN_POINT ( 'NONE',  ( 10.55569598648999907, 5.130952141044000214, 6.826612223887499553 ) ) ;
#46623=VERTEX_POINT ( 'NONE', #30864 ) ;
#46629=SURFACE_STYLE_USAGE ( .BOTH. , #25294 ) ;
#46631=CARTESIAN_POINT ( 'NONE',  ( 9.326684229509998758, 3.098260518542999886, 8.407331414124799451 ) ) ;
#46633=PRODUCT_DEFINITION ( 'UNKNOWN', '', #3895, #31792 ) ;
#46669=CARTESIAN_POINT ( 'NONE',  ( 8.807788144226000426, 4.090932644426789722, 6.546538158064899804 ) ) ;
#46689=CARTESIAN_POINT ( 'NONE',  ( 10.05041772631199848, 4.549624259497900169, 6.368647051112000135 ) ) ;
#46721=ORIENTED_EDGE ( 'NONE', *, *, #27930, .F. ) ;
#46746=CARTESIAN_POINT ( 'NONE',  ( 11.38678751119029897, 2.833702563575000166, 6.889827023674499173 ) ) ;
#46756=CARTESIAN_POINT ( 'NONE',  ( 11.35545123989519922, 4.475221369382300196, 6.582230774881299595 ) ) ;
#46761=CARTESIAN_POINT ( 'NONE',  ( 10.91195257254739914, 2.772832764353999835, 7.143100915737699452 ) ) ;
#46786=CARTESIAN_POINT ( 'NONE',  ( 9.916846873516377059, 3.231816600031355069, 6.500416447002274722 ) ) ;
#46789=CARTESIAN_POINT ( 'NONE',  ( 10.52226222744799955, 3.119510978356100139, 6.774721295617600170 ) ) ;
#46798=CARTESIAN_POINT ( 'NONE',  ( 11.16486084871730000, 5.207010770456999893, 7.825000000000000178 ) ) ;
#46846=CARTESIAN_POINT ( 'NONE',  ( 11.26902897915239876, 4.221721321201099997, 6.662660017635100296 ) ) ;
#46862=CARTESIAN_POINT ( 'NONE',  ( 10.71918447801630059, 5.140463864104999558, 7.525145395936648995 ) ) ;
#46874=CARTESIAN_POINT ( 'NONE',  ( 10.60441638348510018, 3.158410350011299883, 7.705001100909899314 ) ) ;
#46908=CARTESIAN_POINT ( 'NONE',  ( 11.20158531382784162, 4.272452942476327564, 8.749999999999998224 ) ) ;
#46923=CARTESIAN_POINT ( 'NONE',  ( 8.793822372493998785, 3.711294259598199918, 6.555546982591299532 ) ) ;
#46940=DIRECTION ( 'NONE',  ( 0.000000000000000000, -1.000000000000000000, 0.000000000000000000 ) ) ;
#46945=CARTESIAN_POINT ( 'NONE',  ( 11.59610237318921477, 3.189590050595149773, 7.825049231485562196 ) ) ;
#46956=CARTESIAN_POINT ( 'NONE',  ( 11.55811496860034815, 5.045590851977999947, 8.035816473382100256 ) ) ;
#46967=VERTEX_POINT ( 'NONE', #58632 ) ;
#46971=CARTESIAN_POINT ( 'NONE',  ( 9.909254614703000286, 2.760277452415999644, 7.184607557167700165 ) ) ;
#46982=CARTESIAN_POINT ( 'NONE',  ( 8.962753061708918167, 2.887246877270963630, 7.646523492023315605 ) ) ;
#46989=ORIENTED_EDGE ( 'NONE', *, *, #34292, .T. ) ;
#47004=CARTESIAN_POINT ( 'NONE',  ( 9.962988259787000089, 3.832626376493700082, 6.231784538167999266 ) ) ;
#47056=CLOSED_SHELL ( 'NONE', ( #67794, #14447, #41600, #25420, #21, #22036, #2056, #31160, #10555, #65644, #54291, #37576, #41315, #29288, #23122, #18954, #475, #33881, #7085, #44419, #47625, #49562, #5345, #36706, #9918, #17542, #53184, #43800, #63389, #18478, #22808 ) ) ;
#47089=CARTESIAN_POINT ( 'NONE',  ( 11.84388784977539899, 2.744254309011999737, 7.571757098260779806 ) ) ;
#47097=CARTESIAN_POINT ( 'NONE',  ( 10.60235971519489873, 4.605301262871499546, 8.506961598696999971 ) ) ;
#47105=CARTESIAN_POINT ( 'NONE',  ( 10.22687885159599830, 5.132709421626000079, 7.635128076451499268 ) ) ;
#47113=ORIENTED_EDGE ( 'NONE', *, *, #49386, .F. ) ;
#47190=CARTESIAN_POINT ( 'NONE',  ( 10.43210941423799909, 4.641185166475500168, 8.082391773166900606 ) ) ;
#47206=CARTESIAN_POINT ( 'NONE',  ( 11.18687482311539938, 5.057677595549000316, 7.072673169413499217 ) ) ;
#47221=CARTESIAN_POINT ( 'NONE',  ( 11.44133594839949986, 4.569506585117100173, 8.152656755002400502 ) ) ;
#47232=CARTESIAN_POINT ( 'NONE',  ( 10.89393020684959978, 2.750000000000000000, 7.500000000000000000 ) ) ;
#47261=CARTESIAN_POINT ( 'NONE',  ( 8.789886373836322875, 4.000007821194420110, 6.560153657526067938 ) ) ;
#47266=CARTESIAN_POINT ( 'NONE',  ( 9.300405316139999101, 3.786750623988900166, 6.518487389810699639 ) ) ;
#47300=CARTESIAN_POINT ( 'NONE',  ( 11.17901463001529905, 4.697110652903200290, 8.616511311517999872 ) ) ;
#47315=CARTESIAN_POINT ( 'NONE',  ( 9.757279731608999640, 4.114789684104199985, 8.774051692788999546 ) ) ;
#47335=CARTESIAN_POINT ( 'NONE',  ( 10.89393020684959978, 2.750000000000000000, 7.500000000000000000 ) ) ;
#47348=CARTESIAN_POINT ( 'NONE',  ( 10.57088779216199903, 5.183207142131999845, 7.073306690476799830 ) ) ;
#47389=ORIENTED_EDGE ( 'NONE', *, *, #10357, .F. ) ;
#47442=CARTESIAN_POINT ( 'NONE',  ( 10.93479632507519916, 4.557787252275099732, 6.465962698293999722 ) ) ;
#47447=CARTESIAN_POINT ( 'NONE',  ( 10.30072469555899950, 4.570852684939899824, 8.487632181750699445 ) ) ;
#47449=CARTESIAN_POINT ( 'NONE',  ( 11.37299956498129916, 2.792989229543000107, 7.825000000000000178 ) ) ;
#47480=CARTESIAN_POINT ( 'NONE',  ( 10.35410941423799791, 4.742797679580299963, 8.174686939644999484 ) ) ;
#47532=CARTESIAN_POINT ( 'NONE',  ( 11.59999999999999964, 3.182579051151299687, 7.825000000000000178 ) ) ;
#47537=CARTESIAN_POINT ( 'NONE',  ( 11.29364426047339975, 4.466097552695299733, 6.769896129503799820 ) ) ;
#47555=CARTESIAN_POINT ( 'NONE',  ( 11.01456785386839954, 3.053605396817899997, 6.863111178199799767 ) ) ;
#47565=CARTESIAN_POINT ( 'NONE',  ( 10.92028665956053324, 3.257584962274628460, 6.450604656432373574 ) ) ;
#47569=CARTESIAN_POINT ( 'NONE',  ( 11.12133729122639991, 3.134101783108900197, 7.522778681411049995 ) ) ;
#47608=CARTESIAN_POINT ( 'NONE',  ( 8.795853127542962113, 4.029789221522053211, 6.554146822010631368 ) ) ;
#47614=CARTESIAN_POINT ( 'NONE',  ( 8.819151519676999840, 4.021721698617580110, 6.495824366094999469 ) ) ;
#47625=ADVANCED_FACE ( 'NONE', ( #3523 ), #16636, .F. ) ;
#47639=ORIENTED_EDGE ( 'NONE', *, *, #68611, .T. ) ;
#47646=CARTESIAN_POINT ( 'NONE',  ( 10.63880513895979973, 5.150451045932999961, 8.139542779846600240 ) ) ;
#47658=CARTESIAN_POINT ( 'NONE',  ( 9.073392757686999488, 4.863450031739999346, 6.556157624301499176 ) ) ;
#47693=CARTESIAN_POINT ( 'NONE',  ( 9.557721904870000174, 5.115452802765999785, 6.873781641694999500 ) ) ;
#47712=CARTESIAN_POINT ( 'NONE',  ( 8.599999952505998024, 4.000000000000000000, 7.500000000000000000 ) ) ;
#47738=CARTESIAN_POINT ( 'NONE',  ( 11.59999999999999964, 4.187315255316414131, 8.553266857751330221 ) ) ;
#47748=DIRECTION ( 'NONE',  ( 0.000000000000000000, 0.000000000000000000, 1.000000000000000000 ) ) ;
#47772=EDGE_CURVE ( 'NONE', #43157, #39090, #15870, .T. ) ;
#47800=CARTESIAN_POINT ( 'NONE',  ( 10.13662282008599824, 4.594711216567399781, 6.540749699823199315 ) ) ;
#47882=CARTESIAN_POINT ( 'NONE',  ( 10.97364560330029981, 4.265439025801100570, 8.324524538096799375 ) ) ;
#47896=CARTESIAN_POINT ( 'NONE',  ( 10.42795525820099911, 3.905250696375530239, 8.498986197235801399 ) ) ;
#47908=EDGE_LOOP ( 'NONE', ( #55105, #40430, #25323, #32776, #54515 ) ) ;
#47909=CARTESIAN_POINT ( 'NONE',  ( 11.46179707368349909, 3.501542828836900156, 8.370914060838998694 ) ) ;
#47921=CARTESIAN_POINT ( 'NONE',  ( 11.08482133862618113, 4.942979055179590908, 6.626386139742055370 ) ) ;
#47955=CARTESIAN_POINT ( 'NONE',  ( 9.906292290062998163, 4.749786674456300872, 7.935348007132199122 ) ) ;
#47983=ORIENTED_EDGE ( 'NONE', *, *, #162, .F. ) ;
#47984=CARTESIAN_POINT ( 'NONE',  ( 11.59456039236534330, 5.314711678001000195, 7.436015812896529020 ) ) ;
#48000=CARTESIAN_POINT ( 'NONE',  ( 8.820101285864000218, 3.176316400316700150, 8.478738839062499366 ) ) ;
#48008=CARTESIAN_POINT ( 'NONE',  ( 9.910787105781626138, 4.756649759826824919, 7.939332914627393656 ) ) ;
#48029=CARTESIAN_POINT ( 'NONE',  ( 10.34292546752099895, 2.723846966067000164, 7.588418444866789514 ) ) ;
#48036=DIRECTION ( 'NONE',  ( -0.5000000000000150990, -0.08222066253632250021, 0.8621135439442261239 ) ) ;
#48120=CARTESIAN_POINT ( 'NONE',  ( 8.849999778957998942, 4.000000000000000000, 7.500000000000000000 ) ) ;
#48125=CARTESIAN_POINT ( 'NONE',  ( 10.82035090130999855, 4.758726914843000699, 7.030721746772699454 ) ) ;
#48132=CARTESIAN_POINT ( 'NONE',  ( 10.22272469555899832, 4.639546521693399761, 8.606479382885998675 ) ) ;
#48137=EDGE_CURVE ( 'NONE', #14332, #34343, #57056, .T. ) ;
#48159=CARTESIAN_POINT ( 'NONE',  ( 11.39975833414730033, 4.796537143354000499, 7.825000000000000178 ) ) ;
#48203=ORIENTED_EDGE ( 'NONE', *, *, #60777, .T. ) ;
#48212=CARTESIAN_POINT ( 'NONE',  ( 10.57564694612699974, 3.068007311611700150, 7.128058497017000228 ) ) ;
#48228=CARTESIAN_POINT ( 'NONE',  ( 11.30579707368350029, 3.365167912142600137, 8.609190966793999422 ) ) ;
#48241=CARTESIAN_POINT ( 'NONE',  ( 11.78179573085659904, 4.973133828855400118, 7.331616337578100051 ) ) ;
#48280=B_SPLINE_CURVE_WITH_KNOTS ( 'NONE', 3,
 ( #5168, #37329, #31065, #42922, #20906, #41542, #42243, #52718, #10754, #15662, #62854, #63549, #20560, #52373, #68099, #26158, #58306, #58653 ),
 .UNSPECIFIED., .F., .F.,
 ( 4, 2, 2, 2, 2, 2, 2, 2, 4 ),
 ( 0.000000000000000000, 0.1250000000000000000, 0.2500000000000000000, 0.3750000000000000000, 0.5000000000000000000, 0.6250000000000000000, 0.7500000000000000000, 0.8750000000000000000, 1.000000000000000000 ),
 .UNSPECIFIED. ) ;
#48291=CARTESIAN_POINT ( 'NONE',  ( 9.247734463322998977, 4.090312251411040378, 6.637705594503099604 ) ) ;
#48304=CARTESIAN_POINT ( 'NONE',  ( 11.39210538575740017, 4.842454415653899780, 7.701417844014099678 ) ) ;
#48323=CARTESIAN_POINT ( 'NONE',  ( 10.81013259637009938, 2.968328969579000276, 6.937848198857199833 ) ) ;
#48339=CARTESIAN_POINT ( 'NONE',  ( 10.69837472757367713, 3.526507217177279330, 6.765225077371590956 ) ) ;
#48347=CARTESIAN_POINT ( 'NONE',  ( 9.708153928322625248, 3.619812067603167538, 6.711971190259613529 ) ) ;
#48371=CARTESIAN_POINT ( 'NONE',  ( 10.03696314287999947, 5.117257953482000410, 7.735518817439499983 ) ) ;
#48375=CARTESIAN_POINT ( 'NONE',  ( 10.14393020684899938, 5.250000000000000000, 7.500000000000000000 ) ) ;
#48432=ORIENTED_EDGE ( 'NONE', *, *, #53352, .F. ) ;
#48445=B_SPLINE_CURVE_WITH_KNOTS ( 'NONE', 3,
 ( #22397, #38481, #7011, #43736, #53534, #5626, #32897, #65032, #59804, #28345 ),
 .UNSPECIFIED., .F., .F.,
 ( 4, 2, 2, 2, 4 ),
 ( 0.000000000000000000, 0.2500000000000000000, 0.5000000000000000000, 0.7500000000000000000, 1.000000000000000000 ),
 .UNSPECIFIED. ) ;
#48472=CARTESIAN_POINT ( 'NONE',  ( 10.73724174883999893, 3.975468761016990094, 6.608211443991299561 ) ) ;
#48504=CARTESIAN_POINT ( 'NONE',  ( 11.16486084871730000, 5.207010770456999893, 7.825000000000000178 ) ) ;
#48539=CARTESIAN_POINT ( 'NONE',  ( 11.37299956498129916, 2.792989229543000107, 7.825000000000000178 ) ) ;
#48563=CARTESIAN_POINT ( 'NONE',  ( 11.77359063708300013, 4.955772084214699724, 7.231278212164300001 ) ) ;
#48577=CARTESIAN_POINT ( 'NONE',  ( 11.03502897915239878, 4.327133900127000388, 6.264564938179000286 ) ) ;
#48593=CARTESIAN_POINT ( 'NONE',  ( 11.60948876160955479, 3.304472173606900043, 6.776679950459500112 ) ) ;
#48643=CARTESIAN_POINT ( 'NONE',  ( 9.273063610504998167, 4.355629271815800507, 6.709281487801199262 ) ) ;
#48654=CARTESIAN_POINT ( 'NONE',  ( 10.62903166480609940, 3.135947233695900227, 7.439078678739090122 ) ) ;
#48669=CARTESIAN_POINT ( 'NONE',  ( 11.02301463001509774, 4.547357026650399980, 8.376661845795100092 ) ) ;
#48688=VECTOR ( 'NONE', #51942, 1000.000000000000000 ) ;
#48689=CARTESIAN_POINT ( 'NONE',  ( 10.59991360228957191, 3.150711065775904984, 7.706876553803710728 ) ) ;
#48691=B_SPLINE_CURVE_WITH_KNOTS ( 'NONE', 3,
 ( #58400, #63639, #47921, #5596, #20310, #25902, #53160, #52467, #26940, #47232 ),
 .UNSPECIFIED., .F., .F.,
 ( 4, 2, 2, 2, 4 ),
 ( 0.000000000000000000, 0.2500000000000001665, 0.5000000000000003331, 0.7500000000000001110, 1.000000000000000000 ),
 .UNSPECIFIED. ) ;
#48701=CARTESIAN_POINT ( 'NONE',  ( 10.28877584378239796, 4.466001735846802490, 6.763172759027206382 ) ) ;
#48722=CARTESIAN_POINT ( 'NONE',  ( 11.43856039236529831, 5.032284719763000069, 7.449760924956519759 ) ) ;
#48725=CARTESIAN_POINT ( 'NONE',  ( 10.34091290906799898, 3.277531639390499851, 6.615820196229499572 ) ) ;
#48748=ORIENTED_EDGE ( 'NONE', *, *, #41103, .F. ) ;
#48763=CARTESIAN_POINT ( 'NONE',  ( 11.36486084871759950, 2.792989229543000107, 7.174999999999999822 ) ) ;
#48770=CARTESIAN_POINT ( 'NONE',  ( 10.18144474310099845, 5.015709705366000470, 7.007085334055199510 ) ) ;
#48800=CARTESIAN_POINT ( 'NONE',  ( 9.843930206850000530, 2.750000000000000000, 7.500000000000000000 ) ) ;
#48817=CARTESIAN_POINT ( 'NONE',  ( 10.57102344389999971, 3.237334151971200225, 7.962849245488699879 ) ) ;
#48854=CARTESIAN_POINT ( 'NONE',  ( 10.08351354018237345, 5.250000000000000888, 7.336375382625531572 ) ) ;
#48862=CARTESIAN_POINT ( 'NONE',  ( 10.42363156114900136, 3.315688435009791935, 6.424401362931539516 ) ) ;
#48908=CARTESIAN_POINT ( 'NONE',  ( 10.82179975933729921, 4.948878321068100661, 7.826467126457498757 ) ) ;
#48922=CARTESIAN_POINT ( 'NONE',  ( 11.23195122972050086, 4.507250159094099651, 8.673036084990000560 ) ) ;
#48939=CARTESIAN_POINT ( 'NONE',  ( 11.41256651104150066, 4.098999650273559503, 8.498573944230598087 ) ) ;
#48996=CARTESIAN_POINT ( 'NONE',  ( 11.61364291764652812, 3.140345330584100036, 7.606265891492399511 ) ) ;
#49014=CARTESIAN_POINT ( 'NONE',  ( 10.68546886766499959, 3.433493735705800187, 8.529286361367999447 ) ) ;
#49029=SHAPE_REPRESENTATION_RELATIONSHIP ( 'NONE' , 'NONE' ,  #24587, #46039 ) ;
#49032=CARTESIAN_POINT ( 'NONE',  ( 10.37837607040047594, 4.867967756586605965, 7.603545367532808186 ) ) ;
#49062=CARTESIAN_POINT ( 'NONE',  ( 10.89835090130999973, 4.878966983716200190, 6.956352367771000189 ) ) ;
#49064=CARTESIAN_POINT ( 'NONE',  ( 10.08762143724499794, 4.758411336345700349, 8.353549467159899322 ) ) ;
#49072=CARTESIAN_POINT ( 'NONE',  ( 11.59999999999999964, 4.000000000000000000, 7.500000000000000000 ) ) ;
#49109=CARTESIAN_POINT ( 'NONE',  ( 9.936596320338999533, 2.942832934044000037, 7.931430460958599049 ) ) ;
#49115=CARTESIAN_POINT ( 'NONE',  ( 9.737988259786000356, 3.886559292927400211, 6.640442468193600511 ) ) ;
#49123=B_SPLINE_CURVE_WITH_KNOTS ( 'NONE', 3,
 ( #50710, #35664, #18899, #56979 ),
 .UNSPECIFIED., .F., .F.,
 ( 4, 4 ),
 ( 0.000000000000000000, 1.000000000000000000 ),
 .UNSPECIFIED. ) ;
#49151=DIRECTION ( 'NONE',  ( 1.000000000000000000, 0.000000000000000000, 0.000000000000000000 ) ) ;
#49154=CARTESIAN_POINT ( 'NONE',  ( 10.69568717260499824, 3.533932086969799879, 6.739296831621899742 ) ) ;
#49237=AXIS2_PLACEMENT_3D ( 'NONE', #66466, #62257, #14032 ) ;
#49242=CARTESIAN_POINT ( 'NONE',  ( 11.09256785386839894, 3.167490253789400523, 6.939751505745099358 ) ) ;
#49259=CARTESIAN_POINT ( 'NONE',  ( 10.12841772631199966, 4.490588993294299947, 6.490165927606000196 ) ) ;
#49274=CARTESIAN_POINT ( 'NONE',  ( 11.16641369783139837, 3.949373449607799902, 6.497808498716000081 ) ) ;
#49337=CARTESIAN_POINT ( 'NONE',  ( 11.41672066707849886, 4.741156262620799922, 7.948314604624900248 ) ) ;
#49338=VECTOR ( 'NONE', #1995, 1000.000000000000114 ) ;
#49350=CARTESIAN_POINT ( 'NONE',  ( 10.76857802013509868, 2.825431102905000103, 7.527343341769989316 ) ) ;
#49369=CARTESIAN_POINT ( 'NONE',  ( 10.52606775832647656, 3.656473597603909553, 8.303790528164435969 ) ) ;
#49378=CARTESIAN_POINT ( 'NONE',  ( 9.657495633957626779, 3.225830943932614048, 7.092330352431370777 ) ) ;
#49386=EDGE_CURVE ( 'NONE', #21433, #37252, #51399, .T. ) ;
#49401=CARTESIAN_POINT ( 'NONE',  ( 11.18412378248529926, 3.450971646934100079, 8.538714411016998795 ) ) ;
#49403=CARTESIAN_POINT ( 'NONE',  ( 9.960975701332998256, 4.837683410033799980, 6.724099908144899551 ) ) ;
#49452=CARTESIAN_POINT ( 'NONE',  ( 9.837292290062999101, 4.868609929059700470, 8.004340253666999416 ) ) ;
#49454=CARTESIAN_POINT ( 'NONE',  ( 9.539763540182331525, 4.327184855449099921, 6.282534154164603812 ) ) ;
#49457=CARTESIAN_POINT ( 'NONE',  ( 8.902126402770997871, 4.811247217215600003, 7.805918119494599239 ) ) ;
#49493=CARTESIAN_POINT ( 'NONE',  ( 11.04298866606778162, 3.494581883632823516, 8.213191510014491215 ) ) ;
#49532=COLOUR_RGB ( '', 0.66274510, 0.83137255, 0.94901961) ;
#49556=CARTESIAN_POINT ( 'NONE',  ( 11.37077408945317103, 2.816736291912564027, 7.086869749530762874 ) ) ;
#49562=ADVANCED_FACE ( 'NONE', ( #19234 ), #1599, .F. ) ;
#49591=CARTESIAN_POINT ( 'NONE',  ( 11.56025819896753859, 3.013900664291200293, 7.314099615601099558 ) ) ;
#49623=CARTESIAN_POINT ( 'NONE',  ( 10.74379975933729980, 5.078682052940000524, 7.871126858273000515 ) ) ;
#49652=CARTESIAN_POINT ( 'NONE',  ( 9.211801307670125283, 4.111875952999886508, 8.755178286007271993 ) ) ;
#49672=CARTESIAN_POINT ( 'NONE',  ( 11.16486084871730000, 5.207010770456999893, 7.825000000000000178 ) ) ;
#49687=B_SPLINE_CURVE_WITH_KNOTS ( 'NONE', 3,
 ( #4034, #25374, #1217, #32012 ),
 .UNSPECIFIED., .F., .F.,
 ( 4, 4 ),
 ( 0.000000000000000000, 1.000000000000000000 ),
 .UNSPECIFIED. ) ;
#49691=CARTESIAN_POINT ( 'NONE',  ( 11.85979573085659844, 4.840012015667699785, 7.354650721737899133 ) ) ;
#49703=CARTESIAN_POINT ( 'NONE',  ( 10.81524174883999834, 3.971581146373189597, 6.466884287543999577 ) ) ;
#49717=CARTESIAN_POINT ( 'NONE',  ( 10.08521345716899908, 4.924890298941200228, 6.659120737011199331 ) ) ;
#49753=CARTESIAN_POINT ( 'NONE',  ( 11.48011496860029901, 4.919769165942200040, 7.971338736265699332 ) ) ;
#49755=CARTESIAN_POINT ( 'NONE',  ( 10.29025461470400060, 2.893436332050999926, 7.218483930889299849 ) ) ;
#49764=PLANE ( 'NONE',  #36587 ) ;
#49806=CARTESIAN_POINT ( 'NONE',  ( 9.128076168957999670, 3.490299597736799875, 6.634524523592600254 ) ) ;
#49808=CARTESIAN_POINT ( 'NONE',  ( 9.633513540182331525, 5.250000000000001776, 7.336375382625529795 ) ) ;
#49811=CARTESIAN_POINT ( 'NONE',  ( 9.560684229509998744, 3.388828644390000200, 8.114961396014498618 ) ) ;
#49845=CARTESIAN_POINT ( 'NONE',  ( 10.79683585285767577, 4.539293524411616154, 6.812066793331982950 ) ) ;
#49849=CARTESIAN_POINT ( 'NONE',  ( 10.09964828895399869, 5.121614868497999851, 6.887384543790600056 ) ) ;
#49864=ORIENTED_EDGE ( 'NONE', *, *, #10357, .T. ) ;
#49865=VECTOR ( 'NONE', #42660, 1000.000000000000000 ) ;
#49869=CARTESIAN_POINT ( 'NONE',  ( 11.32299956498189886, 2.792989229543000107, 7.825000000000000178 ) ) ;
#49874=EDGE_CURVE ( 'NONE', #1219, #6746, #57004, .T. ) ;
#49885=CARTESIAN_POINT ( 'NONE',  ( 9.654346873515669003, 5.250000000000002665, 7.663624617374463988 ) ) ;
#49894=CARTESIAN_POINT ( 'NONE',  ( 10.51927318630899855, 4.756452637475340417, 6.473854711408037588 ) ) ;
#49934=CARTESIAN_POINT ( 'NONE',  ( 11.80233327354039830, 2.898463260143000042, 8.220500279733599314 ) ) ;
#49940=CARTESIAN_POINT ( 'NONE',  ( 10.28026357027499849, 4.985299147223100746, 7.309904858193100097 ) ) ;
#49963=CARTESIAN_POINT ( 'NONE',  ( 9.823096873516664829, 2.782534154164606921, 7.827184855449101697 ) ) ;
#49970=CARTESIAN_POINT ( 'NONE',  ( 11.58071932425156980, 3.832730087831799803, 6.371589232479998977 ) ) ;
#49984=ORIENTED_EDGE ( 'NONE', *, *, #64540, .T. ) ;
#50032=B_SPLINE_CURVE_WITH_KNOTS ( 'NONE', 3,
 ( #1389, #18167, #6977, #65354 ),
 .UNSPECIFIED., .F., .F.,
 ( 4, 4 ),
 ( 0.000000000000000000, 0.1836163425310829433 ),
 .UNSPECIFIED. ) ;
#50041=CARTESIAN_POINT ( 'NONE',  ( 10.84641504065830020, 4.804462279649600376, 8.099826052678000821 ) ) ;
#50051=VERTEX_POINT ( 'NONE', #61513 ) ;
#50058=CARTESIAN_POINT ( 'NONE',  ( 11.02812378248509795, 3.583106837161099900, 8.288725998710999576 ) ) ;
#50068=ORIENTED_EDGE ( 'NONE', *, *, #53664, .T. ) ;
#50075=CARTESIAN_POINT ( 'NONE',  ( 9.393930206848999376, 2.750000000000000000, 7.500000000000000000 ) ) ;
#50104=CARTESIAN_POINT ( 'NONE',  ( 11.23078751119019891, 3.084247107206000038, 7.020904658857499925 ) ) ;
#50108=CARTESIAN_POINT ( 'NONE',  ( 9.099784697134998268, 4.619613413415000203, 8.459069166353199165 ) ) ;
#50114=B_SPLINE_CURVE_WITH_KNOTS ( 'NONE', 3,
 ( #11418, #18062, #33107, #49869 ),
 .UNSPECIFIED., .F., .F.,
 ( 4, 4 ),
 ( 0.000000000000000000, 1.000000000000000000 ),
 .UNSPECIFIED. ) ;
#50138=B_SPLINE_CURVE_WITH_KNOTS ( 'NONE', 3,
 ( #37454, #41670, #52851, #57740, #30842, #52153, #36425, #31197, #5294, #9851, #68569, #31877, #20691, #26973, #15450, #64011, #37118, #42021 ),
 .UNSPECIFIED., .F., .F.,
 ( 4, 2, 2, 2, 2, 2, 2, 2, 4 ),
 ( 0.000000000000000000, 0.1250000000000000000, 0.2500000000000000000, 0.3750000000000000000, 0.5000000000000000000, 0.6250000000000000000, 0.7500000000000000000, 0.8750000000000000000, 1.000000000000000000 ),
 .UNSPECIFIED. ) ;
#50155=CARTESIAN_POINT ( 'NONE',  ( 10.13922949779699856, 4.633452903845899584, 6.550014196338999284 ) ) ;
#50158=CARTESIAN_POINT ( 'NONE',  ( 9.393930206848999376, 2.750000000000000000, 7.500000000000000000 ) ) ;
#50161=CARTESIAN_POINT ( 'NONE',  ( 9.003442991499998271, 3.945420918055940085, 8.365291319916600798 ) ) ;
#50179=CARTESIAN_POINT ( 'NONE',  ( 9.393930206848999376, 2.750000000000000000, 7.500000000000000000 ) ) ;
#50199=CIRCLE ( 'NONE', #26739, 0.7499999936418002555 ) ;
#50200=CARTESIAN_POINT ( 'NONE',  ( 10.69041504065829962, 5.024558373595999328, 8.263934892306599167 ) ) ;
#50286=CARTESIAN_POINT ( 'NONE',  ( 11.69559063708295987, 5.086518862378000883, 7.194517870904999945 ) ) ;
#50314=CARTESIAN_POINT ( 'NONE',  ( 9.739763540183334456, 3.672815144550903632, 8.717465845835395299 ) ) ;
#50320=CARTESIAN_POINT ( 'NONE',  ( 10.35410941423799791, 4.742797679580299963, 8.174686939644999484 ) ) ;
#50348=CARTESIAN_POINT ( 'NONE',  ( 9.333766445374624965, 2.750000000000000444, 7.659651991919251834 ) ) ;
#50386=CARTESIAN_POINT ( 'NONE',  ( 10.62487750876920067, 3.456442671114800191, 6.656497609330299881 ) ) ;
#50445=CARTESIAN_POINT ( 'NONE',  ( 8.922480666858998433, 4.380700808321400075, 6.423523106103999680 ) ) ;
#50458=CARTESIAN_POINT ( 'NONE',  ( 8.849999778957998942, 4.000000000000000000, 6.500000166194499940 ) ) ;
#50492=CARTESIAN_POINT ( 'NONE',  ( 9.885938025973999288, 3.406370524467499994, 8.475365825607600101 ) ) ;
#50495=CARTESIAN_POINT ( 'NONE',  ( 9.414763540182331525, 2.782534154164605589, 7.172815144550902744 ) ) ;
#50500=CARTESIAN_POINT ( 'NONE',  ( 9.130088727410999638, 3.136022381937999981, 7.427538838030949719 ) ) ;
#50556=CARTESIAN_POINT ( 'NONE',  ( 10.78887616594230003, 3.613544262574699850, 8.718182393403999697 ) ) ;
#50575=AXIS2_PLACEMENT_3D ( 'NONE', #15009, #9075, #20599 ) ;
#50578=PRODUCT ( 'Terminal Screw 2', 'Terminal Screw 2', '', ( #53975 ) ) ;
#50582=EDGE_CURVE ( 'NONE', #10441, #19590, #63626, .T. ) ;
#50620=CARTESIAN_POINT ( 'NONE',  ( 9.965950584426998660, 4.344127791340399725, 8.295791434820300125 ) ) ;
#50630=CARTESIAN_POINT ( 'NONE',  ( 10.76841504065829902, 4.914510326623699576, 8.181880472491098288 ) ) ;
#50657=CARTESIAN_POINT ( 'NONE',  ( 9.760596873516666605, 3.370476274536378547, 8.592232985442823434 ) ) ;
#50664=CARTESIAN_POINT ( 'NONE',  ( 10.96533729122639933, 2.859653469230999612, 7.529998433785960010 ) ) ;
#50710=CARTESIAN_POINT ( 'NONE',  ( 11.37299956498129916, 2.792989229543000107, 7.825000000000000178 ) ) ;
#50732=CARTESIAN_POINT ( 'NONE',  ( 10.50180110216399854, 3.143606124884799957, 8.023010882787499298 ) ) ;
#50745=CARTESIAN_POINT ( 'NONE',  ( 11.15278751119019773, 3.209519379020799867, 7.086443476450299706 ) ) ;
#50761=CARTESIAN_POINT ( 'NONE',  ( 10.06927318630900103, 4.756452637475338641, 6.473854711408034923 ) ) ;
#50781=CARTESIAN_POINT ( 'NONE',  ( 10.57435795695566583, 5.250000000000000000, 7.192559817601734906 ) ) ;
#50799=CARTESIAN_POINT ( 'NONE',  ( 9.781659112603998452, 3.563556310301200014, 6.595367916746299741 ) ) ;
#50840=CARTESIAN_POINT ( 'NONE',  ( 9.303367640780999537, 4.538247246588100303, 8.506987760366000018 ) ) ;
#50852=CARTESIAN_POINT ( 'NONE',  ( 8.710288521113000115, 3.647046440108700160, 6.715449042252499723 ) ) ;
#50871=AXIS2_PLACEMENT_3D ( 'NONE', #30051, #40513, #62180 ) ;
#50882=CARTESIAN_POINT ( 'NONE',  ( 10.37041638348499895, 2.758294858530000226, 7.802464414828100381 ) ) ;
#50930=EDGE_LOOP ( 'NONE', ( #25100, #11831, #22005, #41380, #34609 ) ) ;
#50961=CARTESIAN_POINT ( 'NONE',  ( 10.06726717315599906, 3.340104753140699767, 8.062357722167599050 ) ) ;
#50973=CARTESIAN_POINT ( 'NONE',  ( 10.44841638348500013, 2.891666689023999925, 7.769976643522699788 ) ) ;
#51005=CARTESIAN_POINT ( 'NONE',  ( 11.70379573085659786, 5.106255642043000087, 7.308581953418300081 ) ) ;
#51061=ORIENTED_EDGE ( 'NONE', *, *, #24106, .T. ) ;
#51074=CARTESIAN_POINT ( 'NONE',  ( 11.73256516821459883, 4.706297556651700020, 6.787191910456499500 ) ) ;
#51085=DIRECTION ( 'NONE',  ( 0.000000000000000000, 0.8514543052404082157, -0.5244287998266055073 ) ) ;
#51088=CARTESIAN_POINT ( 'NONE',  ( 10.61257802013489737, 3.108115747127599970, 7.520762592984879369 ) ) ;
#51100=VERTEX_POINT ( 'NONE', #56533 ) ;
#51136=CARTESIAN_POINT ( 'NONE',  ( 11.23589666366019912, 3.960399224793059947, 6.608753462694600067 ) ) ;
#51138=CARTESIAN_POINT ( 'NONE',  ( 9.857646554150999663, 4.486270025758400060, 6.621146336197599958 ) ) ;
#51188=CARTESIAN_POINT ( 'NONE',  ( 9.911267173156000254, 3.130949526459800403, 8.240598219300300897 ) ) ;
#51197=CARTESIAN_POINT ( 'NONE',  ( 11.59999999999999787, 3.707964997157290110, 6.463642954493290738 ) ) ;
#51226=CARTESIAN_POINT ( 'NONE',  ( 10.49349279008999858, 3.667611644732699627, 6.265968249244999733 ) ) ;
#51260=CARTESIAN_POINT ( 'NONE',  ( 11.59999999999999609, 4.247874375640066091, 8.548800951397311110 ) ) ;
#51262=CARTESIAN_POINT ( 'NONE',  ( 9.643930206848999376, 5.250000000000000000, 7.500000000000000000 ) ) ;
#51296=CARTESIAN_POINT ( 'NONE',  ( 8.736413463905998711, 4.084156314540369870, 6.617590440947399344 ) ) ;
#51308=CARTESIAN_POINT ( 'NONE',  ( 11.18923293495519822, 2.967327562101000016, 7.541513160549049744 ) ) ;
#51315=CARTESIAN_POINT ( 'NONE',  ( 10.91610672858429965, 3.088399709291500095, 8.185766014210599906 ) ) ;
#51330=CARTESIAN_POINT ( 'NONE',  ( 9.022188178962252891, 3.408865106546500989, 6.476088678109181984 ) ) ;
#51339=ORIENTED_EDGE ( 'NONE', *, *, #10561, .F. ) ;
#51340=CARTESIAN_POINT ( 'NONE',  ( 9.604346873516666605, 5.250000000000001776, 7.663624617374461323 ) ) ;
#51347=CARTESIAN_POINT ( 'NONE',  ( 11.20733594839949809, 4.840266102192999575, 8.462948211532999920 ) ) ;
#51353=FACE_OUTER_BOUND ( 'NONE', #56412, .T. ) ;
#51386=CARTESIAN_POINT ( 'NONE',  ( 10.13559687351566829, 5.092232985442826099, 8.129523725463617012 ) ) ;
#51399=LINE ( 'NONE', #28710, #58757 ) ;
#51414=CARTESIAN_POINT ( 'NONE',  ( 11.19102897915239936, 4.256858847510399890, 6.529961657816500065 ) ) ;
#51429=CARTESIAN_POINT ( 'NONE',  ( 11.41672066707849886, 4.741156262620799922, 7.948314604624900248 ) ) ;
#51473=CARTESIAN_POINT ( 'NONE',  ( 10.82035090130999855, 4.758726914843000699, 7.030721746772699454 ) ) ;
#51475=CARTESIAN_POINT ( 'NONE',  ( 9.832317406968998696, 4.186809223719299311, 6.513113677132300161 ) ) ;
#51518=CARTESIAN_POINT ( 'NONE',  ( 8.999417874593998334, 2.949199072237000063, 7.053287723251499663 ) ) ;
#51533=CARTESIAN_POINT ( 'NONE',  ( 11.07299956498199833, 5.207010770456999893, 7.174999999999999822 ) ) ;
#51549=CARTESIAN_POINT ( 'NONE',  ( 11.59999999999999964, 4.000000000000000000, 7.500000000000000000 ) ) ;
#51576=CARTESIAN_POINT ( 'NONE',  ( 10.29657053952199952, 3.497746311184500190, 8.675184076076000395 ) ) ;
#51598=EDGE_LOOP ( 'NONE', ( #18061, #2728, #46989, #7530 ) ) ;
#51635=CARTESIAN_POINT ( 'NONE',  ( 11.75203632436369894, 2.890282938442000127, 7.759151359668400083 ) ) ;
#51641=CARTESIAN_POINT ( 'NONE',  ( 10.04193802597399987, 3.549239910423600097, 8.240623579255899500 ) ) ;
#51645=CARTESIAN_POINT ( 'NONE',  ( 11.60477869730532774, 3.532552483170099844, 8.421761806503198500 ) ) ;
#51650=CARTESIAN_POINT ( 'NONE',  ( 11.47810404293059960, 3.436653965247300047, 6.352848032645000309 ) ) ;
#51678=CARTESIAN_POINT ( 'NONE',  ( 9.843930206850000530, 2.750000000000000000, 7.500000000000000000 ) ) ;
#51681=CARTESIAN_POINT ( 'NONE',  ( 11.57656516821460890, 4.899536366368299589, 6.592171857671999646 ) ) ;
#51712=AXIS2_PLACEMENT_3D ( 'NONE', #41930, #26546, #4510 ) ;
#51737=CARTESIAN_POINT ( 'NONE',  ( 10.62903166480609940, 3.135947233695900227, 7.439078678739090122 ) ) ;
#51753=CARTESIAN_POINT ( 'NONE',  ( 11.50687348028854906, 2.996540789803000315, 6.957450711802899868 ) ) ;
#51768=CARTESIAN_POINT ( 'NONE',  ( 11.39210538575740017, 4.842454415653899780, 7.701417844014099678 ) ) ;
#51797=CARTESIAN_POINT ( 'NONE',  ( 10.59393020684899867, 5.250000000000000000, 7.500000000000000000 ) ) ;
#51799=CARTESIAN_POINT ( 'NONE',  ( 11.25361999289386539, 3.455907502640804374, 8.657883396625686956 ) ) ;
#51800=CARTESIAN_POINT ( 'NONE',  ( 11.59999999999999964, 3.182579051151299687, 7.825000000000000178 ) ) ;
#51813=CARTESIAN_POINT ( 'NONE',  ( 9.551684229509998403, 3.388828644390000200, 8.114961396014498618 ) ) ;
#51846=CARTESIAN_POINT ( 'NONE',  ( 10.97124174884019965, 3.963805917081910213, 6.184229974648999928 ) ) ;
#51861=CARTESIAN_POINT ( 'NONE',  ( 8.898101285863999621, 3.264788442324599860, 8.373612278672599274 ) ) ;
#51867=CARTESIAN_POINT ( 'NONE',  ( 11.53828694957233481, 4.309606737214646266, 6.264939056470322676 ) ) ;
#51917=CARTESIAN_POINT ( 'NONE',  ( 10.07503300763299947, 4.881889043637199777, 6.575021251017499679 ) ) ;
#51942=DIRECTION ( 'NONE',  ( -1.000000000000000000, 0.000000000000000000, -2.609704304917999919E-14 ) ) ;
#51972=CARTESIAN_POINT ( 'NONE',  ( 11.71922412107039868, 4.069539071394910223, 8.814426450544999625 ) ) ;
#51980=CARTESIAN_POINT ( 'NONE',  ( 11.39700581613019992, 4.869652672166700391, 6.941573685175900010 ) ) ;
#51986=CARTESIAN_POINT ( 'NONE',  ( 10.76426088462129904, 4.002719309691810778, 8.778009775371000245 ) ) ;
#51992=EDGE_CURVE ( 'NONE', #26661, #46967, #67545, .T. ) ;
#52016=CARTESIAN_POINT ( 'NONE',  ( 9.896013540183126622, 3.000416447002273834, 6.731816600031358178 ) ) ;
#52020=CARTESIAN_POINT ( 'NONE',  ( 10.49764694612699856, 2.940513484064000149, 7.077178005756699974 ) ) ;
#52060=CARTESIAN_POINT ( 'NONE',  ( 10.33351354018233081, 2.750000000000000000, 7.663624617374469317 ) ) ;
#52075=CARTESIAN_POINT ( 'NONE',  ( 11.58902763632552002, 3.213494089586499847, 7.862914650060299770 ) ) ;
#52092=CARTESIAN_POINT ( 'NONE',  ( 10.76841504065829902, 4.914510326623699576, 8.181880472491098288 ) ) ;
#52107=CARTESIAN_POINT ( 'NONE',  ( 11.73671932425159881, 3.872987101045399783, 6.643164954553199664 ) ) ;
#52153=CARTESIAN_POINT ( 'NONE',  ( 10.32101354018304207, 3.231816600031359510, 8.499583552997727054 ) ) ;
#52156=CARTESIAN_POINT ( 'NONE',  ( 9.627671671056999614, 3.144964309357700216, 7.356396684460199786 ) ) ;
#52193=CARTESIAN_POINT ( 'NONE',  ( 11.64122412107036908, 4.062069863985690255, 8.673243607771999208 ) ) ;
#52206=CARTESIAN_POINT ( 'NONE',  ( 9.048063610504998522, 4.524705472883399970, 6.333351572150998976 ) ) ;
#52237=CARTESIAN_POINT ( 'NONE',  ( 10.44424205625099944, 3.541248877825399877, 6.305876158747000026 ) ) ;
#52246=FACE_OUTER_BOUND ( 'NONE', #67997, .T. ) ;
#52255=ORIENTED_EDGE ( 'NONE', *, *, #36615, .F. ) ;
#52336=CARTESIAN_POINT ( 'NONE',  ( 10.68035971519489813, 4.678140486081599825, 8.628134814664999652 ) ) ;
#52341=CARTESIAN_POINT ( 'NONE',  ( 10.41964694612699915, 2.813019656517000477, 7.026297514493899499 ) ) ;
#52352=ORIENTED_EDGE ( 'NONE', *, *, #46005, .F. ) ;
#52368=CARTESIAN_POINT ( 'NONE',  ( 10.01059687351599692, 4.629523725463622341, 6.407767014557176566 ) ) ;
#52369=VERTEX_POINT ( 'NONE', #47335 ) ;
#52373=CARTESIAN_POINT ( 'NONE',  ( 10.69601354018300832, 4.999583552997727054, 8.268183399968641822 ) ) ;
#52421=ORIENTED_EDGE ( 'NONE', *, *, #60777, .F. ) ;
#52424=CARTESIAN_POINT ( 'NONE',  ( 10.45672469555900008, 4.433465011431599656, 8.249937779480299938 ) ) ;
#52429=CARTESIAN_POINT ( 'NONE',  ( 11.59999999999999964, 4.000000000000000000, 7.500000000000000000 ) ) ;
#52431=VECTOR ( 'NONE', #46940, 1000.000000000000000 ) ;
#52441=CARTESIAN_POINT ( 'NONE',  ( 11.40841235500449891, 3.158861363519000154, 8.270568563129298667 ) ) ;
#52456=CARTESIAN_POINT ( 'NONE',  ( 10.89979975933730039, 4.819074589197400726, 7.781807394638899922 ) ) ;
#52467=CARTESIAN_POINT ( 'NONE',  ( 10.93210843320491676, 2.862311695598936723, 6.901605483505059979 ) ) ;
#52504=CARTESIAN_POINT ( 'NONE',  ( 10.21024205624999937, 3.689072563647699976, 6.690659495528099576 ) ) ;
#52536=CARTESIAN_POINT ( 'NONE',  ( 11.30878751119029957, 2.958974835389999836, 6.955365841266999638 ) ) ;
#52548=( NAMED_UNIT ( * ) PLANE_ANGLE_UNIT ( ) SI_UNIT ( $, .RADIAN. ) );
#52550=CARTESIAN_POINT ( 'NONE',  ( 8.870759580228998686, 2.755835090116000696, 7.797385380423699885 ) ) ;
#52583=CARTESIAN_POINT ( 'NONE',  ( 10.36825461470400001, 2.760277452415999644, 7.184607557167700165 ) ) ;
#52625=CARTESIAN_POINT ( 'NONE',  ( 11.60000000000000142, 3.468809616172331634, 8.305884920888427558 ) ) ;
#52640=EDGE_CURVE ( 'NONE', #43427, #12913, #61607, .T. ) ;
#52677=CARTESIAN_POINT ( 'NONE',  ( 10.64391429142989765, 4.022379549362480766, 8.674673860548999471 ) ) ;
#52683=CARTESIAN_POINT ( 'NONE',  ( 10.71503032197929883, 4.743378537856500543, 8.539569492647999027 ) ) ;
#52695=CARTESIAN_POINT ( 'NONE',  ( 8.736413463905998711, 4.084156314540369870, 6.617590440947399344 ) ) ;
#52697=ORIENTED_EDGE ( 'NONE', *, *, #68611, .F. ) ;
#52718=CARTESIAN_POINT ( 'NONE',  ( 10.78976354018297634, 3.672815144550904076, 8.717465845835395299 ) ) ;
#52773=CARTESIAN_POINT ( 'NONE',  ( 11.02287616594229824, 3.738072157442200005, 8.325646653015098764 ) ) ;
#52789=CARTESIAN_POINT ( 'NONE',  ( 10.94072200990529886, 2.922907051630999842, 7.875713849677398848 ) ) ;
#52851=CARTESIAN_POINT ( 'NONE',  ( 10.37309687351658383, 2.782534154164606921, 7.827184855449101697 ) ) ;
#52853=CARTESIAN_POINT ( 'NONE',  ( 10.03293802597399953, 3.549239910423600097, 8.240623579255899500 ) ) ;
#52859=CIRCLE ( 'NONE', #39436, 1.249999999999999778 ) ;
#52898=( LENGTH_UNIT ( ) NAMED_UNIT ( * ) SI_UNIT ( .MILLI., .METRE. ) );
#52900=CARTESIAN_POINT ( 'NONE',  ( 9.706621437244999484, 4.849675135054999586, 8.456261759323901117 ) ) ;
#52961=VERTEX_POINT ( 'NONE', #51296 ) ;
#53029=CARTESIAN_POINT ( 'NONE',  ( 11.48522412107029922, 4.047131449166419870, 8.390877922225699947 ) ) ;
#53031=ORIENTED_EDGE ( 'NONE', *, *, #6613, .T. ) ;
#53034=CARTESIAN_POINT ( 'NONE',  ( 10.25149413291699929, 5.037815157227999663, 7.973529073237199505 ) ) ;
#53117=CARTESIAN_POINT ( 'NONE',  ( 10.87518447801629939, 4.865987311498500389, 7.519093628927509876 ) ) ;
#53135=CARTESIAN_POINT ( 'NONE',  ( 11.67918044953561996, 5.011483761127000669, 6.972563939641199582 ) ) ;
#53146=CARTESIAN_POINT ( 'NONE',  ( 9.448096873516666605, 3.672815144550898303, 6.282534154164604701 ) ) ;
#53148=CARTESIAN_POINT ( 'NONE',  ( 10.53057053952199951, 3.659587858614300249, 8.296503712697200328 ) ) ;
#53160=CARTESIAN_POINT ( 'NONE',  ( 10.97028665956023197, 3.257584962274628904, 6.450604656432374462 ) ) ;
#53184=ADVANCED_FACE ( 'NONE', ( #30663 ), #5464, .F. ) ;
#53196=CARTESIAN_POINT ( 'NONE',  ( 9.754317406968999293, 4.161254277581000416, 6.648116790593900483 ) ) ;
#53240=CARTESIAN_POINT ( 'NONE',  ( 9.478659112603999404, 3.444147913214900214, 6.347865960448999090 ) ) ;
#53246=CARTESIAN_POINT ( 'NONE',  ( 11.60000000000000142, 4.325863785438847309, 6.377063228063085454 ) ) ;
#53248=CARTESIAN_POINT ( 'NONE',  ( 9.556179045228626379, 3.383234358265068575, 8.120590373834733811 ) ) ;
#53270=DIRECTION ( 'NONE',  ( 0.000000000000000000, 1.000000000000000000, 0.000000000000000000 ) ) ;
#53276=FACE_OUTER_BOUND ( 'NONE', #30670, .T. ) ;
#53297=SHAPE_DEFINITION_REPRESENTATION ( #29383, #24587 ) ;
#53352=EDGE_CURVE ( 'NONE', #33283, #43200, #50138, .T. ) ;
#53374=CARTESIAN_POINT ( 'NONE',  ( 11.06967835872019812, 3.245266201729799960, 7.975673736933100777 ) ) ;
#53404=ORIENTED_EDGE ( 'NONE', *, *, #47772, .T. ) ;
#53465=CARTESIAN_POINT ( 'NONE',  ( 11.65871932425156920, 3.852858594438699935, 6.507377093516500288 ) ) ;
#53478=CARTESIAN_POINT ( 'NONE',  ( 10.25149413291699929, 5.037815157227999663, 7.973529073237199505 ) ) ;
#53492=CARTESIAN_POINT ( 'NONE',  ( 10.40749413291699987, 4.788043169210699723, 7.859564368461399830 ) ) ;
#53534=CARTESIAN_POINT ( 'NONE',  ( 11.25962254157670905, 4.169672662336058266, 6.639751609450684100 ) ) ;
#53544=CARTESIAN_POINT ( 'NONE',  ( 8.741151519676998660, 4.018750234858180725, 6.633192605878799775 ) ) ;
#53549=DIRECTION ( 'NONE',  ( 0.7071067617951957152, 0.000000000000000000, -0.7071068005778986532 ) ) ;
#53569=CARTESIAN_POINT ( 'NONE',  ( 10.44999293566599974, 4.720032669050099550, 6.616719557880299085 ) ) ;
#53587=CARTESIAN_POINT ( 'NONE',  ( 8.769442991499998286, 3.919472480837189909, 8.776675254768999679 ) ) ;
#53596=CARTESIAN_POINT ( 'NONE',  ( 9.581508192411627434, 3.220001783077621305, 7.896402636871828307 ) ) ;
#53599=CARTESIAN_POINT ( 'NONE',  ( 11.48513281071060277, 2.915426916004881353, 7.175000865651856685 ) ) ;
#53618=CARTESIAN_POINT ( 'NONE',  ( 9.834329965421998665, 3.206942993865000258, 6.678540912152799436 ) ) ;
#53664=EDGE_CURVE ( 'NONE', #15952, #1219, #49123, .T. ) ;
#53714=CARTESIAN_POINT ( 'NONE',  ( 10.61257802013489737, 3.108115747127599970, 7.520762592984879369 ) ) ;
#53785=ORIENTED_EDGE ( 'NONE', *, *, #32381, .T. ) ;
#53800=CARTESIAN_POINT ( 'NONE',  ( 10.47718582084299932, 3.343463760027599818, 8.258888014436699621 ) ) ;
#53815=CARTESIAN_POINT ( 'NONE',  ( 10.46887750876899936, 3.307728619566300043, 6.425720373262999274 ) ) ;
#53830=CARTESIAN_POINT ( 'NONE',  ( 11.68333460557258796, 4.162011815820000571, 6.509695444280099608 ) ) ;
#53877=CARTESIAN_POINT ( 'NONE',  ( 8.893126402770997530, 4.811247217215600003, 7.805918119494599239 ) ) ;
#53889=CARTESIAN_POINT ( 'NONE',  ( 11.34287482311539996, 4.803125295093300551, 7.175518335304800210 ) ) ;
#53907=CARTESIAN_POINT ( 'NONE',  ( 10.56591429142999949, 4.019686495353769651, 8.533318907609000803 ) ) ;
#53922=DIRECTION ( 'NONE',  ( -1.000000000000000000, 0.000000000000000000, 0.000000000000000000 ) ) ;
#53952=CARTESIAN_POINT ( 'NONE',  ( 10.88813259637009878, 2.844182332072999753, 6.870201387206400057 ) ) ;
#53956=CARTESIAN_POINT ( 'NONE',  ( 9.253772138682000659, 3.523984281974800403, 8.687347221188998603 ) ) ;
#53975=PRODUCT_CONTEXT ( 'NONE', #26660, 'mechanical' ) ;
#53999=CARTESIAN_POINT ( 'NONE',  ( 11.60000000000000142, 3.745359844992759868, 8.477868186285956398 ) ) ;
#54005=CARTESIAN_POINT ( 'NONE',  ( 9.432025935145999185, 3.854158361175799907, 8.493766832166899761 ) ) ;
#54054=CARTESIAN_POINT ( 'NONE',  ( 10.81524174883999834, 3.971581146373189597, 6.466884287543999577 ) ) ;
#54142=CARTESIAN_POINT ( 'NONE',  ( 11.21564426047340035, 4.539962866738299851, 6.654192128557399499 ) ) ;
#54157=CARTESIAN_POINT ( 'NONE',  ( 11.18272066707849888, 5.093522884867000222, 8.161456030935699602 ) ) ;
#54171=CARTESIAN_POINT ( 'NONE',  ( 10.45672469555900008, 4.433465011431599656, 8.249937779480299938 ) ) ;
#54208=EDGE_CURVE ( 'NONE', #32603, #69137, #38355, .T. ) ;
#54215=VECTOR ( 'NONE', #9156, 1000.000000000000114 ) ;
#54233=CARTESIAN_POINT ( 'NONE',  ( 11.44133594839949986, 4.569506585117100173, 8.152656755002400502 ) ) ;
#54248=CARTESIAN_POINT ( 'NONE',  ( 10.56080513895999928, 5.026880838510000338, 8.070849345005600028 ) ) ;
#54278=CARTESIAN_POINT ( 'NONE',  ( 9.606837339593626623, 3.135127465292355087, 7.632392475727677095 ) ) ;
#54291=ADVANCED_FACE ( 'NONE', ( #44543 ), #37729, .T. ) ;
#54299=CARTESIAN_POINT ( 'NONE',  ( 10.85168717260509830, 3.386210853237200169, 6.498190316041999814 ) ) ;
#54302=CARTESIAN_POINT ( 'NONE',  ( 9.454392757686999715, 4.770706668257700400, 6.657535947657399866 ) ) ;
#54349=CARTESIAN_POINT ( 'NONE',  ( 8.748138961223999033, 4.832207374954999857, 6.937618199889199033 ) ) ;
#54357=CARTESIAN_POINT ( 'NONE',  ( 9.940621437244999470, 4.575883738927100097, 8.148124882831599081 ) ) ;
#54396=FACE_OUTER_BOUND ( 'NONE', #50930, .T. ) ;
#54402=CARTESIAN_POINT ( 'NONE',  ( 10.44635971519499940, 4.459622816450200311, 8.264615166761799969 ) ) ;
#54486=CARTESIAN_POINT ( 'NONE',  ( 11.45284386393252696, 4.902679577238613362, 7.824986766837089824 ) ) ;
#54491=CARTESIAN_POINT ( 'NONE',  ( 10.30903300763299946, 4.597717337857299746, 6.873077781830399857 ) ) ;
#54507=CARTESIAN_POINT ( 'NONE',  ( 10.42380110216399913, 3.026453990125600235, 8.094557215852098864 ) ) ;
#54515=ORIENTED_EDGE ( 'NONE', *, *, #25137, .F. ) ;
#54524=CARTESIAN_POINT ( 'NONE',  ( 11.14179841651039915, 3.646693590264900031, 6.560784671286499226 ) ) ;
#54526=CARTESIAN_POINT ( 'NONE',  ( 10.64601354018249957, 4.999583552997728830, 8.268183399968640046 ) ) ;
#54547=CARTESIAN_POINT ( 'NONE',  ( 8.741501215035997419, 3.771222299067000350, 6.624106355763400344 ) ) ;
#54575=CARTESIAN_POINT ( 'NONE',  ( 9.298392757686999133, 4.585219941293100732, 6.860292594369099106 ) ) ;
#54590=CARTESIAN_POINT ( 'NONE',  ( 10.87518447801629939, 4.865987311498500389, 7.519093628927509876 ) ) ;
#54603=CARTESIAN_POINT ( 'NONE',  ( 11.05946005378019947, 5.036385109519999403, 8.053412743695298914 ) ) ;
#54610=AXIS2_PLACEMENT_3D ( 'NONE', #52429, #57669, #10464 ) ;
#54633=CARTESIAN_POINT ( 'NONE',  ( 10.08809113605762597, 3.189914598996232975, 7.830596297620237678 ) ) ;
#54653=CARTESIAN_POINT ( 'NONE',  ( 10.44125056272499918, 5.033400911533000510, 7.484684486284700178 ) ) ;
#54655=CARTESIAN_POINT ( 'NONE',  ( 10.13827973160999818, 4.102460098134500299, 8.637205511891998810 ) ) ;
#54703=CARTESIAN_POINT ( 'NONE',  ( 8.950772138681999834, 3.626242194157900389, 8.432280753260499750 ) ) ;
#54709=CARTESIAN_POINT ( 'NONE',  ( 9.889963142879999225, 4.848366390061300102, 7.678836273503299559 ) ) ;
#54804=CARTESIAN_POINT ( 'NONE',  ( 11.50705667793316778, 4.601576474242010661, 6.338208022222376670 ) ) ;
#54832=CARTESIAN_POINT ( 'NONE',  ( 11.38678751119029897, 2.833702563575000166, 6.889827023674499173 ) ) ;
#54840=CARTESIAN_POINT ( 'NONE',  ( 10.60026222744819790, 3.225465054973100099, 6.861998062869400172 ) ) ;
#54871=CARTESIAN_POINT ( 'NONE',  ( 10.79303032197930001, 4.663532080728800544, 8.427909097977700270 ) ) ;
#54893=CARTESIAN_POINT ( 'NONE',  ( 8.790860954911998704, 4.097566467530549872, 6.578106533244199916 ) ) ;
#54938=CARTESIAN_POINT ( 'NONE',  ( 11.17056785386839834, 3.281375110759499947, 7.016391833292499491 ) ) ;
#54952=CARTESIAN_POINT ( 'NONE',  ( 11.18923293495519822, 2.967327562101000016, 7.541513160549049744 ) ) ;
#54967=( NAMED_UNIT ( * ) SI_UNIT ( $, .STERADIAN. ) SOLID_ANGLE_UNIT ( ) );
#54981=CARTESIAN_POINT ( 'NONE',  ( 8.998937807218627682, 3.944921334759000420, 8.373211663664079651 ) ) ;
#55000=CARTESIAN_POINT ( 'NONE',  ( 10.81013259637009938, 2.968328969579000276, 6.937848198857199833 ) ) ;
#55002=CARTESIAN_POINT ( 'NONE',  ( 10.23959632033899858, 2.942832934044000037, 7.931430460958599049 ) ) ;
#55007=CARTESIAN_POINT ( 'NONE',  ( 10.40434687351665310, 2.750000000000000000, 7.336375382625536901 ) ) ;
#55050=CARTESIAN_POINT ( 'NONE',  ( 9.634659112603999986, 3.563556310301200014, 6.595367916746299741 ) ) ;
#55052=CARTESIAN_POINT ( 'NONE',  ( 9.498096873515667227, 3.672815144550898303, 6.282534154164607365 ) ) ;
#55056=CARTESIAN_POINT ( 'NONE',  ( 8.724822372493999723, 3.750788346126100237, 6.684745346084599582 ) ) ;
#55087=EDGE_LOOP ( 'NONE', ( #52421, #55984, #35000, #41942, #34838 ) ) ;
#55089=CARTESIAN_POINT ( 'NONE',  ( 10.84606641549978256, 4.838299037060044938, 7.252322131039115050 ) ) ;
#55096=CARTESIAN_POINT ( 'NONE',  ( 10.29657053952199952, 3.497746311184500190, 8.675184076076000395 ) ) ;
#55105=ORIENTED_EDGE ( 'NONE', *, *, #15214, .F. ) ;
#55127=CARTESIAN_POINT ( 'NONE',  ( 8.599999952505998024, 3.250000006358199744, 7.500000000000000000 ) ) ;
#55131=B_SPLINE_CURVE_WITH_KNOTS ( 'NONE', 3,
 ( #44993, #61743, #3017, #45680, #7234, #13863, #18076, #56505, #7928, #8611, #39746, #45338, #61066, #66298, #18423, #29959, #49885, #51262 ),
 .UNSPECIFIED., .F., .F.,
 ( 4, 2, 2, 2, 2, 2, 2, 2, 4 ),
 ( 0.000000000000000000, 0.1250000000000000000, 0.2500000000000000000, 0.3750000000000000000, 0.5000000000000000000, 0.6250000000000000000, 0.7500000000000000000, 0.8750000000000000000, 1.000000000000000000 ),
 .UNSPECIFIED. ) ;
#55138=CARTESIAN_POINT ( 'NONE',  ( 11.59999999999999964, 4.000000000000000000, 7.500000000000000000 ) ) ;
#55169=EDGE_CURVE ( 'NONE', #60390, #46623, #16551, .T. ) ;
#55177=CARTESIAN_POINT ( 'NONE',  ( 10.97124174884019965, 3.963805917081910213, 6.184229974648999928 ) ) ;
#55182=CARTESIAN_POINT ( 'NONE',  ( 10.25564828895399927, 4.880669054351300495, 7.018986873610899124 ) ) ;
#55217=CARTESIAN_POINT ( 'NONE',  ( 11.35918179236250047, 3.761636028845500412, 8.615559381441000752 ) ) ;
#55240=CARTESIAN_POINT ( 'NONE',  ( 8.770072224255999416, 4.093776898754200033, 6.613913699222099041 ) ) ;
#55288=CARTESIAN_POINT ( 'NONE',  ( 10.99410672858429905, 3.198097575668700010, 8.103244025831999764 ) ) ;
#55311=CARTESIAN_POINT ( 'NONE',  ( 11.36486084871759950, 2.792989229543000107, 7.174999999999999822 ) ) ;
#55315=CARTESIAN_POINT ( 'NONE',  ( 9.227255459545908423, 4.629538885478623911, 8.592254274082833376 ) ) ;
#55346=CARTESIAN_POINT ( 'NONE',  ( 10.76857802013509868, 2.825431102905000103, 7.527343341769989316 ) ) ;
#55348=CARTESIAN_POINT ( 'NONE',  ( 9.125113844317997547, 4.288351516201100111, 8.604802177355001191 ) ) ;
#55357=FACE_OUTER_BOUND ( 'NONE', #14539, .T. ) ;
#55396=CARTESIAN_POINT ( 'NONE',  ( 9.786633995697998856, 4.998281561686200192, 7.389201877599999690 ) ) ;
#55404=CARTESIAN_POINT ( 'NONE',  ( 9.408709346416998187, 4.783195203880800328, 7.871904849557299855 ) ) ;
#55411=CARTESIAN_POINT ( 'NONE',  ( 8.789886373836322875, 4.000007821194420110, 6.560153657526067938 ) ) ;
#55439=CARTESIAN_POINT ( 'NONE',  ( 10.99375810342578141, 4.001859925960030928, 8.374120210831636157 ) ) ;
#55479=DIRECTION ( 'NONE',  ( 0.000000000000000000, 1.000000000000000000, 0.000000000000000000 ) ) ;
#55480=ORIENTED_EDGE ( 'NONE', *, *, #34292, .F. ) ;
#55534=CARTESIAN_POINT ( 'NONE',  ( 11.21149010443640037, 5.137564434800999891, 7.414927836855409460 ) ) ;
#55566=CARTESIAN_POINT ( 'NONE',  ( 11.48225819896749833, 2.879005208331999910, 7.288668995979000087 ) ) ;
#55595=CARTESIAN_POINT ( 'NONE',  ( 9.272783876522375124, 3.210141752053232711, 8.481892410946455740 ) ) ;
#55634=CARTESIAN_POINT ( 'NONE',  ( 11.70794988689359961, 4.455786710255300598, 6.606015074393400077 ) ) ;
#55649=CARTESIAN_POINT ( 'NONE',  ( 10.57102344389999971, 3.237334151971200225, 7.962849245488699879 ) ) ;
#55667=CARTESIAN_POINT ( 'NONE',  ( 8.807788144226000426, 4.090932644426789722, 6.546538158064899804 ) ) ;
#55698=CARTESIAN_POINT ( 'NONE',  ( 10.44635971519499940, 4.459622816450200311, 8.264615166761799969 ) ) ;
#55700=CARTESIAN_POINT ( 'NONE',  ( 9.984292290062997566, 4.868609929059700470, 8.004340253666999416 ) ) ;
#55748=CARTESIAN_POINT ( 'NONE',  ( 9.354025935145999782, 3.834207658792500251, 8.629711178834000407 ) ) ;
#55750=CARTESIAN_POINT ( 'NONE',  ( 9.623096873515669003, 5.217465845835395299, 7.172815144550900968 ) ) ;
#55752=CARTESIAN_POINT ( 'NONE',  ( 9.099999931440999390, 5.064317881551000156, 6.844464000216799349 ) ) ;
#55753=CARTESIAN_POINT ( 'NONE',  ( 9.586013376692998023, 3.227076647348800176, 7.892807122431200639 ) ) ;
#55784=CARTESIAN_POINT ( 'NONE',  ( 11.06623059009866061, 3.312237475846871781, 8.035958501307058910 ) ) ;
#55787=CARTESIAN_POINT ( 'NONE',  ( 10.46887750876899936, 3.307728619566300043, 6.425720373262999274 ) ) ;
#55807=CARTESIAN_POINT ( 'NONE',  ( 10.59195391537400077, 5.057233422790000432, 6.781965272201699868 ) ) ;
#55846=EDGE_CURVE ( 'NONE', #69137, #19003, #34769, .T. ) ;
#55878=CARTESIAN_POINT ( 'NONE',  ( 11.01456785386839954, 3.053605396817899997, 6.863111178199799767 ) ) ;
#55906=CARTESIAN_POINT ( 'NONE',  ( 9.771013540183334456, 3.231816600031359066, 8.499583552997725278 ) ) ;
#55912=CARTESIAN_POINT ( 'NONE',  ( 10.37872469555899890, 4.502158848185001006, 8.368784980615899372 ) ) ;
#55975=CARTESIAN_POINT ( 'NONE',  ( 10.52641638348499953, 3.025038519517300184, 7.737488872214999702 ) ) ;
#55984=ORIENTED_EDGE ( 'NONE', *, *, #7482, .T. ) ;
#55991=CARTESIAN_POINT ( 'NONE',  ( 10.36325056272499978, 4.892034740700499817, 7.486779603004729111 ) ) ;
#56005=CARTESIAN_POINT ( 'NONE',  ( 8.905196823546312146, 4.608202637908532573, 6.627513167511573045 ) ) ;
#56006=CARTESIAN_POINT ( 'NONE',  ( 9.185590450029499365, 5.092272840597500405, 8.129537449122580028 ) ) ;
#56035=CARTESIAN_POINT ( 'NONE',  ( 9.503038493598998215, 4.726907342723099426, 8.193143574899998782 ) ) ;
#56075=EDGE_LOOP ( 'NONE', ( #47113, #53031, #11301, #63514 ) ) ;
#56080=CARTESIAN_POINT ( 'NONE',  ( 9.278038493598998571, 4.826346105011899645, 8.287963554181398962 ) ) ;
#56089=CARTESIAN_POINT ( 'NONE',  ( 10.34393020684899867, 2.750000000000000000, 7.500000000000000000 ) ) ;
#56217=CARTESIAN_POINT ( 'NONE',  ( 10.30487885159599770, 4.996404279947399552, 7.618867373350600047 ) ) ;
#56251=CARTESIAN_POINT ( 'NONE',  ( 10.42795525820099911, 3.905250696375530239, 8.498986197235801399 ) ) ;
#56298=ORIENTED_EDGE ( 'NONE', *, *, #52640, .F. ) ;
#56316=CARTESIAN_POINT ( 'NONE',  ( 11.00000000000000000, 5.079754677601000523, 7.174999999999999822 ) ) ;
#56321=CARTESIAN_POINT ( 'NONE',  ( 11.16641369783139837, 3.949373449607799902, 6.497808498716000081 ) ) ;
#56331=DIRECTION ( 'NONE',  ( 1.000000000000000000, 0.000000000000000000, 0.000000000000000000 ) ) ;
#56382=CARTESIAN_POINT ( 'NONE',  ( 11.19434208742519843, 3.521141233577200325, 6.747282993577999655 ) ) ;
#56385=CARTESIAN_POINT ( 'NONE',  ( 9.908304848515998131, 4.913464051101100516, 7.082356937474298952 ) ) ;
#56395=LINE ( 'NONE', #50458, #67446 ) ;
#56412=EDGE_LOOP ( 'NONE', ( #24067, #41668, #39643, #45519, #57749 ) ) ;
#56429=CARTESIAN_POINT ( 'NONE',  ( 8.974088727410999056, 2.862182806015999947, 7.404572115919599185 ) ) ;
#56438=CARTESIAN_POINT ( 'NONE',  ( 11.59999999999999964, 3.310169951859693427, 6.761031184901315605 ) ) ;
#56469=CARTESIAN_POINT ( 'NONE',  ( 10.71503032197929883, 4.743378537856500543, 8.539569492647999027 ) ) ;
#56502=CARTESIAN_POINT ( 'NONE',  ( 11.59999999999999964, 4.695782097862117865, 8.404145852941008243 ) ) ;
#56505=CARTESIAN_POINT ( 'NONE',  ( 9.789763540182331525, 3.672815144550904076, 8.717465845835395299 ) ) ;
#56533=CARTESIAN_POINT ( 'NONE',  ( 9.143927823787139531, 5.249988444743198812, 7.500000155056751439 ) ) ;
#56547=CARTESIAN_POINT ( 'NONE',  ( 9.099999931440999390, 5.064317881551000156, 6.844464000216799349 ) ) ;
#56548=CARTESIAN_POINT ( 'NONE',  ( 10.33744474310099903, 4.771257858050099721, 7.125715588371799747 ) ) ;
#56555=CARTESIAN_POINT ( 'NONE',  ( 10.55569598648999907, 5.130952141044000214, 6.826612223887499553 ) ) ;
#56560=CARTESIAN_POINT ( 'NONE',  ( 11.18687482311539938, 5.057677595549000316, 7.072673169413499217 ) ) ;
#56577=VERTEX_POINT ( 'NONE', #42544 ) ;
#56594=CARTESIAN_POINT ( 'NONE',  ( 11.42887348028849992, 2.875789035466000065, 6.892162778124999889 ) ) ;
#56663=CARTESIAN_POINT ( 'NONE',  ( 10.74795391537419853, 4.830118059977199785, 6.936213817702099327 ) ) ;
#56681=CARTESIAN_POINT ( 'NONE',  ( 10.98656920625009903, 4.032067152264009913, 8.391549386185598536 ) ) ;
#56683=CARTESIAN_POINT ( 'NONE',  ( 10.94903032197929882, 4.503839166471300004, 8.204588308639600314 ) ) ;
#56730=CARTESIAN_POINT ( 'NONE',  ( 11.48522412107029922, 4.047131449166419870, 8.390877922225699947 ) ) ;
#56733=CARTESIAN_POINT ( 'NONE',  ( 9.378405316141000370, 3.757578743663700038, 6.384219384258999597 ) ) ;
#56766=CARTESIAN_POINT ( 'NONE',  ( 11.03111947020579819, 3.091200775993899974, 7.825000000000000178 ) ) ;
#56773=CARTESIAN_POINT ( 'NONE',  ( 11.14975833414749928, 3.203462856645999945, 7.174999999999999822 ) ) ;
#56780=CARTESIAN_POINT ( 'NONE',  ( 8.568822372493999140, 3.671800173070400408, 6.426348619097999482 ) ) ;
#56888=CARTESIAN_POINT ( 'NONE',  ( 10.55569598648999907, 5.130952141044000214, 6.826612223887499553 ) ) ;
#56897=CARTESIAN_POINT ( 'NONE',  ( 11.76588784977539781, 2.879134238109999799, 7.564049652083489228 ) ) ;
#56902=CARTESIAN_POINT ( 'NONE',  ( 10.15303300763299887, 4.787165141710600480, 6.674373427955200277 ) ) ;
#56936=CARTESIAN_POINT ( 'NONE',  ( 10.37457053952199892, 3.551693493661699730, 8.548957288282998945 ) ) ;
#56956=ORIENTED_EDGE ( 'NONE', *, *, #1178, .F. ) ;
#56965=EDGE_CURVE ( 'NONE', #69137, #13026, #62736, .T. ) ;
#56975=VECTOR ( 'NONE', #19527, 1000.000000000000000 ) ;
#56979=CARTESIAN_POINT ( 'NONE',  ( 11.58810207955109917, 3.203462856645999945, 7.825000000000000178 ) ) ;
#56987=CARTESIAN_POINT ( 'NONE',  ( 10.31021345716899873, 4.636538040886300394, 6.921280946186199934 ) ) ;
#57000=CARTESIAN_POINT ( 'NONE',  ( 11.55670819615736455, 3.379350336066780702, 8.119355997108680612 ) ) ;
#57002=CARTESIAN_POINT ( 'NONE',  ( 10.96533729122639933, 2.859653469230999612, 7.529998433785960010 ) ) ;
#57004=B_SPLINE_CURVE_WITH_KNOTS ( 'NONE', 3,
 ( #40921, #62244, #57000, #9436, #4194, #57334, #63261, #4534, #20283, #25531 ),
 .UNSPECIFIED., .F., .F.,
 ( 4, 2, 2, 2, 4 ),
 ( 0.000000000000000000, 0.2500000000000000000, 0.5000000000000000000, 0.7500000000000000000, 1.000000000000000000 ),
 .UNSPECIFIED. ) ;
#57015=CARTESIAN_POINT ( 'NONE',  ( 9.396013540183334456, 3.000416447002273834, 6.731816600031358178 ) ) ;
#57018=CARTESIAN_POINT ( 'NONE',  ( 11.81056516821459823, 4.609678151793300316, 6.884701936848800052 ) ) ;
#57043=CARTESIAN_POINT ( 'NONE',  ( 8.755358248830999557, 4.089987329977850194, 6.649720865199900466 ) ) ;
#57056=LINE ( 'NONE', #35738, #54215 ) ;
#57061=CARTESIAN_POINT ( 'NONE',  ( 10.48791429142999831, 4.016993441347180394, 8.391963954669400039 ) ) ;
#57063=CARTESIAN_POINT ( 'NONE',  ( 9.728988259786000015, 3.886559292927400211, 6.640442468193600511 ) ) ;
#57083=CARTESIAN_POINT ( 'NONE',  ( 11.58810207955109917, 3.203462856645999945, 7.825000000000000178 ) ) ;
#57107=CARTESIAN_POINT ( 'NONE',  ( 8.923430433046998900, 3.028322657068899915, 8.099647887697699389 ) ) ;
#57117=CARTESIAN_POINT ( 'NONE',  ( 8.942941355974879158, 3.045333477771414721, 8.051224688103602034 ) ) ;
#57229=CARTESIAN_POINT ( 'NONE',  ( 10.47769598648999967, 5.009476315410999803, 6.898940957443399746 ) ) ;
#57234=CARTESIAN_POINT ( 'NONE',  ( 10.49349279008999858, 3.667611644732699627, 6.265968249244999733 ) ) ;
#57261=CARTESIAN_POINT ( 'NONE',  ( 9.854346873516623972, 2.749999999999999112, 7.336375382625534236 ) ) ;
#57264=CARTESIAN_POINT ( 'NONE',  ( 10.13662282008599824, 4.594711216567399781, 6.540749699823199315 ) ) ;
#57306=CARTESIAN_POINT ( 'NONE',  ( 10.26059687351566652, 3.370476274536378547, 8.592232985442823434 ) ) ;
#57321=CARTESIAN_POINT ( 'NONE',  ( 11.56441235500451015, 3.361299021099800388, 8.085115074060599483 ) ) ;
#57334=CARTESIAN_POINT ( 'NONE',  ( 11.47822875044625945, 4.169680329100683203, 8.360317195474184615 ) ) ;
#57336=CARTESIAN_POINT ( 'NONE',  ( 10.86687616594229944, 3.655053560864600204, 8.587337146608000182 ) ) ;
#57348=CARTESIAN_POINT ( 'NONE',  ( 10.80133863405319872, 4.534404523786000674, 6.818303296693398963 ) ) ;
#57369=ORIENTED_EDGE ( 'NONE', *, *, #12560, .T. ) ;
#57398=CARTESIAN_POINT ( 'NONE',  ( 9.351063610504999346, 4.411988005505000032, 6.583971515917899531 ) ) ;
#57429=CARTESIAN_POINT ( 'NONE',  ( 11.51145123989532948, 4.605239108938600445, 6.331134574721999364 ) ) ;
#57444=CARTESIAN_POINT ( 'NONE',  ( 8.972076168957999087, 3.350848599899200142, 6.397735581984999698 ) ) ;
#57476=CARTESIAN_POINT ( 'NONE',  ( 10.01364655415099847, 4.619310611972400338, 6.380697202105999999 ) ) ;
#57502=EDGE_LOOP ( 'NONE', ( #65932, #64866, #24677, #61405 ) ) ;
#57574=CARTESIAN_POINT ( 'NONE',  ( 10.88813259637009878, 2.844182332072999753, 6.870201387206400057 ) ) ;
#57579=CARTESIAN_POINT ( 'NONE',  ( 10.96118313518939935, 3.207251432249800249, 6.497569908212999401 ) ) ;
#57591=CARTESIAN_POINT ( 'NONE',  ( 8.786046699800500903, 4.845411057630703233, 7.038404655459764570 ) ) ;
#57600=EDGE_CURVE ( 'NONE', #46623, #34343, #57897, .T. ) ;
#57664=CARTESIAN_POINT ( 'NONE',  ( 10.89979975933730039, 4.819074589197400726, 7.781807394638899922 ) ) ;
#57669=DIRECTION ( 'NONE',  ( -1.000000000000000000, 0.000000000000000000, 0.000000000000000000 ) ) ;
#57679=CARTESIAN_POINT ( 'NONE',  ( 10.69456919669529960, 5.093991349577000172, 7.176777099639999768 ) ) ;
#57690=CARTESIAN_POINT ( 'NONE',  ( 10.86301932002748138, 2.749999999999999112, 7.200148911387369566 ) ) ;
#57694=CARTESIAN_POINT ( 'NONE',  ( 10.87518447801629939, 4.865987311498500389, 7.519093628927509876 ) ) ;
#57740=CARTESIAN_POINT ( 'NONE',  ( 10.35226354018316108, 2.907767014557178342, 8.129523725463624118 ) ) ;
#57744=CARTESIAN_POINT ( 'NONE',  ( 9.097772138681998300, 3.626242194157900389, 8.432280753260499750 ) ) ;
#57749=ORIENTED_EDGE ( 'NONE', *, *, #27402, .T. ) ;
#57777=CARTESIAN_POINT ( 'NONE',  ( 11.39189666366029918, 3.947847673382490541, 6.326270943800999191 ) ) ;
#57792=CARTESIAN_POINT ( 'NONE',  ( 8.718784697134999817, 4.694174896253500151, 8.574479223074998657 ) ) ;
#57801=ORIENTED_EDGE ( 'NONE', *, *, #41103, .T. ) ;
#57827=CARTESIAN_POINT ( 'NONE',  ( 9.532392757686999119, 4.863450031739999346, 6.556157624301499176 ) ) ;
#57897=B_SPLINE_CURVE_WITH_KNOTS ( 'NONE', 3,
 ( #24071, #61816, #60445, #51330, #18145, #23385, #45408, #39816, #24420, #39467 ),
 .UNSPECIFIED., .F., .F.,
 ( 4, 2, 2, 2, 4 ),
 ( 0.3934091950370091628, 0.5450568962777568860, 0.6967045975185046647, 0.8483522987592523323, 1.000000000000000000 ),
 .UNSPECIFIED. ) ;
#57915=EDGE_CURVE ( 'NONE', #46967, #52961, #63703, .T. ) ;
#57930=CARTESIAN_POINT ( 'NONE',  ( 10.89324174884020024, 3.967693531726030010, 6.325557131097000685 ) ) ;
#57936=CARTESIAN_POINT ( 'NONE',  ( 10.37041638348499895, 2.758294858530000226, 7.802464414828100381 ) ) ;
#57948=CARTESIAN_POINT ( 'NONE',  ( 8.810863317747999801, 4.960863370448500120, 7.499999999926881600 ) ) ;
#58021=CARTESIAN_POINT ( 'NONE',  ( 11.68748876160954886, 3.399618311400500303, 6.875627981711399883 ) ) ;
#58039=CARTESIAN_POINT ( 'NONE',  ( 11.16225954179439839, 4.877394611789299894, 6.770980925167799036 ) ) ;
#58052=CARTESIAN_POINT ( 'NONE',  ( 11.71210404293059959, 3.618181340822599790, 6.722495590581700320 ) ) ;
#58057=B_SPLINE_CURVE_WITH_KNOTS ( 'NONE', 3,
 ( #15049, #57690, #2, #47565, #4896, #68867, #9800, #10488, #20988, #42652 ),
 .UNSPECIFIED., .F., .F.,
 ( 4, 2, 2, 2, 4 ),
 ( 0.000000000000000000, 0.2500000000000000000, 0.5000000000000000000, 0.7500000000000000000, 1.000000000000000000 ),
 .UNSPECIFIED. ) ;
#58081=CARTESIAN_POINT ( 'NONE',  ( 8.712681907068999365, 3.774194491866800227, 6.635485632555699453 ) ) ;
#58098=CARTESIAN_POINT ( 'NONE',  ( 10.08359632033899800, 3.197262364844699611, 7.827597670336898794 ) ) ;
#58122=AXIS2_PLACEMENT_3D ( 'NONE', #46325, #35830, #37201 ) ;
#58130=CARTESIAN_POINT ( 'NONE',  ( 11.14256920625030034, 4.042230905578960254, 8.674127893687000324 ) ) ;
#58138=ORIENTED_EDGE ( 'NONE', *, *, #49874, .T. ) ;
#58145=PRESENTATION_STYLE_ASSIGNMENT (( #20740 ) ) ;
#58176=CARTESIAN_POINT ( 'NONE',  ( 9.608380199233998553, 5.269225938816000543, 7.659530259549099718 ) ) ;
#58264=ORIENTED_EDGE ( 'NONE', *, *, #49874, .F. ) ;
#58268=CARTESIAN_POINT ( 'NONE',  ( 11.27745123989519982, 4.410212499603100689, 6.707778874960499849 ) ) ;
#58273=CARTESIAN_POINT ( 'NONE',  ( 11.33041235500449950, 3.057642534728299832, 8.363295307663500822 ) ) ;
#58306=CARTESIAN_POINT ( 'NONE',  ( 10.65434687351636178, 5.250000000000002665, 7.663624617374463988 ) ) ;
#58357=CARTESIAN_POINT ( 'NONE',  ( 11.78594988689359901, 4.393436444036099786, 6.728309553046099012 ) ) ;
#58372=CARTESIAN_POINT ( 'NONE',  ( 10.91610672858429965, 3.088399709291500095, 8.185766014210599906 ) ) ;
#58385=CARTESIAN_POINT ( 'NONE',  ( 10.87103032197929942, 4.583685623598699799, 8.316248703309600643 ) ) ;
#58400=CARTESIAN_POINT ( 'NONE',  ( 11.12299956498149811, 5.207010770456999893, 7.174999999999999822 ) ) ;
#58435=CARTESIAN_POINT ( 'NONE',  ( 9.275076168957998135, 3.490299597736799875, 6.634524523592600254 ) ) ;
#58467=CARTESIAN_POINT ( 'NONE',  ( 11.34523293495530005, 2.684794526488000432, 7.552870914315270134 ) ) ;
#58484=CARTESIAN_POINT ( 'NONE',  ( 8.693455549952998851, 4.995562869655000071, 8.303267676773000261 ) ) ;
#58493=CARTESIAN_POINT ( 'NONE',  ( 10.31021345716899873, 4.636538040886300394, 6.921280946186199934 ) ) ;
#58544=ORIENTED_EDGE ( 'NONE', *, *, #22830, .T. ) ;
#58610=CARTESIAN_POINT ( 'NONE',  ( 10.28014141025500017, 4.417352327511700594, 6.756653759087999589 ) ) ;
#58632=CARTESIAN_POINT ( 'NONE',  ( 8.810863317747999801, 4.960863370448500120, 7.499999999926881600 ) ) ;
#58644=CARTESIAN_POINT ( 'NONE',  ( 11.33570505509991655, 4.908984911270270146, 7.824998694764690121 ) ) ;
#58653=CARTESIAN_POINT ( 'NONE',  ( 10.64393020684969926, 5.250000000000000000, 7.500000000000000000 ) ) ;
#58671=B_SPLINE_CURVE_WITH_KNOTS ( 'NONE', 3,
 ( #19701, #4295, #56766, #8863, #20727, #9891 ),
 .UNSPECIFIED., .F., .F.,
 ( 4, 1, 1, 4 ),
 ( 0.000000000000000000, 0.3333333333333000081, 0.6666666666667000474, 1.000000000000000000 ),
 .UNSPECIFIED. ) ;
#58673=CARTESIAN_POINT ( 'NONE',  ( 10.84393020684979980, 2.750000000000000000, 7.500000000000000000 ) ) ;
#58693=CIRCLE ( 'NONE', #21862, 0.7499999936418002555 ) ;
#58702=CARTESIAN_POINT ( 'NONE',  ( 11.24025954179439957, 4.771812902496799680, 6.858707791728399172 ) ) ;
#58718=CARTESIAN_POINT ( 'NONE',  ( 10.91195257254739914, 2.772832764353999835, 7.143100915737699452 ) ) ;
#58731=CARTESIAN_POINT ( 'NONE',  ( 10.57564694612699974, 3.068007311611700150, 7.128058497017000228 ) ) ;
#58757=VECTOR ( 'NONE', #19587, 1000.000000000000000 ) ;
#58760=CARTESIAN_POINT ( 'NONE',  ( 8.712501735000000025, 3.641148095589300304, 6.723921629386799381 ) ) ;
#58777=CARTESIAN_POINT ( 'NONE',  ( 9.222405316139999698, 3.815922504313999930, 6.652755395362000002 ) ) ;
#58812=CARTESIAN_POINT ( 'NONE',  ( 10.52799293566599914, 4.806678152079100208, 6.510429574318199464 ) ) ;
#58825=CARTESIAN_POINT ( 'NONE',  ( 9.605304848515999083, 5.163382381259999931, 6.968092280137199168 ) ) ;
#58834=CARTESIAN_POINT ( 'NONE',  ( 11.60000000000000320, 4.109635333090444043, 6.362414725044395425 ) ) ;
#58836=CARTESIAN_POINT ( 'NONE',  ( 9.454862456499625978, 4.412447805680870694, 8.271634030165902374 ) ) ;
#58856=ORIENTED_EDGE ( 'NONE', *, *, #63984, .F. ) ;
#58949=VECTOR ( 'NONE', #44855, 1000.000000000000000 ) ;
#59021=CARTESIAN_POINT ( 'NONE',  ( 8.789886373836322875, 4.000007821194420110, 6.560153657526067938 ) ) ;
#59050=CARTESIAN_POINT ( 'NONE',  ( 10.55103166480599874, 2.999015536536000504, 7.429424106427209296 ) ) ;
#59064=CARTESIAN_POINT ( 'NONE',  ( 10.27610941423800028, 4.844410192686099847, 8.266982106121901097 ) ) ;
#59078=CARTESIAN_POINT ( 'NONE',  ( 10.77256919669529900, 4.962345366016100101, 7.215672285280100517 ) ) ;
#59137=CARTESIAN_POINT ( 'NONE',  ( 11.49056651104150006, 4.085456792591960706, 8.361971998931499783 ) ) ;
#59153=CARTESIAN_POINT ( 'NONE',  ( 10.69057802013490033, 2.966773425016000054, 7.524052967375959966 ) ) ;
#59168=( NAMED_UNIT ( * ) SI_UNIT ( $, .STERADIAN. ) SOLID_ANGLE_UNIT ( ) );
#59183=CARTESIAN_POINT ( 'NONE',  ( 9.632166486775625813, 3.137137839323436594, 7.355082228165340297 ) ) ;
#59203=CARTESIAN_POINT ( 'NONE',  ( 10.48444474310099928, 5.015709705366000470, 7.007085334055199510 ) ) ;
#59214=ORIENTED_EDGE ( 'NONE', *, *, #534, .F. ) ;
#59244=ORIENTED_EDGE ( 'NONE', *, *, #7177, .F. ) ;
#59248=CARTESIAN_POINT ( 'NONE',  ( 9.533342523874999586, 3.007153757386999526, 7.651982363644999730 ) ) ;
#59253=CARTESIAN_POINT ( 'NONE',  ( 11.33830977893730108, 3.023401864784708515, 8.326430086672806041 ) ) ;
#59295=CARTESIAN_POINT ( 'NONE',  ( 11.31900581613029821, 4.750686773407899466, 7.017964743997199939 ) ) ;
#59307=B_SPLINE_CURVE_WITH_KNOTS ( 'NONE', 3,
 ( #19096, #8949, #30290, #9977, #3014, #30623, #61741, #13861, #35191, #56502, #8609, #3690, #29956, #51260, #47738, #27099, #32349, #37239, #69053, #53999, #32008, #36902, #68698, #52625, #38266, #27440, #5074, #5757, #21494, #15906 ),
 .UNSPECIFIED., .F., .F.,
 ( 4, 2, 1, 1, 2, 2, 2, 2, 2, 2, 2, 2, 2, 2, 2, 4 ),
 ( 0.000000000000000000, 0.1250000000000020817, 0.1875000000000028033, 0.2187500000000024702, 0.2343750000000020262, 0.2500000000000015543, 0.3750000000000015543, 0.4375000000000014433, 0.5000000000000013323, 0.5625000000000011102, 0.6250000000000009992, 0.6875000000000007772, 0.7500000000000005551, 0.8125000000000004441, 0.8750000000000002220, 1.000000000000000000 ),
 .UNSPECIFIED. ) ;
#59333=CARTESIAN_POINT ( 'NONE',  ( 10.09393020684899867, 5.250000000000000000, 7.500000000000000000 ) ) ;
#59380=CARTESIAN_POINT ( 'NONE',  ( 11.59999999999999964, 5.179498027601999510, 7.825000000000000178 ) ) ;
#59385=CARTESIAN_POINT ( 'NONE',  ( 10.69872335273220010, 4.349306362047499874, 6.559289673553299060 ) ) ;
#59402=CARTESIAN_POINT ( 'NONE',  ( 10.15303300763299887, 4.787165141710600480, 6.674373427955200277 ) ) ;
#59415=CARTESIAN_POINT ( 'NONE',  ( 9.541846873516668381, 4.999583552997725278, 6.731816600031356401 ) ) ;
#59416=CARTESIAN_POINT ( 'NONE',  ( 11.21564426047340035, 4.539962866738299851, 6.654192128557399499 ) ) ;
#59465=CARTESIAN_POINT ( 'NONE',  ( 9.349051052051999378, 4.850870049477099322, 7.333482423122699601 ) ) ;
#59477=CARTESIAN_POINT ( 'NONE',  ( 11.83518044953559922, 4.768048975940600620, 7.099502491684900107 ) ) ;
#59496=CARTESIAN_POINT ( 'NONE',  ( 10.60235971519489873, 4.605301262871499546, 8.506961598696999971 ) ) ;
#59517=FILL_AREA_STYLE ('',( #38185 ) ) ;
#59519=CARTESIAN_POINT ( 'NONE',  ( 10.67375944625267614, 3.325302618462734561, 6.944236520041479288 ) ) ;
#59528=CARTESIAN_POINT ( 'NONE',  ( 9.885457958598628636, 4.856131813426149968, 7.680473230592850697 ) ) ;
#59549=CARTESIAN_POINT ( 'NONE',  ( 11.05946005378019947, 5.036385109519999403, 8.053412743695298914 ) ) ;
#59551=CARTESIAN_POINT ( 'NONE',  ( 9.935646554150999066, 4.552790318865400643, 6.500921769151600138 ) ) ;
#59555=CARTESIAN_POINT ( 'NONE',  ( 10.64393020684969926, 5.250000000000000000, 7.500000000000000000 ) ) ;
#59599=CARTESIAN_POINT ( 'NONE',  ( 9.026759580228999269, 3.023107159668900312, 7.733500918284399894 ) ) ;
#59606=CARTESIAN_POINT ( 'NONE',  ( 9.434038493598999153, 4.627468580434300094, 8.098323595618600379 ) ) ;
#59645=CARTESIAN_POINT ( 'NONE',  ( 11.40211496860029783, 4.793947479907100018, 7.906860999147899527 ) ) ;
#59733=CARTESIAN_POINT ( 'NONE',  ( 10.77256919669529900, 4.962345366016100101, 7.215672285280100517 ) ) ;
#59749=CARTESIAN_POINT ( 'NONE',  ( 10.64118447801629941, 5.277702140407999565, 7.528171279442569919 ) ) ;
#59765=CARTESIAN_POINT ( 'NONE',  ( 10.94487616594229884, 3.696562859151900415, 8.456491899811199531 ) ) ;
#59767=CARTESIAN_POINT ( 'NONE',  ( 10.63559687351579974, 5.092232985442826099, 8.129523725463617012 ) ) ;
#59778=DIRECTION ( 'NONE',  ( -0.4999999999999719669, 0.6407827956774649891, -0.5825782426110679424 ) ) ;
#59787=ORIENTED_EDGE ( 'NONE', *, *, #10561, .T. ) ;
#59804=CARTESIAN_POINT ( 'NONE',  ( 11.16544712921906957, 3.267598948716616825, 7.017906594554381705 ) ) ;
#59829=CARTESIAN_POINT ( 'NONE',  ( 11.68748876160954886, 3.399618311400500303, 6.875627981711399883 ) ) ;
#59838=ORIENTED_EDGE ( 'NONE', *, *, #40642, .T. ) ;
#59843=CARTESIAN_POINT ( 'NONE',  ( 11.52166954483529793, 4.562096242626500597, 8.367285821793199574 ) ) ;
#59857=CARTESIAN_POINT ( 'NONE',  ( 11.58810207955109917, 3.203462856645999945, 7.825000000000000178 ) ) ;
#59862=CARTESIAN_POINT ( 'NONE',  ( 10.42760663304247615, 4.647051049978554005, 8.087719785218890678 ) ) ;
#59872=CARTESIAN_POINT ( 'NONE',  ( 9.353545867770625577, 4.858658389798049981, 7.331958223794097229 ) ) ;
#59892=CARTESIAN_POINT ( 'NONE',  ( 10.60746886766490071, 3.501664543805500074, 8.405426684175299812 ) ) ;
#59895=CARTESIAN_POINT ( 'NONE',  ( 9.355088727410999283, 2.725263018055000153, 7.393088754863899936 ) ) ;
#59924=ORIENTED_EDGE ( 'NONE', *, *, #67293, .T. ) ;
#59943=CARTESIAN_POINT ( 'NONE',  ( 9.609329965421999020, 3.302375896175799852, 6.777391592843399870 ) ) ;
#59951=CARTESIAN_POINT ( 'NONE',  ( 10.06525461470299909, 3.026595211686900377, 7.252360304610999897 ) ) ;
#60052=CARTESIAN_POINT ( 'NONE',  ( 11.46550210169813511, 3.941925478257526372, 6.192987292895718809 ) ) ;
#60066=B_SPLINE_CURVE_WITH_KNOTS ( 'NONE', 3,
 ( #57083, #42042, #46945, #26308 ),
 .UNSPECIFIED., .F., .F.,
 ( 4, 4 ),
 ( 0.000000000000000000, 1.000000000000000000 ),
 .UNSPECIFIED. ) ;
#60087=CARTESIAN_POINT ( 'NONE',  ( 11.33872066707849768, 4.858611803369300652, 8.019361746728900897 ) ) ;
#60112=LINE ( 'NONE', #29264, #11526 ) ;
#60118=CARTESIAN_POINT ( 'NONE',  ( 10.81764560330029923, 4.349570499512200428, 8.585859374935999710 ) ) ;
#60170=CARTESIAN_POINT ( 'NONE',  ( 8.943784697134999462, 4.470490447737899942, 8.228249052908999772 ) ) ;
#60185=CARTESIAN_POINT ( 'NONE',  ( 11.78594988689359901, 4.393436444036099786, 6.728309553046099012 ) ) ;
#60199=CARTESIAN_POINT ( 'NONE',  ( 11.40211496860029783, 4.793947479907100018, 7.906860999147899527 ) ) ;
#60216=CARTESIAN_POINT ( 'NONE',  ( 10.35376078907947495, 4.858294075600578132, 7.334408124199476298 ) ) ;
#60217=CARTESIAN_POINT ( 'NONE',  ( 9.310585478579783469, 3.370455731697034718, 8.592274333092914773 ) ) ;
#60222=EDGE_CURVE ( 'NONE', #15952, #61459, #32700, .T. ) ;
#60248=CARTESIAN_POINT ( 'NONE',  ( 11.01790547754519878, 5.174295865741999734, 7.462730980357120458 ) ) ;
#60250=CARTESIAN_POINT ( 'NONE',  ( 9.910317406968998100, 4.212364169857599983, 6.378110563671000044 ) ) ;
#60255=CARTESIAN_POINT ( 'NONE',  ( 10.62309687351639020, 5.217465845835395299, 7.172815144550900968 ) ) ;
#60295=CARTESIAN_POINT ( 'NONE',  ( 9.913279731609000223, 4.090130512164860122, 8.500359330993999762 ) ) ;
#60300=CARTESIAN_POINT ( 'NONE',  ( 10.11591290906799934, 3.364470222553300083, 6.722218404915299317 ) ) ;
#60390=VERTEX_POINT ( 'NONE', #55752 ) ;
#60430=CARTESIAN_POINT ( 'NONE',  ( 10.89149144726329865, 3.340422662105400065, 8.430724369296298093 ) ) ;
#60445=CARTESIAN_POINT ( 'NONE',  ( 9.035395982797805203, 3.688926447190844726, 6.345787448237017792 ) ) ;
#60462=CARTESIAN_POINT ( 'NONE',  ( 10.64533863405319991, 4.703785194191100416, 6.602238051205399749 ) ) ;
#60488=CARTESIAN_POINT ( 'NONE',  ( 9.201637546194751494, 4.272535203994794806, 8.730330573913894554 ) ) ;
#60517=CARTESIAN_POINT ( 'NONE',  ( 8.849999778957998942, 4.000000000000000000, 6.500000166194499940 ) ) ;
#60526=CARTESIAN_POINT ( 'NONE',  ( 11.28949010443639978, 5.000675062740000065, 7.425165037173959703 ) ) ;
#60555=CARTESIAN_POINT ( 'NONE',  ( 9.909870477708999204, 2.749999999999999556, 7.249610810850631637 ) ) ;
#60561=CARTESIAN_POINT ( 'NONE',  ( 9.383499245234510511, 2.750003956825025853, 7.663630899194567192 ) ) ;
#60590=CARTESIAN_POINT ( 'NONE',  ( 10.43614141025499897, 4.549633050978300730, 6.521048559232099251 ) ) ;
#60592=CARTESIAN_POINT ( 'NONE',  ( 10.31558376188599802, 3.037118682679400106, 6.886327436977599525 ) ) ;
#60639=CARTESIAN_POINT ( 'NONE',  ( 9.811963142879999822, 4.982812171771600518, 7.707177545471399327 ) ) ;
#60644=CARTESIAN_POINT ( 'NONE',  ( 8.750151519676999001, 4.018750234858180725, 6.633192605878799775 ) ) ;
#60766=CARTESIAN_POINT ( 'NONE',  ( 11.84388784977539899, 2.744254309011999737, 7.571757098260779806 ) ) ;
#60771=CARTESIAN_POINT ( 'NONE',  ( 10.52226222744799955, 3.119510978356100139, 6.774721295617600170 ) ) ;
#60777=EDGE_CURVE ( 'NONE', #51100, #64627, #7551, .T. ) ;
#60799=CARTESIAN_POINT ( 'NONE',  ( 9.635596873516668381, 5.092232985442826099, 8.129523725463617012 ) ) ;
#60808=CARTESIAN_POINT ( 'NONE',  ( 11.45764291764649911, 2.867875922590999771, 7.639947095788999221 ) ) ;
#60835=CARTESIAN_POINT ( 'NONE',  ( 9.120327454391752298, 5.191173620088457064, 7.911210609455967102 ) ) ;
#60875=CARTESIAN_POINT ( 'NONE',  ( 11.56025819896753859, 3.013900664291200293, 7.314099615601099558 ) ) ;
#60901=CARTESIAN_POINT ( 'NONE',  ( 9.973631561148998514, 3.315688435009791490, 6.424401362931538628 ) ) ;
#60905=CARTESIAN_POINT ( 'NONE',  ( 9.248087964304160025, 4.327168543240619947, 8.717422821756878548 ) ) ;
#60914=CARTESIAN_POINT ( 'NONE',  ( 8.948279512853625661, 4.474797027487648293, 8.234914996158446243 ) ) ;
#60937=CARTESIAN_POINT ( 'NONE',  ( 10.68546886766499959, 3.433493735705800187, 8.529286361367999447 ) ) ;
#60939=CARTESIAN_POINT ( 'NONE',  ( 9.074455549952999078, 4.888629236328500660, 8.216988513669100769 ) ) ;
#60985=CARTESIAN_POINT ( 'NONE',  ( 9.860608878791998322, 3.741427262966100287, 8.612148635591999835 ) ) ;
#60990=CARTESIAN_POINT ( 'NONE',  ( 9.662000818238999145, 3.232852935619000334, 7.096028062709999418 ) ) ;
#61030=CARTESIAN_POINT ( 'NONE',  ( 10.17349413291699811, 5.162701151235999930, 8.030511425625498134 ) ) ;
#61045=CARTESIAN_POINT ( 'NONE',  ( 11.01041369783139956, 3.935522326596939902, 6.223614866029000048 ) ) ;
#61066=CARTESIAN_POINT ( 'NONE',  ( 9.716846873515667227, 4.768183399968648040, 8.499583552997721725 ) ) ;
#61068=ORIENTED_EDGE ( 'NONE', *, *, #56965, .T. ) ;
#61071=B_SPLINE_CURVE_WITH_KNOTS ( 'NONE', 3,
 ( #58493, #37859, #48701, #802, #26693, #11624, #22118, #17224, #38549, #27374, #54633, #43463, #16188, #1151, #16874, #5354, #38198, #48008, #59528, #108, #10596, #32964, #21096, #22460, #6728, #48347, #31938, #49378, #59183, #54278, #53596, #53248, #63729, #37512, #21771, #58836, #15841, #43805, #65101, #59872, #11977, #11283, #37173, #10944, #32622, #21424, #5692, #453, #43107, #6036, #64408, #12332, #18616, #54981, #29469, #60914, #13380, #39591, #44508, #17929, #33663, #45188, #8468, #44159, #2192 ),
 .UNSPECIFIED., .F., .F.,
 ( 4, 1, 1, 1, 1, 1, 1, 1, 1, 1, 1, 1, 1, 1, 1, 1, 1, 1, 1, 1, 1, 1, 1, 1, 1, 1, 1, 1, 1, 1, 1, 1, 1, 1, 1, 1, 1, 1, 1, 1, 1, 1, 1, 1, 1, 1, 1, 1, 1, 1, 1, 1, 1, 1, 1, 1, 1, 1, 1, 1, 1, 1, 4 ),
 ( 0.000000000000000000, 0.01249986222369732156, 0.02874986775682976045, 0.04499987328996220282, 0.06124987882309464171, 0.07749988435622708061, 0.09374988988935951950, 0.1099998954224919584, 0.1262499009556244112, 0.1424999064887568501, 0.1587499120218892890, 0.1749999175550217279, 0.1912499230881541668, 0.2074999286212866056, 0.2237499341544190445, 0.2399999396875514834, 0.2562499452206838946, 0.2724999507538163890, 0.2887499562869488279, 0.3049999618200812668, 0.3212499673532136502, 0.3374999728863461446, 0.3537499784194785835, 0.3699999839526110224, 0.3862499894857434612, 0.4024999950188759001, 0.4187500005520083390, 0.4350000060851407779, 0.4512500116182732168, 0.4675000171514057112, 0.4837500226845380946, 0.5000000282176705335, 0.5162500337508029169, 0.5325000392839353003, 0.5487500448170677947, 0.5650000503502001781, 0.5812500558833327835, 0.5975000614164651669, 0.6137500669495975503, 0.6300000724827300447, 0.6462500780158624281, 0.6625000835489948114, 0.6787500890821273059, 0.6950000946152596892, 0.7112501001483922947, 0.7275001056815246780, 0.7437501112146570614, 0.7600001167477895558, 0.7762501222809219392, 0.7925001278140544336, 0.8087501333471868170, 0.8250001388803192004, 0.8412501444134518058, 0.8575001499465841892, 0.8737501554797166836, 0.8900001610128490670, 0.9062501665459814504, 0.9225001720791139448, 0.9387501776122463282, 0.9550001831453788226, 0.9712501886785112060, 0.9875001942116437004, 1.000000000000000000 ),
 .UNSPECIFIED. ) ;
#61123=CARTESIAN_POINT ( 'NONE',  ( 11.08841369783139896, 3.942447888101379583, 6.360711682373000109 ) ) ;
#61154=CARTESIAN_POINT ( 'NONE',  ( 11.01456785386839954, 3.053605396817899997, 6.863111178199799767 ) ) ;
#61194=CARTESIAN_POINT ( 'NONE',  ( 10.22934687351566474, 3.836375382625535124, 8.750000000000000000 ) ) ;
#61222=CARTESIAN_POINT ( 'NONE',  ( 11.21564426047340035, 4.539962866738299851, 6.654192128557399499 ) ) ;
#61285=CARTESIAN_POINT ( 'NONE',  ( 9.604355082327998616, 3.550486524676900402, 8.398209294002699110 ) ) ;
#61316=CARTESIAN_POINT ( 'NONE',  ( 9.143927823787139531, 5.249988444743198812, 7.500000155056751439 ) ) ;
#61326=EDGE_LOOP ( 'NONE', ( #59214, #2840, #42514, #5542 ) ) ;
#61330=CARTESIAN_POINT ( 'NONE',  ( 9.556659112603998807, 3.503852111758100296, 6.471616938597000157 ) ) ;
#61373=CARTESIAN_POINT ( 'NONE',  ( 10.88733729122639993, 2.722429312291999803, 7.533608309972310124 ) ) ;
#61388=CARTESIAN_POINT ( 'NONE',  ( 10.09964828895399869, 5.121614868497999851, 6.887384543790600056 ) ) ;
#61405=ORIENTED_EDGE ( 'NONE', *, *, #53352, .T. ) ;
#61409=CARTESIAN_POINT ( 'NONE',  ( 10.39393020684999946, 2.750000000000000000, 7.500000000000000000 ) ) ;
#61457=FACE_OUTER_BOUND ( 'NONE', #10426, .T. ) ;
#61459=VERTEX_POINT ( 'NONE', #49672 ) ;
#61462=CARTESIAN_POINT ( 'NONE',  ( 11.53148876160955005, 3.209326035813000022, 6.677731919207799294 ) ) ;
#61495=CARTESIAN_POINT ( 'NONE',  ( 11.69559063708295987, 5.086518862378000883, 7.194517870904999945 ) ) ;
#61497=CARTESIAN_POINT ( 'NONE',  ( 10.67726354018259904, 4.629523725463628558, 8.592232985442819881 ) ) ;
#61513=CARTESIAN_POINT ( 'NONE',  ( 10.08521345716899908, 4.924890298941200228, 6.659120737011199331 ) ) ;
#61523=CARTESIAN_POINT ( 'NONE',  ( 9.110163692916374956, 5.234200089434220438, 7.754438396796453858 ) ) ;
#61560=CARTESIAN_POINT ( 'NONE',  ( 11.78179573085659904, 4.973133828855400118, 7.331616337578100051 ) ) ;
#61575=CARTESIAN_POINT ( 'NONE',  ( 10.73724174883999893, 3.975468761016990094, 6.608211443991299561 ) ) ;
#61591=CARTESIAN_POINT ( 'NONE',  ( 9.002599499754321499, 5.050337702473633783, 7.001638755957637628 ) ) ;
#61607=LINE ( 'NONE', #51800, #58949 ) ;
#61618=CARTESIAN_POINT ( 'NONE',  ( 10.52946886766499901, 3.569835351907400423, 8.281567006984099422 ) ) ;
#61623=CARTESIAN_POINT ( 'NONE',  ( 9.427051052051998781, 4.985712601322500603, 7.307093369932900373 ) ) ;
#61657=CARTESIAN_POINT ( 'NONE',  ( 9.129282595918651211, 5.249943393780838186, 7.269976573734645342 ) ) ;
#61669=CARTESIAN_POINT ( 'NONE',  ( 9.252709346416999381, 5.031430618794000331, 7.989780896525600085 ) ) ;
#61677=CARTESIAN_POINT ( 'NONE',  ( 11.59999999999999964, 5.064318446328999634, 6.844464917182299324 ) ) ;
#61741=CARTESIAN_POINT ( 'NONE',  ( 11.59999999999999787, 4.834915812642035959, 8.298683811023389367 ) ) ;
#61743=CARTESIAN_POINT ( 'NONE',  ( 9.883513540182333301, 2.750000000000000000, 7.663624617374469317 ) ) ;
#61797=CARTESIAN_POINT ( 'NONE',  ( 11.31389666366019853, 3.954123449088899900, 6.467512203247999913 ) ) ;
#61802=CARTESIAN_POINT ( 'NONE',  ( 11.60533460557258323, 4.184174550317700358, 6.374224726731999802 ) ) ;
#61816=CARTESIAN_POINT ( 'NONE',  ( 9.041999884715581359, 3.843103124197280618, 6.308000049678228471 ) ) ;
#61827=CARTESIAN_POINT ( 'NONE',  ( 9.698096873516668381, 4.327184855449106138, 8.717465845835393523 ) ) ;
#61832=CARTESIAN_POINT ( 'NONE',  ( 10.44841638348500013, 2.891666689023999925, 7.769976643522699788 ) ) ;
#61842=VECTOR ( 'NONE', #39690, 1000.000000000000000 ) ;
#61876=CARTESIAN_POINT ( 'NONE',  ( 10.11476354018233081, 5.217465845835394411, 7.827184855449092815 ) ) ;
#61880=EDGE_LOOP ( 'NONE', ( #11846, #68599, #22019, #49984 ) ) ;
#61904=CARTESIAN_POINT ( 'NONE',  ( 11.24025954179439957, 4.771812902496799680, 6.858707791728399172 ) ) ;
#61920=CARTESIAN_POINT ( 'NONE',  ( 10.97364560330029981, 4.265439025801100570, 8.324524538096799375 ) ) ;
#61945=CARTESIAN_POINT ( 'NONE',  ( 10.39393020684999946, 2.750000000000000000, 7.500000000000000000 ) ) ;
#61968=CARTESIAN_POINT ( 'NONE',  ( 10.32169598648999909, 4.766524664146899681, 7.043598424555200133 ) ) ;
#61971=CARTESIAN_POINT ( 'NONE',  ( 10.08560887879199797, 3.772542739612499751, 8.478317686146800369 ) ) ;
#62015=CARTESIAN_POINT ( 'NONE',  ( 8.948759580228999866, 2.889471124893000287, 7.765443149353999708 ) ) ;
#62054=CARTESIAN_POINT ( 'NONE',  ( 11.00000000000000000, 2.941427501403999667, 7.174999999999999822 ) ) ;
#62125=CARTESIAN_POINT ( 'NONE',  ( 10.63880513895979973, 5.150451045932999961, 8.139542779846600240 ) ) ;
#62137=CARTESIAN_POINT ( 'NONE',  ( 11.39189666366029918, 3.947847673382490541, 6.326270943800999191 ) ) ;
#62141=B_SPLINE_CURVE_WITH_KNOTS ( 'NONE', 3,
 ( #16805, #43740, #44092, #33250 ),
 .UNSPECIFIED., .F., .F.,
 ( 4, 4 ),
 ( 0.000000000000000000, 1.000000000000000000 ),
 .UNSPECIFIED. ) ;
#62143=CARTESIAN_POINT ( 'NONE',  ( 10.88733729122639993, 2.722429312291999803, 7.533608309972310124 ) ) ;
#62172=CARTESIAN_POINT ( 'NONE',  ( 11.05964426047339799, 4.687693494822500639, 6.422784126663999338 ) ) ;
#62174=CARTESIAN_POINT ( 'NONE',  ( 10.69809687351599869, 4.327184855449106138, 8.717465845835393523 ) ) ;
#62180=DIRECTION ( 'NONE',  ( 0.000000000000000000, 1.000000000000000000, 0.000000000000000000 ) ) ;
#62244=CARTESIAN_POINT ( 'NONE',  ( 11.57240408529958842, 3.267527001822357224, 7.982112976485220557 ) ) ;
#62247=CARTESIAN_POINT ( 'NONE',  ( 11.55610404293055993, 3.497163090439000310, 6.476063885290000322 ) ) ;
#62257=DIRECTION ( 'NONE',  ( 1.000000000000000000, 0.000000000000000000, 0.000000000000000000 ) ) ;
#62260=CARTESIAN_POINT ( 'NONE',  ( 10.75210807141120029, 4.040019166404060336, 6.634727177901499573 ) ) ;
#62268=CARTESIAN_POINT ( 'NONE',  ( 11.39975833414730033, 4.796537143354000499, 7.825000000000000178 ) ) ;
#62296=CARTESIAN_POINT ( 'NONE',  ( 11.32299956498189886, 2.792989229543000107, 7.825000000000000178 ) ) ;
#62308=CARTESIAN_POINT ( 'NONE',  ( 10.28014141025500017, 4.417352327511700594, 6.756653759087999589 ) ) ;
#62310=CARTESIAN_POINT ( 'NONE',  ( 10.33890035061499901, 4.267716286314199969, 6.531924610394499453 ) ) ;
#62313=DIRECTION ( 'NONE',  ( 0.7071067388045961799, 0.7071068235684964121, -1.176037761303994353E-10 ) ) ;
#62355=ORIENTED_EDGE ( 'NONE', *, *, #41065, .F. ) ;
#62356=CARTESIAN_POINT ( 'NONE',  ( 10.06122949779699915, 4.709679768527199606, 6.435697190503999465 ) ) ;
#62442=ORIENTED_EDGE ( 'NONE', *, *, #25137, .T. ) ;
#62465=CARTESIAN_POINT ( 'NONE',  ( 11.68277869730536977, 3.468607053297499743, 8.547856079839998955 ) ) ;
#62473=CARTESIAN_POINT ( 'NONE',  ( 11.75203632436369894, 2.890282938442000127, 7.759151359668400083 ) ) ;
#62480=CARTESIAN_POINT ( 'NONE',  ( 10.12841772631199966, 4.490588993294299947, 6.490165927606000196 ) ) ;
#62513=CARTESIAN_POINT ( 'NONE',  ( 11.47810404293059960, 3.436653965247300047, 6.352848032645000309 ) ) ;
#62541=CARTESIAN_POINT ( 'NONE',  ( 10.59393020684899867, 5.250000000000000000, 7.500000000000000000 ) ) ;
#62548=ORIENTED_EDGE ( 'NONE', *, *, #63952, .T. ) ;
#62565=DIRECTION ( 'NONE',  ( 1.000000000000000000, 0.000000000000000000, 0.000000000000000000 ) ) ;
#62567=CARTESIAN_POINT ( 'NONE',  ( 11.19518313518939934, 3.462699341914400097, 6.820583637845799352 ) ) ;
#62582=CARTESIAN_POINT ( 'NONE',  ( 11.13764426047339917, 4.613828180779599997, 6.538488127609999978 ) ) ;
#62589=EDGE_CURVE ( 'NONE', #52961, #25295, #50032, .T. ) ;
#62594=CARTESIAN_POINT ( 'NONE',  ( 11.58902763632552002, 3.213494089586499847, 7.862914650060299770 ) ) ;
#62624=CARTESIAN_POINT ( 'NONE',  ( 8.969356963619999235, 2.880642974985999860, 7.500000000085178087 ) ) ;
#62640=CARTESIAN_POINT ( 'NONE',  ( 8.945797255587999430, 5.003512473869000665, 7.542485555928779561 ) ) ;
#62688=CARTESIAN_POINT ( 'NONE',  ( 9.858596320338998353, 2.815618218644000414, 7.983346856269500691 ) ) ;
#62692=VECTOR ( 'NONE', #53922, 1000.000000000000000 ) ;
#62719=CARTESIAN_POINT ( 'NONE',  ( 10.19095058442699830, 4.507735863714500191, 8.674133161175999973 ) ) ;
#62736=LINE ( 'NONE', #8581, #34265 ) ;
#62759=CARTESIAN_POINT ( 'NONE',  ( 11.00000000000000000, 4.991767524623399233, 7.825000000000000178 ) ) ;
#62772=FACE_OUTER_BOUND ( 'NONE', #9113, .T. ) ;
#62774=EDGE_CURVE ( 'NONE', #52369, #16060, #48280, .T. ) ;
#62814=CARTESIAN_POINT ( 'NONE',  ( 11.30878751119029957, 2.958974835389999836, 6.955365841266999638 ) ) ;
#62819=CARTESIAN_POINT ( 'NONE',  ( 10.64118447801629941, 5.277702140407999565, 7.528171279442569919 ) ) ;
#62836=FACE_OUTER_BOUND ( 'NONE', #55087, .T. ) ;
#62850=CARTESIAN_POINT ( 'NONE',  ( 11.37964291764649971, 2.731641218595000087, 7.656787697937099679 ) ) ;
#62854=CARTESIAN_POINT ( 'NONE',  ( 10.74809687351632448, 4.327184855449106138, 8.717465845835393523 ) ) ;
#62870=ORIENTED_EDGE ( 'NONE', *, *, #63984, .T. ) ;
#62877=DIRECTION ( 'NONE',  ( 0.000000000000000000, 1.000000000000000000, 0.000000000000000000 ) ) ;
#62902=DIRECTION ( 'NONE',  ( 0.000000000000000000, 0.000000000000000000, -1.000000000000000000 ) ) ;
#62904=CARTESIAN_POINT ( 'NONE',  ( 11.04749144726329924, 3.499163784537000055, 8.206726025856399431 ) ) ;
#62920=CARTESIAN_POINT ( 'NONE',  ( 10.84226088462129844, 4.002427228022017225, 8.640738455926999961 ) ) ;
#62932=CARTESIAN_POINT ( 'NONE',  ( 11.61364291764652812, 3.140345330584100036, 7.606265891492399511 ) ) ;
#62978=CARTESIAN_POINT ( 'NONE',  ( 9.779646554150998483, 4.419749732651400365, 6.741370903243699253 ) ) ;
#63008=CARTESIAN_POINT ( 'NONE',  ( 11.43345123989529810, 4.540230239159599890, 6.456682674800999777 ) ) ;
#63014=ORIENTED_EDGE ( 'NONE', *, *, #22830, .F. ) ;
#63021=CARTESIAN_POINT ( 'NONE',  ( 9.453329965421998438, 3.111510091554099855, 6.579690231462300254 ) ) ;
#63030=CARTESIAN_POINT ( 'NONE',  ( 11.59999999999999964, 4.924024592270519918, 6.664392815890117561 ) ) ;
#63054=CARTESIAN_POINT ( 'NONE',  ( 9.861671671056999600, 2.738456190347000163, 7.288123611975898974 ) ) ;
#63074=DIRECTION ( 'NONE',  ( -1.000000000000000000, 0.000000000000000000, 0.000000000000000000 ) ) ;
#63095=CARTESIAN_POINT ( 'NONE',  ( 11.11486084871780022, 5.207010770456999893, 7.825000000000000178 ) ) ;
#63152=CARTESIAN_POINT ( 'NONE',  ( 10.63880513895979973, 5.150451045932999961, 8.139542779846600240 ) ) ;
#63157=CARTESIAN_POINT ( 'NONE',  ( 10.59195391537400077, 5.057233422790000432, 6.781965272201699868 ) ) ;
#63247=CARTESIAN_POINT ( 'NONE',  ( 10.33364828895399867, 4.760196147278000112, 7.084788038520800413 ) ) ;
#63261=CARTESIAN_POINT ( 'NONE',  ( 11.46253286130405691, 4.338994305312701805, 8.308656198582323071 ) ) ;
#63263=CARTESIAN_POINT ( 'NONE',  ( 11.35918179236250047, 3.761636028845500412, 8.615559381441000752 ) ) ;
#63324=CARTESIAN_POINT ( 'NONE',  ( 9.602342523874998648, 3.142972170141900001, 7.631191628371899682 ) ) ;
#63358=CARTESIAN_POINT ( 'NONE',  ( 11.22567835872029995, 3.006051690924700370, 8.126439557340900066 ) ) ;
#63375=CARTESIAN_POINT ( 'NONE',  ( 9.276025935145998602, 3.814256956409300070, 8.765655525501999890 ) ) ;
#63388=CARTESIAN_POINT ( 'NONE',  ( 8.857090631127384484, 4.619515535681817830, 8.304725771527001754 ) ) ;
#63389=ADVANCED_FACE ( 'NONE', ( #62772 ), #68360, .F. ) ;
#63408=CARTESIAN_POINT ( 'NONE',  ( 9.583051052052001140, 5.255397705012999410, 7.254315263553399618 ) ) ;
#63457=DIRECTION ( 'NONE',  ( -1.000000000000000000, 0.000000000000000000, -1.233561263588000078E-14 ) ) ;
#63461=CARTESIAN_POINT ( 'NONE',  ( 10.14393020684899938, 5.250000000000000000, 7.500000000000000000 ) ) ;
#63464=ORIENTED_EDGE ( 'NONE', *, *, #66781, .F. ) ;
#63473=EDGE_CURVE ( 'NONE', #43200, #23962, #42160, .T. ) ;
#63504=CARTESIAN_POINT ( 'NONE',  ( 10.60746886766490071, 3.501664543805500074, 8.405426684175299812 ) ) ;
#63511=CARTESIAN_POINT ( 'NONE',  ( 11.30579707368350029, 3.365167912142600137, 8.609190966793999422 ) ) ;
#63514=ORIENTED_EDGE ( 'NONE', *, *, #6125, .T. ) ;
#63549=CARTESIAN_POINT ( 'NONE',  ( 10.72726354018300121, 4.629523725463627670, 8.592232985442818105 ) ) ;
#63568=ORIENTED_EDGE ( 'NONE', *, *, #534, .T. ) ;
#63596=CARTESIAN_POINT ( 'NONE',  ( 10.48133997687999930, 4.184599793140999502, 8.346298710230199092 ) ) ;
#63614=CARTESIAN_POINT ( 'NONE',  ( 10.40333997687999990, 4.213854445120500003, 8.480416814141699788 ) ) ;
#63626=B_SPLINE_CURVE_WITH_KNOTS ( 'NONE', 3,
 ( #27992, #61523, #60835, #66069, #39165, #39862, #34275, #60488, #49652, #8040, #18879, #12598, #55595, #28330, #34625, #1757, #50348, #33925 ),
 .UNSPECIFIED., .F., .F.,
 ( 4, 2, 2, 2, 2, 2, 2, 2, 4 ),
 ( 0.000000000000000000, 0.1250000000000000000, 0.2500000000000000000, 0.3750000000000000000, 0.5000000000000000000, 0.6250000000000000000, 0.7500000000000000000, 0.8750000000000000000, 1.000000000000000000 ),
 .UNSPECIFIED. ) ;
#63629=CARTESIAN_POINT ( 'NONE',  ( 11.06795257254739973, 3.036453385827900142, 7.219770138693499817 ) ) ;
#63639=CARTESIAN_POINT ( 'NONE',  ( 11.10391045180383962, 5.129049487418003928, 6.885461205208883051 ) ) ;
#63672=CARTESIAN_POINT ( 'NONE',  ( 8.920468108405998464, 4.966402032527499344, 7.226304214866999587 ) ) ;
#63703=B_SPLINE_CURVE_WITH_KNOTS ( 'NONE', 3,
 ( #57948, #31727, #57591, #31383, #9017, #52695 ),
 .UNSPECIFIED., .F., .F.,
 ( 4, 2, 4 ),
 ( 0.000000000000000000, 0.5000000000000000000, 1.000000000000000000 ),
 .UNSPECIFIED. ) ;
#63720=CARTESIAN_POINT ( 'NONE',  ( 9.402671671056999969, 2.738456190347000163, 7.288123611975898974 ) ) ;
#63727=CARTESIAN_POINT ( 'NONE',  ( 11.59999999999999964, 4.738901876697420690, 6.529275711103850632 ) ) ;
#63729=CARTESIAN_POINT ( 'NONE',  ( 9.530849898046625412, 3.608426922415753690, 8.282433891029866047 ) ) ;
#63750=DIRECTION ( 'NONE',  ( -1.000000000000000000, 0.000000000000000000, 0.000000000000000000 ) ) ;
#63752=CARTESIAN_POINT ( 'NONE',  ( 10.49490035061499782, 4.340961869598300105, 6.267064942904999825 ) ) ;
#63798=CARTESIAN_POINT ( 'NONE',  ( 11.20596535229475776, 3.091087823720314987, 7.175015064079871330 ) ) ;
#63844=AXIS2_PLACEMENT_3D ( 'NONE', #6387, #31945, #27043 ) ;
#63847=CARTESIAN_POINT ( 'NONE',  ( 10.35814141025499957, 4.483492689244800822, 6.638851159159999682 ) ) ;
#63852=CARTESIAN_POINT ( 'NONE',  ( 10.05862282008599884, 4.666276081381299790, 6.425317846273999933 ) ) ;
#63938=CARTESIAN_POINT ( 'NONE',  ( 10.77672335273219950, 4.301522290735800169, 6.687976048055599421 ) ) ;
#63952=EDGE_CURVE ( 'NONE', #25385, #45676, #7366, .T. ) ;
#63953=CARTESIAN_POINT ( 'NONE',  ( 11.55194988689359903, 4.580487242693600081, 6.361426117087999543 ) ) ;
#63965=CARTESIAN_POINT ( 'NONE',  ( 11.56025819896753859, 3.013900664291200293, 7.314099615601099558 ) ) ;
#63984=EDGE_CURVE ( 'NONE', #56577, #50051, #15419, .T. ) ;
#64011=CARTESIAN_POINT ( 'NONE',  ( 10.16476354018241501, 5.217465845835396188, 7.827184855449094592 ) ) ;
#64013=CARTESIAN_POINT ( 'NONE',  ( 8.715822372493999382, 3.750788346126100237, 6.684745346084599582 ) ) ;
#64041=CARTESIAN_POINT ( 'NONE',  ( 10.72191429142990060, 4.025072603369280522, 8.816028813488999916 ) ) ;
#64055=CARTESIAN_POINT ( 'NONE',  ( 8.499265421555000088, 3.759926620436100375, 6.258138488953999712 ) ) ;
#64086=DIRECTION ( 'NONE',  ( -1.000000000000000000, 0.000000000000000000, 0.000000000000000000 ) ) ;
#64094=CARTESIAN_POINT ( 'NONE',  ( 9.405747021775999528, 3.038503783616799847, 6.656252755052399550 ) ) ;
#64189=CARTESIAN_POINT ( 'NONE',  ( 11.60988784977536348, 3.148894096305599799, 7.548634759728509280 ) ) ;
#64277=CARTESIAN_POINT ( 'NONE',  ( 11.75718044953559804, 4.889766368533900120, 7.036033215662999218 ) ) ;
#64290=CARTESIAN_POINT ( 'NONE',  ( 11.35502763632549872, 2.839566963815999934, 8.035454525731699604 ) ) ;
#64305=CARTESIAN_POINT ( 'NONE',  ( 10.43210941423799909, 4.641185166475500168, 8.082391773166900606 ) ) ;
#64308=CARTESIAN_POINT ( 'NONE',  ( 9.643930206848999376, 5.250000000000000000, 7.500000000000000000 ) ) ;
#64354=CARTESIAN_POINT ( 'NONE',  ( 11.00000000000000000, 3.031410575668799900, 7.825000000000000178 ) ) ;
#64382=CARTESIAN_POINT ( 'NONE',  ( 10.85679632507500081, 4.490665650747399873, 6.590394082213600235 ) ) ;
#64399=CARTESIAN_POINT ( 'NONE',  ( 10.57529832096847677, 3.253995305422127782, 7.955594773867785463 ) ) ;
#64408=CARTESIAN_POINT ( 'NONE',  ( 9.074925248765625341, 3.255423617190434271, 7.959497855362744012 ) ) ;
#64432=CARTESIAN_POINT ( 'NONE',  ( 8.958265421554999719, 3.759926620436100375, 6.258138488953999712 ) ) ;
#64481=CARTESIAN_POINT ( 'NONE',  ( 9.761304848515999666, 4.913464051101100516, 7.082356937474298952 ) ) ;
#64528=CARTESIAN_POINT ( 'NONE',  ( 10.85679632507500081, 4.490665650747399873, 6.590394082213600235 ) ) ;
#64535=CARTESIAN_POINT ( 'NONE',  ( 10.17349413291699811, 5.162701151235999930, 8.030511425625498134 ) ) ;
#64540=EDGE_CURVE ( 'NONE', #34343, #46967, #33129, .T. ) ;
#64624=CARTESIAN_POINT ( 'NONE',  ( 10.37872469555899890, 4.502158848185001006, 8.368784980615899372 ) ) ;
#64627=VERTEX_POINT ( 'NONE', #6729 ) ;
#64641=CARTESIAN_POINT ( 'NONE',  ( 10.30072469555899950, 4.570852684939899824, 8.487632181750699445 ) ) ;
#64642=ORIENTED_EDGE ( 'NONE', *, *, #48137, .F. ) ;
#64654=CARTESIAN_POINT ( 'NONE',  ( 9.521013540183334456, 4.768183399968643599, 6.500416447002272946 ) ) ;
#64656=CARTESIAN_POINT ( 'NONE',  ( 11.51102763632551884, 3.088851714329700293, 7.920427941950599404 ) ) ;
#64669=CARTESIAN_POINT ( 'NONE',  ( 11.57299956498156845, 5.207010770456999893, 7.174999999999999822 ) ) ;
#64714=CARTESIAN_POINT ( 'NONE',  ( 10.82595391537419971, 4.716560378569699452, 7.013338090450799811 ) ) ;
#64728=CARTESIAN_POINT ( 'NONE',  ( 10.37199293566600034, 4.633387186021100668, 6.723009541442299231 ) ) ;
#64779=CARTESIAN_POINT ( 'NONE',  ( 11.10612378248509913, 3.517039242046199998, 8.413720204863100349 ) ) ;
#64781=CARTESIAN_POINT ( 'NONE',  ( 9.479721904869998994, 4.995641764568400589, 6.941043897400199114 ) ) ;
#64785=CARTESIAN_POINT ( 'NONE',  ( 10.41476354018330852, 2.782534154164605589, 7.172815144550902744 ) ) ;
#64798=ORIENTED_EDGE ( 'NONE', *, *, #36615, .T. ) ;
#64829=CARTESIAN_POINT ( 'NONE',  ( 10.01258376188599897, 3.037118682679400106, 6.886327436977599525 ) ) ;
#64866=ORIENTED_EDGE ( 'NONE', *, *, #38092, .T. ) ;
#64875=CARTESIAN_POINT ( 'NONE',  ( 10.98146005378009882, 4.911671201000399556, 7.986817550794899745 ) ) ;
#64918=CARTESIAN_POINT ( 'NONE',  ( 10.45551210286900279, 3.782771630962270759, 6.243812680477911492 ) ) ;
#64963=CARTESIAN_POINT ( 'NONE',  ( 11.31410538575739899, 4.975963290822400076, 7.733337754805098996 ) ) ;
#64978=CARTESIAN_POINT ( 'NONE',  ( 10.83810672858429847, 2.978701842912999886, 8.268288002587098617 ) ) ;
#64991=CARTESIAN_POINT ( 'NONE',  ( 10.96949144726329806, 3.419793223320000131, 8.318725197575499664 ) ) ;
#64995=CARTESIAN_POINT ( 'NONE',  ( 10.61476354018239832, 5.217465845835394411, 7.827184855449092815 ) ) ;
#65032=CARTESIAN_POINT ( 'NONE',  ( 11.18114303127866727, 3.379301870158037069, 6.880574739649332194 ) ) ;
#65055=CARTESIAN_POINT ( 'NONE',  ( 11.51518179236248862, 3.819003318705799899, 8.347076615013298451 ) ) ;
#65070=CARTESIAN_POINT ( 'NONE',  ( 11.52677869730533011, 3.596497913043499750, 8.295667533166499297 ) ) ;
#65101=CARTESIAN_POINT ( 'NONE',  ( 9.378875014952626543, 4.868116531169106587, 7.609114422657746069 ) ) ;
#65125=CARTESIAN_POINT ( 'NONE',  ( 10.69057802013490033, 2.966773425016000054, 7.524052967375959966 ) ) ;
#65127=CARTESIAN_POINT ( 'NONE',  ( 9.000480666858997836, 4.426512626096299918, 6.293984733123999753 ) ) ;
#65178=CARTESIAN_POINT ( 'NONE',  ( 8.798797255587999189, 5.003512473869000665, 7.542485555928790220 ) ) ;
#65184=CARTESIAN_POINT ( 'NONE',  ( 10.16657120343299958, 3.951311476804090006, 6.496769302834999316 ) ) ;
#65245=CARTESIAN_POINT ( 'NONE',  ( 8.599999952505998024, 4.000000000000000000, 6.750000006358199300 ) ) ;
#65317=CARTESIAN_POINT ( 'NONE',  ( 10.92026088462129962, 4.002135146349410810, 8.503467136482999678 ) ) ;
#65334=CARTESIAN_POINT ( 'NONE',  ( 11.15810538575740019, 5.242981041160000188, 7.797177576385699638 ) ) ;
#65350=CARTESIAN_POINT ( 'NONE',  ( 10.91610672858429965, 3.088399709291500095, 8.185766014210599906 ) ) ;
#65354=CARTESIAN_POINT ( 'NONE',  ( 8.731616107288068918, 4.000002263255225898, 6.618420992905501343 ) ) ;
#65398=CARTESIAN_POINT ( 'NONE',  ( 9.095759580228998331, 3.156743194445300382, 7.701558687214699717 ) ) ;
#65413=CARTESIAN_POINT ( 'NONE',  ( 11.26902897915239876, 4.221721321201099997, 6.662660017635100296 ) ) ;
#65428=CARTESIAN_POINT ( 'NONE',  ( 10.72702344389999851, 2.995605560827999891, 8.109550315577399360 ) ) ;
#65475=CARTESIAN_POINT ( 'NONE',  ( 10.48280513895999988, 4.903310631086600146, 8.002155910165599906 ) ) ;
#65479=CARTESIAN_POINT ( 'NONE',  ( 9.101797255588000013, 5.278067516796999925, 7.554109351283189611 ) ) ;
#65489=CYLINDRICAL_SURFACE ( 'NONE', #17599, 1.250000000000000222 ) ;
#65526=CARTESIAN_POINT ( 'NONE',  ( 9.659988259785999176, 3.868581654116200141, 6.504223158184999853 ) ) ;
#65535=CARTESIAN_POINT ( 'NONE',  ( 9.788646554150998824, 4.419749732651400365, 6.741370903243699253 ) ) ;
#65618=AXIS2_PLACEMENT_3D ( 'NONE', #10752, #27189, #6541 ) ;
#65633=CARTESIAN_POINT ( 'NONE',  ( 9.893930206848997599, 2.750000000000000000, 7.500000000000000000 ) ) ;
#65644=ADVANCED_FACE ( 'NONE', ( #40785 ), #46038, .T. ) ;
#65660=CARTESIAN_POINT ( 'NONE',  ( 11.13746005378019888, 5.161099018038999731, 8.120007936598501175 ) ) ;
#65665=CARTESIAN_POINT ( 'NONE',  ( 11.01872200990539952, 3.052519557825900343, 7.830502140005199507 ) ) ;
#65697=CARTESIAN_POINT ( 'NONE',  ( 10.69456919669529960, 5.093991349577000172, 7.176777099639999768 ) ) ;
#65752=CARTESIAN_POINT ( 'NONE',  ( 8.807788144226000426, 4.090932644426789722, 6.546538158064899804 ) ) ;
#65762=CARTESIAN_POINT ( 'NONE',  ( 10.57980110216399972, 3.260758259645400337, 7.951464549725199227 ) ) ;
#65774=CARTESIAN_POINT ( 'NONE',  ( 10.60746886766490071, 3.501664543805500074, 8.405426684175299812 ) ) ;
#65787=CARTESIAN_POINT ( 'NONE',  ( 9.925810748568999031, 2.827416853083249304, 6.999756549658379789 ) ) ;
#65805=B_SPLINE_SURFACE_WITH_KNOTS ( 'NONE', 3, 3, ( 
 ( #34891, #56548, #30334, #24735, #23701, #8654, #46062, #29308, #29660, #14251, #35579, #24392, #50961, #51641, #3059, #34556, #50620, #54357, #23929, #54709, #22540, #43880, #27809, #65535, #28496, #49115, #18005, #34439, #60990, #39671, #44239, #55753, #49811, #1229, #65879, #7498, #12409, #59606, #55404, #11704, #28853, #33392, #39323, #6461, #23243, #18348, #1922, #6808, #38983, #50500, #33043, #22888, #17660, #16946, #50161, #2264, #23582, #44921, #49457, #12062, #45265, #13108, #7158, #7855, #60644, #66226, #55056 ),
 ( #2598, #12757, #38629, #29189, #38279, #65184, #28145, #60300, #17304, #59951, #1568, #33742, #44586, #34086, #36494, #60295, #22533, #44234, #49452, #60639, #55396, #64481, #34081, #28138, #27446, #65526, #55050, #59943, #37929, #33734, #59248, #7153, #11697, #17654, #54005, #1561, #65872, #22883, #33037, #17297, #28847, #11354, #1220, #43872, #16604, #28488, #49806, #1916, #23236, #27803, #59599, #2259, #17997, #54703, #39317, #38977, #44580, #33387, #12403, #65178, #38622, #54349, #32692, #6107, #7492, #12750, #12054 ),
 ( #878, #48770, #22193, #50155, #6801, #16939, #23573, #43530, #64829, #38272, #6453, #49109, #51188, #50492, #60985, #18683, #13100, #35792, #3284, #45937, #2937, #40686, #24953, #34771, #3957, #29881, #61330, #24614, #44916, #14128, #39662, #8878, #13450, #7848, #55748, #30213, #50840, #56080, #61669, #13784, #40016, #8189, #29183, #2593, #19363, #23924, #35455, #66220, #51518, #56429, #62015, #57107, #51861, #46285, #35117, #29539, #66564, #45259, #24266, #19713, #45603, #66907, #19022, #8533, #67248, #3618, #56780 ),
 ( #40348, #67589, #41033, #62356, #14474, #30547, #9205, #18343, #34432, #46971, #41720, #62688, #20739, #25296, #20053, #47315, #42067, #52900, #21417, #42752, #31582, #58825, #4997, #68274, #31927, #10934, #53240, #63021, #4647, #63720, #30893, #14811, #46631, #26335, #63375, #20394, #5339, #15499, #15833, #41381, #26684, #21086, #47658, #52206, #36130, #15151, #57444, #16176, #68973, #42413, #52550, #37163, #48000, #36472, #53587, #10244, #57792, #58484, #67937, #10588, #9552, #98, #9904, #4307, #25641, #64055, #31243 ) ),
 .UNSPECIFIED., .F., .F., .F.,
 ( 4, 4 ),
 ( 4, 1, 1, 1, 1, 1, 1, 1, 1, 1, 1, 1, 1, 1, 1, 1, 1, 1, 1, 1, 1, 1, 1, 1, 1, 1, 1, 1, 1, 1, 1, 1, 1, 1, 1, 1, 1, 1, 1, 1, 1, 1, 1, 1, 1, 1, 1, 1, 1, 1, 1, 1, 1, 1, 1, 1, 1, 1, 1, 1, 1, 1, 1, 1, 4 ),
 ( -0.02000000000000000042, 1.020000000000000018 ),
 ( -0.02000000000000000042, -0.003749999999999999861, 0.01250000000000000069, 0.02875000000000000125, 0.04499999999999999833, 0.06124999999999999889, 0.07749999999999999944, 0.09375000000000000000, 0.1100000000000000006, 0.1262500000000000011, 0.1424999999999999878, 0.1587500000000000022, 0.1749999999999999889, 0.1912500000000000033, 0.2074999999999999900, 0.2237500000000000044, 0.2399999999999999911, 0.2562499999999999778, 0.2725000000000000200, 0.2887500000000000067, 0.3049999999999999933, 0.3212499999999999800, 0.3375000000000000222, 0.3537500000000000089, 0.3699999999999999956, 0.3862499999999999822, 0.4025000000000000244, 0.4187500000000000111, 0.4349999999999999978, 0.4512499999999999845, 0.4675000000000000266, 0.4837500000000000133, 0.5000000000000000000, 0.5162499999999999867, 0.5324999999999999734, 0.5487499999999999600, 0.5649999999999999467, 0.5812500000000000444, 0.5975000000000000311, 0.6137500000000000178, 0.6300000000000000044, 0.6462499999999999911, 0.6624999999999999778, 0.6787499999999999645, 0.6949999999999999512, 0.7112500000000000488, 0.7275000000000000355, 0.7437500000000000222, 0.7600000000000000089, 0.7762499999999999956, 0.7924999999999999822, 0.8087499999999999689, 0.8249999999999999556, 0.8412500000000000533, 0.8575000000000000400, 0.8737500000000000266, 0.8900000000000000133, 0.9062500000000000000, 0.9224999999999999867, 0.9387499999999999734, 0.9549999999999999600, 0.9712499999999999467, 0.9875000000000000444, 1.003749999999999920, 1.020000000000000018 ),
 .UNSPECIFIED. ) ;
#65823=CARTESIAN_POINT ( 'NONE',  ( 10.44999293566599974, 4.720032669050099550, 6.616719557880299085 ) ) ;
#65825=CARTESIAN_POINT ( 'NONE',  ( 9.127126402770999292, 5.196937059091999878, 7.951360234587600218 ) ) ;
#65829=UNCERTAINTY_MEASURE_WITH_UNIT (LENGTH_MEASURE( 1.000000000000000082E-05 ), #52898, 'distance_accuracy_value', 'NONE');
#65830=CARTESIAN_POINT ( 'NONE',  ( 10.44601354018326944, 3.000416447002273834, 6.731816600031359066 ) ) ;
#65831=ORIENTED_EDGE ( 'NONE', *, *, #68408, .T. ) ;
#65832=EDGE_CURVE ( 'NONE', #14332, #26661, #58693, .T. ) ;
#65872=CARTESIAN_POINT ( 'NONE',  ( 9.381367640780998940, 4.473477001189199775, 8.385811396220899994 ) ) ;
#65874=CARTESIAN_POINT ( 'NONE',  ( 9.529346873515667227, 4.163624617374466652, 6.250000000000000000 ) ) ;
#65879=CARTESIAN_POINT ( 'NONE',  ( 9.510025935145998588, 3.874109063559000088, 8.357822485499299958 ) ) ;
#65932=ORIENTED_EDGE ( 'NONE', *, *, #63473, .T. ) ;
#65959=EDGE_CURVE ( 'NONE', #33463, #21890, #3089, .T. ) ;
#66001=CARTESIAN_POINT ( 'NONE',  ( 11.76077869730539938, 3.404661623424200201, 8.673950353177000139 ) ) ;
#66007=CARTESIAN_POINT ( 'NONE',  ( 10.66995391537419913, 4.943675741382899780, 6.859089544950699668 ) ) ;
#66033=CARTESIAN_POINT ( 'NONE',  ( 9.646013540183334456, 4.999583552997728830, 8.268183399968640046 ) ) ;
#66039=CARTESIAN_POINT ( 'NONE',  ( 10.57149279008999798, 3.703313553258400059, 6.398515879103999993 ) ) ;
#66054=VERTEX_POINT ( 'NONE', #34015 ) ;
#66064=CARTESIAN_POINT ( 'NONE',  ( 8.748004441081999261, 3.610923974646400136, 6.658556819429599649 ) ) ;
#66069=CARTESIAN_POINT ( 'NONE',  ( 9.140654977342494547, 5.049579698492543400, 8.197403194024859729 ) ) ;
#66109=CARTESIAN_POINT ( 'NONE',  ( 11.41256651104150066, 4.098999650273559503, 8.498573944230598087 ) ) ;
#66129=EDGE_CURVE ( 'NONE', #15952, #8994, #15686, .T. ) ;
#66143=CARTESIAN_POINT ( 'NONE',  ( 9.164757945270769923, 5.217425660116052022, 7.827174490145248242 ) ) ;
#66171=EDGE_LOOP ( 'NONE', ( #63014, #34441, #27792, #59924, #33883 ) ) ;
#66172=CARTESIAN_POINT ( 'NONE',  ( 11.51656039236534923, 5.173498198882000132, 7.442888368925779652 ) ) ;
#66174=CARTESIAN_POINT ( 'NONE',  ( 8.998468108405997867, 5.098602956001000663, 7.188863445572599709 ) ) ;
#66220=CARTESIAN_POINT ( 'NONE',  ( 9.024747021775999301, 3.141778309999299967, 6.746879837742599584 ) ) ;
#66226=CARTESIAN_POINT ( 'NONE',  ( 8.733265421555000074, 3.837285628664199866, 6.658304367510099908 ) ) ;
#66264=CARTESIAN_POINT ( 'NONE',  ( 10.05862282008599884, 4.666276081381299790, 6.425317846273999933 ) ) ;
#66298=CARTESIAN_POINT ( 'NONE',  ( 9.696013540182335078, 4.999583552997727054, 8.268183399968641822 ) ) ;
#66354=CARTESIAN_POINT ( 'NONE',  ( 11.23610538575739959, 5.109472165990999848, 7.765257665594799796 ) ) ;
#66388=CARTESIAN_POINT ( 'NONE',  ( 11.11302897915239818, 4.291996373817799970, 6.397263297997000109 ) ) ;
#66395=CYLINDRICAL_SURFACE ( 'NONE', #50871, 1.250000000000000222 ) ;
#66455=CARTESIAN_POINT ( 'NONE',  ( 10.87103032197929942, 4.583685623598699799, 8.316248703309600643 ) ) ;
#66466=CARTESIAN_POINT ( 'NONE',  ( 8.784678295047998020, 4.000000000000000000, 7.500000000000000000 ) ) ;
#66467=CARTESIAN_POINT ( 'NONE',  ( 10.28014141025500017, 4.417352327511700594, 6.756653759087999589 ) ) ;
#66487=ORIENTED_EDGE ( 'NONE', *, *, #50582, .F. ) ;
#66513=CARTESIAN_POINT ( 'NONE',  ( 11.15278751119019773, 3.209519379020799867, 7.086443476450299706 ) ) ;
#66515=CARTESIAN_POINT ( 'NONE',  ( 9.553696787962998371, 4.172481380750499902, 8.489491017455099708 ) ) ;
#66564=CARTESIAN_POINT ( 'NONE',  ( 8.796784697134999220, 4.619613413415000203, 8.459069166353199165 ) ) ;
#66574=CARTESIAN_POINT ( 'NONE',  ( 11.59999999999999964, 3.116215992411100366, 7.174999999999999822 ) ) ;
#66605=DIRECTION ( 'NONE',  ( -1.000000000000000000, 0.000000000000000000, -3.164702532202999971E-14 ) ) ;
#66626=CARTESIAN_POINT ( 'NONE',  ( 10.05862282008599884, 4.666276081381299790, 6.425317846273999933 ) ) ;
#66700=CARTESIAN_POINT ( 'NONE',  ( 11.30995122972050027, 4.452766304612699955, 8.547040013405998948 ) ) ;
#66733=CARTESIAN_POINT ( 'NONE',  ( 10.21462282008599942, 4.523146351753199568, 6.656181553372300108 ) ) ;
#66757=CARTESIAN_POINT ( 'NONE',  ( 11.21022026213526601, 5.045753393512712570, 7.175001674908393134 ) ) ;
#66777=CARTESIAN_POINT ( 'NONE',  ( 10.10434687351566474, 5.250000000000001776, 7.663624617374461323 ) ) ;
#66781=EDGE_CURVE ( 'NONE', #21416, #43157, #15468, .T. ) ;
#66786=CARTESIAN_POINT ( 'NONE',  ( 11.59999999999999964, 5.207010770456999893, 7.174999999999999822 ) ) ;
#66805=CARTESIAN_POINT ( 'NONE',  ( 10.28441772631199846, 4.372518460886800185, 6.733203680593099705 ) ) ;
#66817=ORIENTED_EDGE ( 'NONE', *, *, #6613, .F. ) ;
#66862=CARTESIAN_POINT ( 'NONE',  ( 10.94501463001509833, 4.472480213525599879, 8.256737112932800216 ) ) ;
#66864=CARTESIAN_POINT ( 'NONE',  ( 10.16159632033899918, 3.070047649444500149, 7.879514065647800436 ) ) ;
#66880=ORIENTED_EDGE ( 'NONE', *, *, #66932, .T. ) ;
#66907=CARTESIAN_POINT ( 'NONE',  ( 8.670138961223999630, 4.946050868436800307, 6.860686042446299204 ) ) ;
#66917=CARTESIAN_POINT ( 'NONE',  ( 11.58457173739308210, 4.937225096800481161, 6.638117766810080589 ) ) ;
#66932=EDGE_CURVE ( 'NONE', #10742, #13026, #62141, .T. ) ;
#66987=FACE_OUTER_BOUND ( 'NONE', #27771, .T. ) ;
#67040=CARTESIAN_POINT ( 'NONE',  ( 10.42380110216399913, 3.026453990125600235, 8.094557215852098864 ) ) ;
#67044=ORIENTED_EDGE ( 'NONE', *, *, #6464, .F. ) ;
#67071=CARTESIAN_POINT ( 'NONE',  ( 11.25656651104150008, 4.126085365637900182, 8.771777834828998976 ) ) ;
#67138=CARTESIAN_POINT ( 'NONE',  ( 10.29262282008599882, 4.451581486939200083, 6.771613406921599854 ) ) ;
#67169=CARTESIAN_POINT ( 'NONE',  ( 8.832144816391009456, 4.216552416542988624, 6.534094574943864586 ) ) ;
#67198=CARTESIAN_POINT ( 'NONE',  ( 10.90346005378009941, 4.786957292481900161, 7.920222357891399945 ) ) ;
#67201=CARTESIAN_POINT ( 'NONE',  ( 9.327747021775998348, 3.141778309999299967, 6.746879837742599584 ) ) ;
#67207=B_SPLINE_CURVE_WITH_KNOTS ( 'NONE', 3,
 ( #51678, #57261, #24773, #15655, #52016, #46786, #41534, #36289, #9713, #31058, #46100, #52368, #4461, #20901, #36988, #3436, #48854, #59333 ),
 .UNSPECIFIED., .F., .F.,
 ( 4, 2, 2, 2, 2, 2, 2, 2, 4 ),
 ( 0.000000000000000000, 0.1250000000000000000, 0.2500000000000000000, 0.3750000000000000000, 0.5000000000000000000, 0.6250000000000000000, 0.7500000000000000000, 0.8750000000000000000, 1.000000000000000000 ),
 .UNSPECIFIED. ) ;
#67243=ORIENTED_EDGE ( 'NONE', *, *, #11924, .F. ) ;
#67248=CARTESIAN_POINT ( 'NONE',  ( 8.594151519676998419, 4.024693162376980382, 6.358456126310000123 ) ) ;
#67288=CARTESIAN_POINT ( 'NONE',  ( 11.05336220499919797, 3.034597079077000270, 7.174999999999999822 ) ) ;
#67293=EDGE_CURVE ( 'NONE', #23956, #33463, #42086, .T. ) ;
#67313=ORIENTED_EDGE ( 'NONE', *, *, #15618, .F. ) ;
#67359=CARTESIAN_POINT ( 'NONE',  ( 10.76346886766499900, 3.365322927604099679, 8.653146038559000885 ) ) ;
#67371=CARTESIAN_POINT ( 'NONE',  ( 11.48011496860029901, 4.919769165942200040, 7.971338736265699332 ) ) ;
#67377=CARTESIAN_POINT ( 'NONE',  ( 11.45764291764649911, 2.867875922590999771, 7.639947095788999221 ) ) ;
#67409=CARTESIAN_POINT ( 'NONE',  ( 11.08425954179440076, 4.982976321082899673, 6.683254058608399717 ) ) ;
#67437=CARTESIAN_POINT ( 'NONE',  ( 11.59999999999999964, 2.500145227336000087, 7.174999999999999822 ) ) ;
#67446=VECTOR ( 'NONE', #44880, 1000.000000000000227 ) ;
#67482=CARTESIAN_POINT ( 'NONE',  ( 11.53564291764652872, 3.004110626587600308, 7.623106493640399606 ) ) ;
#67495=FACE_OUTER_BOUND ( 'NONE', #61880, .T. ) ;
#67499=CARTESIAN_POINT ( 'NONE',  ( 11.04749144726329924, 3.499163784537000055, 8.206726025856399431 ) ) ;
#67529=CARTESIAN_POINT ( 'NONE',  ( 11.28830977893787768, 3.023401864784706738, 8.326430086672806041 ) ) ;
#67540=CARTESIAN_POINT ( 'NONE',  ( 11.02812378248509795, 3.583106837161099900, 8.288725998710999576 ) ) ;
#67543=CARTESIAN_POINT ( 'NONE',  ( 9.023797255587998833, 5.140789995332999851, 7.548297453605989027 ) ) ;
#67545=LINE ( 'NONE', #30503, #9791 ) ;
#67589=CARTESIAN_POINT ( 'NONE',  ( 10.10344474310099905, 5.137935629024000583, 6.947770206896899836 ) ) ;
#67595=CARTESIAN_POINT ( 'NONE',  ( 10.09393020684899867, 5.250000000000000000, 7.500000000000000000 ) ) ;
#67644=CARTESIAN_POINT ( 'NONE',  ( 10.12426357027499790, 5.254871132332000094, 7.257895958275299542 ) ) ;
#67712=CARTESIAN_POINT ( 'NONE',  ( 11.72433327354039889, 3.016779570871600313, 8.143111181492699302 ) ) ;
#67717=CARTESIAN_POINT ( 'NONE',  ( 11.08425954179440076, 4.982976321082899673, 6.683254058608399717 ) ) ;
#67748=CARTESIAN_POINT ( 'NONE',  ( 10.15303300763299887, 4.787165141710600480, 6.674373427955200277 ) ) ;
#67789=AXIS2_PLACEMENT_3D ( 'NONE', #7925, #29262, #35865 ) ;
#67794=ADVANCED_FACE ( 'NONE', ( #62836 ), #10393, .T. ) ;
#67807=CARTESIAN_POINT ( 'NONE',  ( 10.60441638348510018, 3.158410350011299883, 7.705001100909899314 ) ) ;
#67825=CARTESIAN_POINT ( 'NONE',  ( 11.26072066707849828, 4.976067344118500380, 8.090408888831799317 ) ) ;
#67830=CARTESIAN_POINT ( 'NONE',  ( 8.599999952505998024, 4.749999993641800700, 7.500000000000000000 ) ) ;
#67840=CARTESIAN_POINT ( 'NONE',  ( 9.343930206849998754, 2.750000000000000000, 7.500000000000000000 ) ) ;
#67853=CARTESIAN_POINT ( 'NONE',  ( 9.466846873515667227, 3.231816600031355069, 6.500416447002276499 ) ) ;
#67890=CARTESIAN_POINT ( 'NONE',  ( 10.31155864497999808, 4.682585200569199912, 6.965412239408199646 ) ) ;
#67937=CARTESIAN_POINT ( 'NONE',  ( 8.668126402770999661, 5.196937059091999878, 7.951360234587600218 ) ) ;
#67968=FACE_OUTER_BOUND ( 'NONE', #2266, .T. ) ;
#67970=CARTESIAN_POINT ( 'NONE',  ( 10.56244474310100045, 5.137935629024000583, 6.947770206896899836 ) ) ;
#67997=EDGE_LOOP ( 'NONE', ( #51061, #3188, #62355 ) ) ;
#68018=CARTESIAN_POINT ( 'NONE',  ( 11.59999999999999964, 5.386831235742000068, 7.825000000000000178 ) ) ;
#68051=CARTESIAN_POINT ( 'NONE',  ( 11.80233327354039830, 2.898463260143000042, 8.220500279733599314 ) ) ;
#68059=CARTESIAN_POINT ( 'NONE',  ( 11.18412378248529926, 3.450971646934100079, 8.538714411016998795 ) ) ;
#68064=CARTESIAN_POINT ( 'NONE',  ( 10.78887616594230003, 3.613544262574699850, 8.718182393403999697 ) ) ;
#68080=DIRECTION ( 'NONE',  ( -1.000000000000000000, 0.000000000000000000, 0.000000000000000000 ) ) ;
#68095=CARTESIAN_POINT ( 'NONE',  ( 11.28118179236249929, 3.732952383914999839, 8.749800764654999341 ) ) ;
#68099=CARTESIAN_POINT ( 'NONE',  ( 10.68559687351635112, 5.092232985442825210, 8.129523725463618788 ) ) ;
#68150=CARTESIAN_POINT ( 'NONE',  ( 11.17056785386839834, 3.281375110759499947, 7.016391833292499491 ) ) ;
#68165=CARTESIAN_POINT ( 'NONE',  ( 10.62072335273219892, 4.397090433355999473, 6.430603299050000388 ) ) ;
#68176=VERTEX_POINT ( 'NONE', #15900 ) ;
#68182=CARTESIAN_POINT ( 'NONE',  ( 11.85979573085659844, 4.840012015667699785, 7.354650721737899133 ) ) ;
#68221=ORIENTED_EDGE ( 'NONE', *, *, #17175, .F. ) ;
#68222=B_SPLINE_CURVE_WITH_KNOTS ( 'NONE', 3,
 ( #33208, #43699, #64995, #59767, #54526, #6628, #61497, #62174, #24093, #45426, #13274, #29016, #34938, #7669, #14297, #40509, #44743, #35625 ),
 .UNSPECIFIED., .F., .F.,
 ( 4, 2, 2, 2, 2, 2, 2, 2, 4 ),
 ( 0.000000000000000000, 0.1249999999999996669, 0.2499999999999993339, 0.3749999999999990008, 0.4999999999999986677, 0.6249999999999990008, 0.7499999999999993339, 0.8749999999999996669, 1.000000000000000000 ),
 .UNSPECIFIED. ) ;
#68226=CARTESIAN_POINT ( 'NONE',  ( 9.123101285863999266, 3.353260484332500013, 8.268485718282699182 ) ) ;
#68259=CARTESIAN_POINT ( 'NONE',  ( 11.51656039236534923, 5.173498198882000132, 7.442888368925779652 ) ) ;
#68272=( NAMED_UNIT ( * ) SI_UNIT ( $, .STERADIAN. ) SOLID_ANGLE_UNIT ( ) );
#68274=CARTESIAN_POINT ( 'NONE',  ( 9.554646554150998838, 4.619310611972400338, 6.380697202105999999 ) ) ;
#68285=CARTESIAN_POINT ( 'NONE',  ( 8.810863317747999801, 4.960863370448500120, 7.499999999926881600 ) ) ;
#68306=CARTESIAN_POINT ( 'NONE',  ( 9.735025935145998233, 3.814256956409300070, 8.765655525501999890 ) ) ;
#68354=ORIENTED_EDGE ( 'NONE', *, *, #21180, .T. ) ;
#68360=PLANE ( 'NONE',  #37504 ) ;
#68389=CARTESIAN_POINT ( 'NONE',  ( 11.09590547754519996, 5.315605332491999846, 7.458246194669389872 ) ) ;
#68397=CARTESIAN_POINT ( 'NONE',  ( 11.43345123989529810, 4.540230239159599890, 6.456682674800999777 ) ) ;
#68402=CARTESIAN_POINT ( 'NONE',  ( 10.20226357027499908, 5.120085139777000194, 7.283900408233900059 ) ) ;
#68406=CARTESIAN_POINT ( 'NONE',  ( 8.724024145839393896, 3.782477278638352036, 6.654559194835224289 ) ) ;
#68408=EDGE_CURVE ( 'NONE', #60390, #51100, #12739, .T. ) ;
#68413=AXIS2_PLACEMENT_3D ( 'NONE', #48120, #49151, #6498 ) ;
#68429=ORIENTED_EDGE ( 'NONE', *, *, #54208, .T. ) ;
#68480=STYLED_ITEM ( 'NONE', ( #58145 ), #30727 ) ;
#68491=CARTESIAN_POINT ( 'NONE',  ( 10.40749413291699987, 4.788043169210699723, 7.859564368461399830 ) ) ;
#68508=CARTESIAN_POINT ( 'NONE',  ( 10.52226222744799955, 3.119510978356100139, 6.774721295617600170 ) ) ;
#68524=CARTESIAN_POINT ( 'NONE',  ( 11.09672200990539892, 3.182132064022000328, 7.785290430335599865 ) ) ;
#68551=CARTESIAN_POINT ( 'NONE',  ( 8.705629240797998492, 3.771058080785100408, 6.623477632995699693 ) ) ;
#68569=CARTESIAN_POINT ( 'NONE',  ( 10.24809687351608289, 4.327184855449106138, 8.717465845835393523 ) ) ;
#68571=CARTESIAN_POINT ( 'NONE',  ( 8.971126402771000485, 4.939810497841199854, 7.854398824525599565 ) ) ;
#68576=VERTEX_POINT ( 'NONE', #25630 ) ;
#68599=ORIENTED_EDGE ( 'NONE', *, *, #65832, .F. ) ;
#68604=CARTESIAN_POINT ( 'NONE',  ( 11.26723293495529887, 2.826061044294000180, 7.547192037433419820 ) ) ;
#68611=EDGE_CURVE ( 'NONE', #19003, #26690, #58671, .T. ) ;
#68631=CARTESIAN_POINT ( 'NONE',  ( 8.824071121570657539, 4.974071175014779911, 7.751553442067931954 ) ) ;
#68632=CARTESIAN_POINT ( 'NONE',  ( 11.54684497800060150, 3.023157657667436826, 7.175001354288133015 ) ) ;
#68653=CARTESIAN_POINT ( 'NONE',  ( 10.24160887879199855, 3.710311786319799854, 8.745979585038000437 ) ) ;
#68698=CARTESIAN_POINT ( 'NONE',  ( 11.60000000000000497, 3.552887809908070960, 8.372281669763946610 ) ) ;
#68748=CARTESIAN_POINT ( 'NONE',  ( 11.67403632436368888, 3.023821283238099955, 7.727966254184200245 ) ) ;
#68753=CARTESIAN_POINT ( 'NONE',  ( 10.46887750876899936, 3.307728619566300043, 6.425720373262999274 ) ) ;
#68842=CARTESIAN_POINT ( 'NONE',  ( 10.57980110216399972, 3.260758259645400337, 7.951464549725199227 ) ) ;
#68856=CARTESIAN_POINT ( 'NONE',  ( 10.32949413291699869, 4.912929163218899831, 7.916546720849799712 ) ) ;
#68867=CARTESIAN_POINT ( 'NONE',  ( 10.97755399909358154, 4.133346405062088280, 6.221473734489901375 ) ) ;
#68872=CARTESIAN_POINT ( 'NONE',  ( 11.78594988689359901, 4.393436444036099786, 6.728309553046099012 ) ) ;
#68924=CARTESIAN_POINT ( 'NONE',  ( 10.23557120343299864, 3.957971921952620598, 6.634008278083699750 ) ) ;
#68930=EDGE_LOOP ( 'NONE', ( #9963, #43112, #64798 ) ) ;
#68956=FACE_OUTER_BOUND ( 'NONE', #28585, .T. ) ;
#68973=CARTESIAN_POINT ( 'NONE',  ( 8.921417874593998931, 2.822750429186000165, 6.999532383170999239 ) ) ;
#68992=CYLINDRICAL_SURFACE ( 'NONE', #63844, 1.250000000000000222 ) ;
#69005=CARTESIAN_POINT ( 'NONE',  ( 9.507063610504999929, 4.524705472883399970, 6.333351572150998976 ) ) ;
#69053=CARTESIAN_POINT ( 'NONE',  ( 11.59999999999999964, 3.850275034462829815, 8.514310854298580367 ) ) ;
#69080=B_SPLINE_CURVE_WITH_KNOTS ( 'NONE', 3,
 ( #3557, #14413, #25581, #30486, #46908, #19298, #51799, #67529, #24201, #62296 ),
 .UNSPECIFIED., .F., .F.,
 ( 4, 2, 2, 2, 4 ),
 ( 0.000000000000000000, 0.2499999999999997780, 0.4999999999999995559, 0.7499999999999997780, 1.000000000000000000 ),
 .UNSPECIFIED. ) ;
#69137=VERTEX_POINT ( 'NONE', #33732 ) ;
#69186=CARTESIAN_POINT ( 'NONE',  ( 10.92441504065829960, 4.694414232677499577, 8.017771632862299214 ) ) ;
ENDSEC;
END-ISO-10303-21;
